ISO-10303-21;
HEADER;
/* Generated by software containing ST-Developer
 * from STEP Tools, Inc. (www.steptools.com) 
 */

FILE_DESCRIPTION(
/* description */ ('', 'CAx-IF Rec.Pracs.---Representation and Presentation of Product Manufa
cturing Information (PMI)---4.0---2014-10-13'),
/* implementation_level */ '2;1');

FILE_NAME(
/* name */ 'Screw M3.step',
/* time_stamp */ '2026-10-28T14:45:12+01:00',
/* author */ (''),
/* organization */ (''),
/* preprocessor_version */ 'ST-DEVELOPER v20.2',
/* originating_system */ 'Autodesk Translation Framework v15.17.0.0',
/* authorisation */ '');

FILE_SCHEMA (('AP242_MANAGED_MODEL_BASED_3D_ENGINEERING_MIM_LF { 1 0 10303 442 2 1 4 }'));
ENDSEC;

DATA;
#10=MECHANICAL_DESIGN_GEOMETRIC_PRESENTATION_REPRESENTATION('',(#262),#52164);
#63=(
BOUNDED_CURVE()
B_SPLINE_CURVE(2,(#29010,#29011,#29012),.UNSPECIFIED.,.F.,.F.)
B_SPLINE_CURVE_WITH_KNOTS((3,3),(-1.41025055977478,-0.304692654014095),
 .UNSPECIFIED.)
CURVE()
GEOMETRIC_REPRESENTATION_ITEM()
RATIONAL_B_SPLINE_CURVE((0.957089080441345,0.830796931423118,1.))
REPRESENTATION_ITEM('')
);
#65=ELLIPSE('',#9725,0.771415586451778,0.0652711480392958);
#66=ELLIPSE('',#9726,0.771415586451778,0.0652711480392958);
#67=ELLIPSE('',#9729,0.771415586459596,0.0652711480406291);
#68=ELLIPSE('',#9733,0.251906298612587,0.25);
#69=ELLIPSE('',#9735,0.251906298612587,0.25);
#70=ELLIPSE('',#9736,0.251906298612587,0.25);
#71=ELLIPSE('',#9737,0.251906298612587,0.25);
#72=ELLIPSE('',#9738,0.251906298612587,0.25);
#73=ELLIPSE('',#9739,0.251906298612587,0.25);
#74=ELLIPSE('',#9740,0.251906298612587,0.25);
#75=ELLIPSE('',#9741,0.251906298612587,0.25);
#76=ELLIPSE('',#9742,0.251906298612587,0.25);
#77=ELLIPSE('',#9743,0.251906298612587,0.25);
#78=ELLIPSE('',#9744,0.251906298612587,0.25);
#79=ELLIPSE('',#9745,0.251906298612587,0.25);
#80=ELLIPSE('',#9748,0.251906298612587,0.25);
#81=ELLIPSE('',#9750,0.251906298612587,0.25);
#82=ELLIPSE('',#9752,0.251906298612587,0.25);
#83=ELLIPSE('',#9754,0.251906298612587,0.25);
#127=(
BOUNDED_SURFACE()
B_SPLINE_SURFACE(2,2,((#28929,#28930,#28931,#28932,#28933,#28934,#28935,
#28936,#28937),(#28938,#28939,#28940,#28941,#28942,#28943,#28944,#28945,
#28946),(#28947,#28948,#28949,#28950,#28951,#28952,#28953,#28954,#28955)),
 .UNSPECIFIED.,.F.,.T.,.F.)
B_SPLINE_SURFACE_WITH_KNOTS((3,3),(3,2,2,2,3),(0.304692654014095,1.57079632680149),
(-3.14159265358979,-1.5707963267949,0.,1.5707963267949,3.14159265358979),
 .UNSPECIFIED.)
GEOMETRIC_REPRESENTATION_ITEM()
RATIONAL_B_SPLINE_SURFACE(((1.,0.707106781186548,1.,0.707106781186548,1.,
0.707106781186548,1.,0.707106781186548,1.),(0.806225774827519,0.570087712547917,
0.806225774827519,0.570087712547917,0.806225774827519,0.570087712547917,
0.806225774827519,0.570087712547917,0.806225774827519),(1.,0.707106781186548,
1.,0.707106781186548,1.,0.707106781186548,1.,0.707106781186548,1.)))
REPRESENTATION_ITEM('')
SURFACE()
);
#199=CONICAL_SURFACE('',#9705,1.393148400081,0.349065850398866);
#200=CONICAL_SURFACE('',#9711,1.308493649054,1.0471975511966);
#201=CONICAL_SURFACE('',#9717,1.393148400081,0.349065850398866);
#209=TOROIDAL_SURFACE('',#9712,1.707288968431,0.4);
#236=SHAPE_REPRESENTATION_RELATIONSHIP('SRR','None',#52215,#249);
#249=ADVANCED_BREP_SHAPE_REPRESENTATION('',(#275),#52155);
#262=STYLED_ITEM('',(#52325),#275);
#275=MANIFOLD_SOLID_BREP('Body1',#9122);
#299=FACE_BOUND('',#1298,.T.);
#358=B_SPLINE_SURFACE_WITH_KNOTS('',3,3,((#25222,#25223,#25224,#25225,#25226,
#25227,#25228,#25229,#25230,#25231,#25232,#25233,#25234,#25235,#25236,#25237,
#25238,#25239,#25240,#25241,#25242,#25243,#25244,#25245,#25246,#25247,#25248,
#25249,#25250,#25251,#25252,#25253,#25254,#25255,#25256),(#25257,#25258,
#25259,#25260,#25261,#25262,#25263,#25264,#25265,#25266,#25267,#25268,#25269,
#25270,#25271,#25272,#25273,#25274,#25275,#25276,#25277,#25278,#25279,#25280,
#25281,#25282,#25283,#25284,#25285,#25286,#25287,#25288,#25289,#25290,#25291),
(#25292,#25293,#25294,#25295,#25296,#25297,#25298,#25299,#25300,#25301,
#25302,#25303,#25304,#25305,#25306,#25307,#25308,#25309,#25310,#25311,#25312,
#25313,#25314,#25315,#25316,#25317,#25318,#25319,#25320,#25321,#25322,#25323,
#25324,#25325,#25326),(#25327,#25328,#25329,#25330,#25331,#25332,#25333,
#25334,#25335,#25336,#25337,#25338,#25339,#25340,#25341,#25342,#25343,#25344,
#25345,#25346,#25347,#25348,#25349,#25350,#25351,#25352,#25353,#25354,#25355,
#25356,#25357,#25358,#25359,#25360,#25361)),.UNSPECIFIED.,.F.,.F.,.F.,(4,
4),(4,1,1,1,1,1,1,1,1,1,1,1,1,1,1,1,1,1,1,1,1,1,1,1,1,1,1,1,1,1,1,1,4),
(-0.2772301033111,1.277230103311),(-0.02,0.0125,0.045,0.0775,0.11,0.1425,
0.175,0.2075,0.24,0.2725,0.305,0.3375,0.37,0.4025,0.435,0.4675,0.5,0.5325,
0.565,0.5975,0.63,0.6625,0.695,0.7275,0.76,0.7925,0.825,0.8575,0.89,0.9225,
0.955,0.9875,1.02),.UNSPECIFIED.);
#359=B_SPLINE_SURFACE_WITH_KNOTS('',3,3,((#25881,#25882,#25883,#25884,#25885,
#25886,#25887,#25888,#25889,#25890,#25891,#25892,#25893,#25894,#25895,#25896,
#25897,#25898,#25899,#25900,#25901,#25902,#25903,#25904,#25905,#25906,#25907,
#25908,#25909,#25910,#25911,#25912,#25913,#25914,#25915),(#25916,#25917,
#25918,#25919,#25920,#25921,#25922,#25923,#25924,#25925,#25926,#25927,#25928,
#25929,#25930,#25931,#25932,#25933,#25934,#25935,#25936,#25937,#25938,#25939,
#25940,#25941,#25942,#25943,#25944,#25945,#25946,#25947,#25948,#25949,#25950),
(#25951,#25952,#25953,#25954,#25955,#25956,#25957,#25958,#25959,#25960,
#25961,#25962,#25963,#25964,#25965,#25966,#25967,#25968,#25969,#25970,#25971,
#25972,#25973,#25974,#25975,#25976,#25977,#25978,#25979,#25980,#25981,#25982,
#25983,#25984,#25985),(#25986,#25987,#25988,#25989,#25990,#25991,#25992,
#25993,#25994,#25995,#25996,#25997,#25998,#25999,#26000,#26001,#26002,#26003,
#26004,#26005,#26006,#26007,#26008,#26009,#26010,#26011,#26012,#26013,#26014,
#26015,#26016,#26017,#26018,#26019,#26020)),.UNSPECIFIED.,.F.,.F.,.F.,(4,
4),(4,1,1,1,1,1,1,1,1,1,1,1,1,1,1,1,1,1,1,1,1,1,1,1,1,1,1,1,1,1,1,1,4),
(-0.03619071925572,1.036190719256),(-0.02,0.0125,0.045,0.0775,0.11,0.1425,
0.175,0.2075,0.24,0.2725,0.305,0.3375,0.37,0.4025,0.435,0.4675,0.5,0.5325,
0.565,0.5975,0.63,0.6625,0.695,0.7275,0.76,0.7925,0.825,0.8575,0.89,0.9225,
0.955,0.9875,1.02),.UNSPECIFIED.);
#360=B_SPLINE_SURFACE_WITH_KNOTS('',3,3,((#26236,#26237,#26238,#26239,#26240,
#26241,#26242,#26243,#26244,#26245,#26246,#26247,#26248,#26249,#26250,#26251,
#26252,#26253,#26254,#26255,#26256,#26257,#26258,#26259,#26260,#26261,#26262,
#26263,#26264,#26265,#26266,#26267,#26268,#26269,#26270),(#26271,#26272,
#26273,#26274,#26275,#26276,#26277,#26278,#26279,#26280,#26281,#26282,#26283,
#26284,#26285,#26286,#26287,#26288,#26289,#26290,#26291,#26292,#26293,#26294,
#26295,#26296,#26297,#26298,#26299,#26300,#26301,#26302,#26303,#26304,#26305),
(#26306,#26307,#26308,#26309,#26310,#26311,#26312,#26313,#26314,#26315,
#26316,#26317,#26318,#26319,#26320,#26321,#26322,#26323,#26324,#26325,#26326,
#26327,#26328,#26329,#26330,#26331,#26332,#26333,#26334,#26335,#26336,#26337,
#26338,#26339,#26340),(#26341,#26342,#26343,#26344,#26345,#26346,#26347,
#26348,#26349,#26350,#26351,#26352,#26353,#26354,#26355,#26356,#26357,#26358,
#26359,#26360,#26361,#26362,#26363,#26364,#26365,#26366,#26367,#26368,#26369,
#26370,#26371,#26372,#26373,#26374,#26375)),.UNSPECIFIED.,.F.,.F.,.F.,(4,
4),(4,1,1,1,1,1,1,1,1,1,1,1,1,1,1,1,1,1,1,1,1,1,1,1,1,1,1,1,1,1,1,1,4),
(-0.03619071925572,1.036190719256),(0.01365127283277,0.04507905090427,0.07650682897578,
0.1079346070473,0.1393623851188,0.1707901631903,0.2022179412618,0.2336457193333,
0.2650734974048,0.2965012754763,0.3279290535478,0.3593568316193,0.3907846096908,
0.4222123877623,0.4536401658338,0.4850679439053,0.5164957219768,0.5479235000484,
0.5793512781199,0.6107790561914,0.6422068342629,0.6736346123344,0.7050623904059,
0.7364901684774,0.7679179465489,0.7993457246204,0.8307735026919,0.8622012807634,
0.8936290588349,0.9250568369064,0.9564846149779,0.9879123930494,1.019340171121),
 .UNSPECIFIED.);
#361=B_SPLINE_SURFACE_WITH_KNOTS('',3,3,((#26377,#26378,#26379,#26380,#26381,
#26382,#26383,#26384,#26385,#26386,#26387,#26388,#26389,#26390,#26391,#26392,
#26393,#26394,#26395,#26396,#26397,#26398,#26399,#26400,#26401,#26402,#26403,
#26404,#26405,#26406,#26407,#26408,#26409,#26410,#26411),(#26412,#26413,
#26414,#26415,#26416,#26417,#26418,#26419,#26420,#26421,#26422,#26423,#26424,
#26425,#26426,#26427,#26428,#26429,#26430,#26431,#26432,#26433,#26434,#26435,
#26436,#26437,#26438,#26439,#26440,#26441,#26442,#26443,#26444,#26445,#26446),
(#26447,#26448,#26449,#26450,#26451,#26452,#26453,#26454,#26455,#26456,
#26457,#26458,#26459,#26460,#26461,#26462,#26463,#26464,#26465,#26466,#26467,
#26468,#26469,#26470,#26471,#26472,#26473,#26474,#26475,#26476,#26477,#26478,
#26479,#26480,#26481),(#26482,#26483,#26484,#26485,#26486,#26487,#26488,
#26489,#26490,#26491,#26492,#26493,#26494,#26495,#26496,#26497,#26498,#26499,
#26500,#26501,#26502,#26503,#26504,#26505,#26506,#26507,#26508,#26509,#26510,
#26511,#26512,#26513,#26514,#26515,#26516)),.UNSPECIFIED.,.F.,.F.,.F.,(4,
4),(4,1,1,1,1,1,1,1,1,1,1,1,1,1,1,1,1,1,1,1,1,1,1,1,1,1,1,1,1,1,1,1,4),
(-0.03619071925572,1.036190719256),(-0.02,0.0125,0.045,0.0775,0.11,0.1425,
0.175,0.2075,0.24,0.2725,0.305,0.3375,0.37,0.4025,0.435,0.4675,0.5,0.5325,
0.565,0.5975,0.63,0.6625,0.695,0.7275,0.76,0.7925,0.825,0.8575,0.89,0.9225,
0.955,0.9875,1.02),.UNSPECIFIED.);
#362=B_SPLINE_SURFACE_WITH_KNOTS('',3,3,((#26768,#26769,#26770,#26771,#26772,
#26773,#26774,#26775,#26776,#26777,#26778,#26779,#26780,#26781,#26782,#26783,
#26784,#26785,#26786,#26787,#26788,#26789,#26790,#26791,#26792,#26793,#26794,
#26795,#26796,#26797,#26798,#26799,#26800,#26801,#26802),(#26803,#26804,
#26805,#26806,#26807,#26808,#26809,#26810,#26811,#26812,#26813,#26814,#26815,
#26816,#26817,#26818,#26819,#26820,#26821,#26822,#26823,#26824,#26825,#26826,
#26827,#26828,#26829,#26830,#26831,#26832,#26833,#26834,#26835,#26836,#26837),
(#26838,#26839,#26840,#26841,#26842,#26843,#26844,#26845,#26846,#26847,
#26848,#26849,#26850,#26851,#26852,#26853,#26854,#26855,#26856,#26857,#26858,
#26859,#26860,#26861,#26862,#26863,#26864,#26865,#26866,#26867,#26868,#26869,
#26870,#26871,#26872),(#26873,#26874,#26875,#26876,#26877,#26878,#26879,
#26880,#26881,#26882,#26883,#26884,#26885,#26886,#26887,#26888,#26889,#26890,
#26891,#26892,#26893,#26894,#26895,#26896,#26897,#26898,#26899,#26900,#26901,
#26902,#26903,#26904,#26905,#26906,#26907)),.UNSPECIFIED.,.F.,.F.,.F.,(4,
4),(4,1,1,1,1,1,1,1,1,1,1,1,1,1,1,1,1,1,1,1,1,1,1,1,1,1,1,1,1,1,1,1,4),
(-0.2772301033111,1.277230103311),(-0.02,0.0125,0.045,0.0775,0.11,0.1425,
0.175,0.2075,0.24,0.2725,0.305,0.3375,0.37,0.4025,0.435,0.4675,0.5,0.5325,
0.565,0.5975,0.63,0.6625,0.695,0.7275,0.76,0.7925,0.825,0.8575,0.89,0.9225,
0.955,0.9875,1.02),.UNSPECIFIED.);
#363=B_SPLINE_SURFACE_WITH_KNOTS('',3,3,((#27028,#27029,#27030,#27031,#27032,
#27033,#27034,#27035,#27036,#27037,#27038,#27039,#27040,#27041,#27042,#27043,
#27044,#27045,#27046,#27047,#27048,#27049,#27050,#27051,#27052,#27053,#27054,
#27055,#27056,#27057,#27058,#27059,#27060,#27061,#27062),(#27063,#27064,
#27065,#27066,#27067,#27068,#27069,#27070,#27071,#27072,#27073,#27074,#27075,
#27076,#27077,#27078,#27079,#27080,#27081,#27082,#27083,#27084,#27085,#27086,
#27087,#27088,#27089,#27090,#27091,#27092,#27093,#27094,#27095,#27096,#27097),
(#27098,#27099,#27100,#27101,#27102,#27103,#27104,#27105,#27106,#27107,
#27108,#27109,#27110,#27111,#27112,#27113,#27114,#27115,#27116,#27117,#27118,
#27119,#27120,#27121,#27122,#27123,#27124,#27125,#27126,#27127,#27128,#27129,
#27130,#27131,#27132),(#27133,#27134,#27135,#27136,#27137,#27138,#27139,
#27140,#27141,#27142,#27143,#27144,#27145,#27146,#27147,#27148,#27149,#27150,
#27151,#27152,#27153,#27154,#27155,#27156,#27157,#27158,#27159,#27160,#27161,
#27162,#27163,#27164,#27165,#27166,#27167)),.UNSPECIFIED.,.F.,.F.,.F.,(4,
4),(4,1,1,1,1,1,1,1,1,1,1,1,1,1,1,1,1,1,1,1,1,1,1,1,1,1,1,1,1,1,1,1,4),
(-0.03619071925572,1.036190719256),(-0.02,0.0125,0.045,0.0775,0.11,0.1425,
0.175,0.2075,0.24,0.2725,0.305,0.3375,0.37,0.4025,0.435,0.4675,0.5,0.5325,
0.565,0.5975,0.63,0.6625,0.695,0.7275,0.76,0.7925,0.825,0.8575,0.89,0.9225,
0.955,0.9875,1.02),.UNSPECIFIED.);
#364=B_SPLINE_SURFACE_WITH_KNOTS('',3,3,((#27212,#27213,#27214,#27215,#27216,
#27217,#27218,#27219,#27220,#27221,#27222,#27223,#27224,#27225,#27226,#27227,
#27228,#27229,#27230,#27231,#27232,#27233,#27234,#27235,#27236,#27237,#27238,
#27239,#27240,#27241,#27242,#27243,#27244,#27245,#27246),(#27247,#27248,
#27249,#27250,#27251,#27252,#27253,#27254,#27255,#27256,#27257,#27258,#27259,
#27260,#27261,#27262,#27263,#27264,#27265,#27266,#27267,#27268,#27269,#27270,
#27271,#27272,#27273,#27274,#27275,#27276,#27277,#27278,#27279,#27280,#27281),
(#27282,#27283,#27284,#27285,#27286,#27287,#27288,#27289,#27290,#27291,
#27292,#27293,#27294,#27295,#27296,#27297,#27298,#27299,#27300,#27301,#27302,
#27303,#27304,#27305,#27306,#27307,#27308,#27309,#27310,#27311,#27312,#27313,
#27314,#27315,#27316),(#27317,#27318,#27319,#27320,#27321,#27322,#27323,
#27324,#27325,#27326,#27327,#27328,#27329,#27330,#27331,#27332,#27333,#27334,
#27335,#27336,#27337,#27338,#27339,#27340,#27341,#27342,#27343,#27344,#27345,
#27346,#27347,#27348,#27349,#27350,#27351)),.UNSPECIFIED.,.F.,.F.,.F.,(4,
4),(4,1,1,1,1,1,1,1,1,1,1,1,1,1,1,1,1,1,1,1,1,1,1,1,1,1,1,1,1,1,1,1,4),
(-0.03619071925572,1.036190719256),(-0.02,0.0125,0.045,0.0775,0.11,0.1425,
0.175,0.2075,0.24,0.2725,0.305,0.3375,0.37,0.4025,0.435,0.4675,0.5,0.5325,
0.565,0.5975,0.63,0.6625,0.695,0.7275,0.76,0.7925,0.825,0.8575,0.89,0.9225,
0.955,0.9875,1.02),.UNSPECIFIED.);
#365=B_SPLINE_SURFACE_WITH_KNOTS('',3,3,((#27603,#27604,#27605,#27606,#27607,
#27608,#27609,#27610,#27611,#27612,#27613,#27614,#27615,#27616,#27617,#27618,
#27619,#27620,#27621,#27622,#27623,#27624,#27625,#27626,#27627,#27628,#27629,
#27630,#27631,#27632,#27633,#27634,#27635,#27636,#27637),(#27638,#27639,
#27640,#27641,#27642,#27643,#27644,#27645,#27646,#27647,#27648,#27649,#27650,
#27651,#27652,#27653,#27654,#27655,#27656,#27657,#27658,#27659,#27660,#27661,
#27662,#27663,#27664,#27665,#27666,#27667,#27668,#27669,#27670,#27671,#27672),
(#27673,#27674,#27675,#27676,#27677,#27678,#27679,#27680,#27681,#27682,
#27683,#27684,#27685,#27686,#27687,#27688,#27689,#27690,#27691,#27692,#27693,
#27694,#27695,#27696,#27697,#27698,#27699,#27700,#27701,#27702,#27703,#27704,
#27705,#27706,#27707),(#27708,#27709,#27710,#27711,#27712,#27713,#27714,
#27715,#27716,#27717,#27718,#27719,#27720,#27721,#27722,#27723,#27724,#27725,
#27726,#27727,#27728,#27729,#27730,#27731,#27732,#27733,#27734,#27735,#27736,
#27737,#27738,#27739,#27740,#27741,#27742)),.UNSPECIFIED.,.F.,.F.,.F.,(4,
4),(4,1,1,1,1,1,1,1,1,1,1,1,1,1,1,1,1,1,1,1,1,1,1,1,1,1,1,1,1,1,1,1,4),
(-0.2772301033111,1.277230103311),(-0.02,0.0125,0.045,0.0775,0.11,0.1425,
0.175,0.2075,0.24,0.2725,0.305,0.3375,0.37,0.4025,0.435,0.4675,0.5,0.5325,
0.565,0.5975,0.63,0.6625,0.695,0.7275,0.76,0.7925,0.825,0.8575,0.89,0.9225,
0.955,0.9875,1.02),.UNSPECIFIED.);
#366=B_SPLINE_SURFACE_WITH_KNOTS('',3,3,((#27863,#27864,#27865,#27866,#27867,
#27868,#27869,#27870,#27871,#27872,#27873,#27874,#27875,#27876,#27877,#27878,
#27879,#27880,#27881,#27882,#27883,#27884,#27885,#27886,#27887,#27888,#27889,
#27890,#27891,#27892,#27893,#27894,#27895,#27896,#27897),(#27898,#27899,
#27900,#27901,#27902,#27903,#27904,#27905,#27906,#27907,#27908,#27909,#27910,
#27911,#27912,#27913,#27914,#27915,#27916,#27917,#27918,#27919,#27920,#27921,
#27922,#27923,#27924,#27925,#27926,#27927,#27928,#27929,#27930,#27931,#27932),
(#27933,#27934,#27935,#27936,#27937,#27938,#27939,#27940,#27941,#27942,
#27943,#27944,#27945,#27946,#27947,#27948,#27949,#27950,#27951,#27952,#27953,
#27954,#27955,#27956,#27957,#27958,#27959,#27960,#27961,#27962,#27963,#27964,
#27965,#27966,#27967),(#27968,#27969,#27970,#27971,#27972,#27973,#27974,
#27975,#27976,#27977,#27978,#27979,#27980,#27981,#27982,#27983,#27984,#27985,
#27986,#27987,#27988,#27989,#27990,#27991,#27992,#27993,#27994,#27995,#27996,
#27997,#27998,#27999,#28000,#28001,#28002)),.UNSPECIFIED.,.F.,.F.,.F.,(4,
4),(4,1,1,1,1,1,1,1,1,1,1,1,1,1,1,1,1,1,1,1,1,1,1,1,1,1,1,1,1,1,1,1,4),
(-0.03619071925572,1.036190719256),(-0.02,0.0125,0.045,0.0775,0.11,0.1425,
0.175,0.2075,0.24,0.2725,0.305,0.3375,0.37,0.4025,0.435,0.4675,0.5,0.5325,
0.565,0.5975,0.63,0.6625,0.695,0.7275,0.76,0.7925,0.825,0.8575,0.89,0.9225,
0.955,0.9875,1.02),.UNSPECIFIED.);
#367=B_SPLINE_SURFACE_WITH_KNOTS('',3,3,((#28047,#28048,#28049,#28050,#28051,
#28052,#28053,#28054,#28055,#28056,#28057,#28058,#28059,#28060,#28061,#28062,
#28063,#28064,#28065,#28066,#28067,#28068,#28069,#28070,#28071,#28072,#28073,
#28074,#28075,#28076,#28077,#28078,#28079,#28080,#28081),(#28082,#28083,
#28084,#28085,#28086,#28087,#28088,#28089,#28090,#28091,#28092,#28093,#28094,
#28095,#28096,#28097,#28098,#28099,#28100,#28101,#28102,#28103,#28104,#28105,
#28106,#28107,#28108,#28109,#28110,#28111,#28112,#28113,#28114,#28115,#28116),
(#28117,#28118,#28119,#28120,#28121,#28122,#28123,#28124,#28125,#28126,
#28127,#28128,#28129,#28130,#28131,#28132,#28133,#28134,#28135,#28136,#28137,
#28138,#28139,#28140,#28141,#28142,#28143,#28144,#28145,#28146,#28147,#28148,
#28149,#28150,#28151),(#28152,#28153,#28154,#28155,#28156,#28157,#28158,
#28159,#28160,#28161,#28162,#28163,#28164,#28165,#28166,#28167,#28168,#28169,
#28170,#28171,#28172,#28173,#28174,#28175,#28176,#28177,#28178,#28179,#28180,
#28181,#28182,#28183,#28184,#28185,#28186)),.UNSPECIFIED.,.F.,.F.,.F.,(4,
4),(4,1,1,1,1,1,1,1,1,1,1,1,1,1,1,1,1,1,1,1,1,1,1,1,1,1,1,1,1,1,1,1,4),
(-0.03619071925572,1.036190719256),(-0.02,0.0125,0.045,0.0775,0.11,0.1425,
0.175,0.2075,0.24,0.2725,0.305,0.3375,0.37,0.4025,0.435,0.4675,0.5,0.5325,
0.565,0.5975,0.63,0.6625,0.695,0.7275,0.76,0.7925,0.825,0.8575,0.89,0.9225,
0.955,0.9875,1.02),.UNSPECIFIED.);
#368=B_SPLINE_SURFACE_WITH_KNOTS('',3,3,((#28449,#28450,#28451,#28452,#28453,
#28454,#28455,#28456,#28457,#28458,#28459,#28460,#28461,#28462,#28463,#28464,
#28465,#28466,#28467,#28468,#28469,#28470,#28471,#28472,#28473,#28474,#28475,
#28476,#28477,#28478,#28479,#28480,#28481,#28482,#28483),(#28484,#28485,
#28486,#28487,#28488,#28489,#28490,#28491,#28492,#28493,#28494,#28495,#28496,
#28497,#28498,#28499,#28500,#28501,#28502,#28503,#28504,#28505,#28506,#28507,
#28508,#28509,#28510,#28511,#28512,#28513,#28514,#28515,#28516,#28517,#28518),
(#28519,#28520,#28521,#28522,#28523,#28524,#28525,#28526,#28527,#28528,
#28529,#28530,#28531,#28532,#28533,#28534,#28535,#28536,#28537,#28538,#28539,
#28540,#28541,#28542,#28543,#28544,#28545,#28546,#28547,#28548,#28549,#28550,
#28551,#28552,#28553),(#28554,#28555,#28556,#28557,#28558,#28559,#28560,
#28561,#28562,#28563,#28564,#28565,#28566,#28567,#28568,#28569,#28570,#28571,
#28572,#28573,#28574,#28575,#28576,#28577,#28578,#28579,#28580,#28581,#28582,
#28583,#28584,#28585,#28586,#28587,#28588)),.UNSPECIFIED.,.F.,.F.,.F.,(4,
4),(4,1,1,1,1,1,1,1,1,1,1,1,1,1,1,1,1,1,1,1,1,1,1,1,1,1,1,1,1,1,1,1,4),
(-0.03619071925572,1.036190719256),(-0.02,0.0125,0.045,0.0775,0.11,0.1425,
0.175,0.2075,0.24,0.2725,0.305,0.3375,0.37,0.4025,0.435,0.4675,0.5,0.5325,
0.565,0.5975,0.63,0.6625,0.695,0.7275,0.76,0.7925,0.825,0.8575,0.89,0.9225,
0.955,0.9875,1.02),.UNSPECIFIED.);
#369=B_SPLINE_SURFACE_WITH_KNOTS('',3,3,((#28780,#28781,#28782,#28783,#28784,
#28785,#28786,#28787,#28788,#28789,#28790,#28791,#28792,#28793,#28794,#28795,
#28796,#28797,#28798,#28799,#28800,#28801,#28802,#28803,#28804,#28805,#28806,
#28807,#28808,#28809,#28810,#28811,#28812,#28813,#28814),(#28815,#28816,
#28817,#28818,#28819,#28820,#28821,#28822,#28823,#28824,#28825,#28826,#28827,
#28828,#28829,#28830,#28831,#28832,#28833,#28834,#28835,#28836,#28837,#28838,
#28839,#28840,#28841,#28842,#28843,#28844,#28845,#28846,#28847,#28848,#28849),
(#28850,#28851,#28852,#28853,#28854,#28855,#28856,#28857,#28858,#28859,
#28860,#28861,#28862,#28863,#28864,#28865,#28866,#28867,#28868,#28869,#28870,
#28871,#28872,#28873,#28874,#28875,#28876,#28877,#28878,#28879,#28880,#28881,
#28882,#28883,#28884),(#28885,#28886,#28887,#28888,#28889,#28890,#28891,
#28892,#28893,#28894,#28895,#28896,#28897,#28898,#28899,#28900,#28901,#28902,
#28903,#28904,#28905,#28906,#28907,#28908,#28909,#28910,#28911,#28912,#28913,
#28914,#28915,#28916,#28917,#28918,#28919)),.UNSPECIFIED.,.F.,.F.,.F.,(4,
4),(4,1,1,1,1,1,1,1,1,1,1,1,1,1,1,1,1,1,1,1,1,1,1,1,1,1,1,1,1,1,1,1,4),
(-0.2772301033111,1.277230103311),(-0.02,0.0125,0.045,0.0775,0.11,0.1425,
0.175,0.2075,0.24,0.2725,0.305,0.3375,0.37,0.4025,0.435,0.4675,0.5,0.5325,
0.565,0.5975,0.63,0.6625,0.695,0.7275,0.76,0.7925,0.825,0.8575,0.89,0.9225,
0.955,0.9875,1.02),.UNSPECIFIED.);
#438=PLANE('',#9707);
#439=PLANE('',#9718);
#440=PLANE('',#9719);
#441=PLANE('',#9731);
#442=PLANE('',#9734);
#443=PLANE('',#9746);
#444=PLANE('',#9747);
#445=PLANE('',#9749);
#446=PLANE('',#9751);
#447=PLANE('',#9753);
#448=PLANE('',#9755);
#449=PLANE('',#9757);
#450=PLANE('',#9759);
#451=PLANE('',#9761);
#452=PLANE('',#9764);
#453=PLANE('',#9766);
#454=PLANE('',#9768);
#455=PLANE('',#9770);
#456=PLANE('',#9772);
#457=PLANE('',#9774);
#730=FACE_OUTER_BOUND('',#1278,.T.);
#731=FACE_OUTER_BOUND('',#1279,.T.);
#732=FACE_OUTER_BOUND('',#1280,.T.);
#733=FACE_OUTER_BOUND('',#1281,.T.);
#734=FACE_OUTER_BOUND('',#1282,.T.);
#735=FACE_OUTER_BOUND('',#1283,.T.);
#736=FACE_OUTER_BOUND('',#1284,.T.);
#737=FACE_OUTER_BOUND('',#1285,.T.);
#738=FACE_OUTER_BOUND('',#1286,.T.);
#739=FACE_OUTER_BOUND('',#1287,.T.);
#740=FACE_OUTER_BOUND('',#1288,.T.);
#741=FACE_OUTER_BOUND('',#1289,.T.);
#742=FACE_OUTER_BOUND('',#1290,.T.);
#743=FACE_OUTER_BOUND('',#1291,.T.);
#744=FACE_OUTER_BOUND('',#1292,.T.);
#745=FACE_OUTER_BOUND('',#1293,.T.);
#746=FACE_OUTER_BOUND('',#1294,.T.);
#747=FACE_OUTER_BOUND('',#1295,.T.);
#748=FACE_OUTER_BOUND('',#1296,.T.);
#749=FACE_OUTER_BOUND('',#1297,.T.);
#750=FACE_OUTER_BOUND('',#1299,.T.);
#751=FACE_OUTER_BOUND('',#1300,.T.);
#752=FACE_OUTER_BOUND('',#1301,.T.);
#753=FACE_OUTER_BOUND('',#1302,.T.);
#754=FACE_OUTER_BOUND('',#1303,.T.);
#755=FACE_OUTER_BOUND('',#1304,.T.);
#756=FACE_OUTER_BOUND('',#1305,.T.);
#757=FACE_OUTER_BOUND('',#1306,.T.);
#758=FACE_OUTER_BOUND('',#1307,.T.);
#759=FACE_OUTER_BOUND('',#1308,.T.);
#760=FACE_OUTER_BOUND('',#1309,.T.);
#761=FACE_OUTER_BOUND('',#1310,.T.);
#762=FACE_OUTER_BOUND('',#1311,.T.);
#763=FACE_OUTER_BOUND('',#1312,.T.);
#764=FACE_OUTER_BOUND('',#1313,.T.);
#765=FACE_OUTER_BOUND('',#1314,.T.);
#766=FACE_OUTER_BOUND('',#1315,.T.);
#767=FACE_OUTER_BOUND('',#1316,.T.);
#768=FACE_OUTER_BOUND('',#1317,.T.);
#769=FACE_OUTER_BOUND('',#1318,.T.);
#770=FACE_OUTER_BOUND('',#1319,.T.);
#771=FACE_OUTER_BOUND('',#1320,.T.);
#772=FACE_OUTER_BOUND('',#1321,.T.);
#773=FACE_OUTER_BOUND('',#1322,.T.);
#774=FACE_OUTER_BOUND('',#1323,.T.);
#775=FACE_OUTER_BOUND('',#1324,.T.);
#776=FACE_OUTER_BOUND('',#1325,.T.);
#777=FACE_OUTER_BOUND('',#1326,.T.);
#778=FACE_OUTER_BOUND('',#1327,.T.);
#779=FACE_OUTER_BOUND('',#1328,.T.);
#780=FACE_OUTER_BOUND('',#1329,.T.);
#1278=EDGE_LOOP('',(#6776,#6777,#6778));
#1279=EDGE_LOOP('',(#6779,#6780));
#1280=EDGE_LOOP('',(#6781,#6782,#6783,#6784,#6785));
#1281=EDGE_LOOP('',(#6786,#6787,#6788,#6789,#6790,#6791));
#1282=EDGE_LOOP('',(#6792,#6793,#6794,#6795,#6796,#6797));
#1283=EDGE_LOOP('',(#6798,#6799,#6800));
#1284=EDGE_LOOP('',(#6801,#6802,#6803,#6804,#6805,#6806));
#1285=EDGE_LOOP('',(#6807,#6808,#6809,#6810,#6811));
#1286=EDGE_LOOP('',(#6812,#6813,#6814,#6815));
#1287=EDGE_LOOP('',(#6816,#6817,#6818,#6819,#6820));
#1288=EDGE_LOOP('',(#6821,#6822,#6823,#6824,#6825));
#1289=EDGE_LOOP('',(#6826,#6827,#6828,#6829));
#1290=EDGE_LOOP('',(#6830,#6831,#6832,#6833,#6834));
#1291=EDGE_LOOP('',(#6835,#6836,#6837,#6838,#6839,#6840,#6841));
#1292=EDGE_LOOP('',(#6842,#6843,#6844,#6845,#6846,#6847,#6848,#6849,#6850));
#1293=EDGE_LOOP('',(#6851,#6852,#6853,#6854,#6855,#6856,#6857,#6858));
#1294=EDGE_LOOP('',(#6859,#6860,#6861,#6862,#6863));
#1295=EDGE_LOOP('',(#6864,#6865,#6866,#6867,#6868));
#1296=EDGE_LOOP('',(#6869,#6870,#6871,#6872));
#1297=EDGE_LOOP('',(#6873));
#1298=EDGE_LOOP('',(#6874));
#1299=EDGE_LOOP('',(#6875,#6876,#6877,#6878,#6879));
#1300=EDGE_LOOP('',(#6880,#6881,#6882,#6883,#6884,#6885,#6886,#6887,#6888,
#6889,#6890,#6891,#6892,#6893,#6894,#6895,#6896,#6897,#6898,#6899,#6900,
#6901,#6902,#6903,#6904,#6905,#6906,#6907,#6908));
#1301=EDGE_LOOP('',(#6909,#6910,#6911,#6912,#6913));
#1302=EDGE_LOOP('',(#6914,#6915,#6916,#6917));
#1303=EDGE_LOOP('',(#6918,#6919,#6920,#6921,#6922,#6923,#6924,#6925,#6926,
#6927,#6928,#6929,#6930,#6931,#6932,#6933,#6934,#6935,#6936,#6937,#6938,
#6939,#6940,#6941));
#1304=EDGE_LOOP('',(#6942,#6943,#6944,#6945,#6946));
#1305=EDGE_LOOP('',(#6947,#6948,#6949,#6950));
#1306=EDGE_LOOP('',(#6951,#6952,#6953,#6954));
#1307=EDGE_LOOP('',(#6955,#6956,#6957,#6958));
#1308=EDGE_LOOP('',(#6959,#6960,#6961,#6962));
#1309=EDGE_LOOP('',(#6963,#6964,#6965,#6966,#6967));
#1310=EDGE_LOOP('',(#6968,#6969,#6970,#6971));
#1311=EDGE_LOOP('',(#6972,#6973,#6974,#6975));
#1312=EDGE_LOOP('',(#6976,#6977,#6978,#6979));
#1313=EDGE_LOOP('',(#6980,#6981,#6982,#6983));
#1314=EDGE_LOOP('',(#6984,#6985,#6986,#6987));
#1315=EDGE_LOOP('',(#6988,#6989,#6990,#6991,#6992));
#1316=EDGE_LOOP('',(#6993,#6994,#6995,#6996));
#1317=EDGE_LOOP('',(#6997,#6998,#6999,#7000));
#1318=EDGE_LOOP('',(#7001,#7002,#7003,#7004,#7005));
#1319=EDGE_LOOP('',(#7006,#7007,#7008,#7009));
#1320=EDGE_LOOP('',(#7010,#7011,#7012,#7013,#7014));
#1321=EDGE_LOOP('',(#7015,#7016,#7017,#7018));
#1322=EDGE_LOOP('',(#7019,#7020,#7021,#7022));
#1323=EDGE_LOOP('',(#7023,#7024,#7025,#7026));
#1324=EDGE_LOOP('',(#7027,#7028,#7029,#7030,#7031));
#1325=EDGE_LOOP('',(#7032,#7033,#7034,#7035));
#1326=EDGE_LOOP('',(#7036,#7037,#7038,#7039,#7040));
#1327=EDGE_LOOP('',(#7041,#7042,#7043,#7044));
#1328=EDGE_LOOP('',(#7045,#7046,#7047,#7048,#7049));
#1329=EDGE_LOOP('',(#7050,#7051,#7052,#7053));
#1874=CIRCLE('',#9706,1.331411920116);
#1875=CIRCLE('',#9708,1.116987298108);
#1876=CIRCLE('',#9710,1.116987298108);
#1877=CIRCLE('',#9713,0.4);
#1878=CIRCLE('',#9714,1.331411920116);
#1879=CIRCLE('',#9715,0.4);
#1880=CIRCLE('',#9716,1.707288968431);
#1881=CIRCLE('',#9720,3.);
#1882=CIRCLE('',#9722,3.);
#1883=CIRCLE('',#9723,3.);
#1884=CIRCLE('',#9724,1.092121597166);
#1885=CIRCLE('',#9727,1.092121597166);
#1886=CIRCLE('',#9728,1.092121597166);
#1887=CIRCLE('',#9730,1.092121597166);
#2213=B_SPLINE_CURVE_WITH_KNOTS('',3,(#25159,#25160,#25161,#25162,#25163,
#25164,#25165,#25166,#25167,#25168,#25169,#25170,#25171,#25172,#25173,#25174),
 .UNSPECIFIED.,.F.,.F.,(4,2,2,2,2,2,2,4),(-0.997882818540195,-0.95890297017825,
-0.915601512736776,-0.890692190934456,-0.842383484706287,-0.788483554860223,
-0.738305310250689,-0.724835095226849),.UNSPECIFIED.);
#2214=B_SPLINE_CURVE_WITH_KNOTS('',3,(#25180,#25181,#25182,#25183,#25184,
#25185,#25186,#25187,#25188,#25189,#25190,#25191,#25192,#25193,#25194,#25195,
#25196,#25197,#25198),.UNSPECIFIED.,.F.,.F.,(4,3,3,3,3,3,4),(2.30639007129119E-6,
0.168219155399412,0.242220953770006,0.434178569252148,0.633536045455965,
0.816764967682345,0.999993889908724),.UNSPECIFIED.);
#2215=B_SPLINE_CURVE_WITH_KNOTS('',3,(#25205,#25206,#25207,#25208),
 .UNSPECIFIED.,.F.,.F.,(4,4),(-0.00458558691821468,0.),.UNSPECIFIED.);
#2216=B_SPLINE_CURVE_WITH_KNOTS('',3,(#25209,#25210,#25211,#25212,#25213,
#25214,#25215,#25216,#25217,#25218,#25219,#25220,#25221),.UNSPECIFIED.,
 .F.,.F.,(4,3,3,3,4),(0.,0.3333333333333,0.569543342469847,0.6666666666667,
0.99998534170567),.UNSPECIFIED.);
#2217=B_SPLINE_CURVE_WITH_KNOTS('',3,(#25363,#25364,#25365,#25366,#25367,
#25368,#25369,#25370,#25371,#25372,#25373,#25374,#25375,#25376,#25377,#25378,
#25379,#25380,#25381,#25382,#25383,#25384,#25385,#25386,#25387,#25388,#25389,
#25390,#25391,#25392,#25393,#25394,#25395,#25396,#25397,#25398,#25399,#25400,
#25401,#25402,#25403,#25404,#25405,#25406,#25407,#25408,#25409,#25410,#25411,
#25412,#25413,#25414,#25415,#25416,#25417,#25418,#25419,#25420,#25421,#25422,
#25423,#25424,#25425,#25426,#25427,#25428,#25429,#25430,#25431,#25432,#25433,
#25434,#25435,#25436,#25437,#25438,#25439,#25440,#25441,#25442,#25443,#25444,
#25445,#25446,#25447,#25448,#25449,#25450,#25451,#25452,#25453,#25454,#25455,
#25456,#25457,#25458,#25459,#25460,#25461,#25462,#25463,#25464,#25465,#25466,
#25467,#25468,#25469,#25470,#25471,#25472,#25473,#25474,#25475,#25476,#25477,
#25478,#25479,#25480,#25481,#25482,#25483,#25484,#25485,#25486,#25487,#25488,
#25489,#25490,#25491,#25492,#25493,#25494,#25495,#25496,#25497,#25498,#25499,
#25500,#25501,#25502,#25503,#25504,#25505,#25506,#25507,#25508,#25509,#25510,
#25511,#25512,#25513,#25514,#25515,#25516,#25517,#25518,#25519,#25520,#25521,
#25522,#25523,#25524,#25525,#25526,#25527,#25528,#25529,#25530,#25531,#25532,
#25533,#25534,#25535,#25536,#25537,#25538,#25539,#25540,#25541,#25542,#25543,
#25544,#25545,#25546,#25547,#25548,#25549,#25550,#25551,#25552,#25553,#25554,
#25555,#25556,#25557,#25558,#25559,#25560,#25561,#25562,#25563,#25564,#25565,
#25566,#25567,#25568,#25569,#25570,#25571,#25572,#25573,#25574,#25575,#25576,
#25577,#25578,#25579,#25580,#25581,#25582,#25583,#25584,#25585,#25586,#25587,
#25588,#25589,#25590,#25591,#25592,#25593,#25594,#25595,#25596,#25597,#25598,
#25599,#25600,#25601,#25602,#25603,#25604,#25605,#25606,#25607,#25608,#25609,
#25610,#25611,#25612,#25613,#25614,#25615,#25616,#25617,#25618,#25619,#25620,
#25621,#25622,#25623,#25624,#25625,#25626,#25627,#25628,#25629,#25630,#25631,
#25632,#25633,#25634,#25635,#25636,#25637,#25638,#25639,#25640,#25641,#25642,
#25643,#25644,#25645,#25646,#25647,#25648,#25649,#25650,#25651,#25652,#25653,
#25654,#25655,#25656,#25657,#25658,#25659,#25660,#25661,#25662,#25663,#25664,
#25665,#25666,#25667,#25668,#25669,#25670,#25671,#25672,#25673,#25674,#25675,
#25676,#25677,#25678,#25679,#25680,#25681,#25682,#25683,#25684,#25685,#25686,
#25687,#25688,#25689,#25690,#25691,#25692,#25693,#25694,#25695,#25696,#25697,
#25698,#25699,#25700,#25701,#25702,#25703,#25704,#25705,#25706,#25707,#25708,
#25709,#25710,#25711,#25712,#25713,#25714,#25715,#25716,#25717,#25718,#25719,
#25720,#25721,#25722,#25723,#25724,#25725,#25726,#25727,#25728,#25729,#25730,
#25731,#25732,#25733,#25734,#25735,#25736,#25737,#25738,#25739,#25740,#25741,
#25742,#25743,#25744,#25745,#25746,#25747,#25748,#25749,#25750,#25751,#25752,
#25753,#25754,#25755,#25756,#25757,#25758,#25759,#25760),.UNSPECIFIED.,
 .F.,.F.,(4,2,2,2,2,2,2,2,2,2,2,2,2,2,2,2,2,2,2,2,2,2,2,2,2,2,2,2,2,2,2,
2,2,2,2,2,2,2,2,2,2,2,2,2,2,2,2,2,2,2,2,2,2,2,2,2,2,2,2,2,2,2,2,2,2,2,2,
2,2,2,2,2,2,2,2,2,2,2,2,2,2,2,2,2,2,2,2,2,2,2,2,2,2,2,2,2,2,2,2,2,2,2,2,
2,2,2,2,2,2,2,2,2,2,2,2,2,2,2,2,2,2,2,2,2,2,2,2,2,2,2,2,2,2,2,2,2,2,2,2,
2,2,2,2,2,2,2,2,2,2,2,2,2,2,2,2,2,2,2,2,2,2,2,2,2,2,2,2,2,2,2,2,2,2,2,2,
2,2,2,2,2,2,2,2,2,2,2,2,2,2,2,2,2,2,2,2,2,2,2,4),(-2.36492523745759,-2.34255296682852,
-2.3199656508682,-2.27585417903727,-2.25354275255567,-2.21054282254419,
-2.18644688059544,-2.17004409694976,-2.13488673135029,-2.11668240985326,
-2.10027976460783,-2.08774450478953,-2.05477340268109,-2.03507134009305,
-2.01951470315281,-2.00996653487751,-1.99755255991591,-1.97234100153057,
-1.95774451386731,-1.9481161572119,-1.93420090833259,-1.92534809472293,
-1.89682963918897,-1.88594722890426,-1.87680322226878,-1.86124282768097,
-1.85436376885839,-1.84672198839416,-1.83490432477196,-1.81557320818878,
-1.80683548582628,-1.79915234399613,-1.79070246008438,-1.77651955263018,
-1.76981925147615,-1.76127412212674,-1.7392331290447,-1.72754921515706,
-1.72102908066663,-1.71232177348829,-1.69956321522094,-1.69317593387435,
-1.68647055161581,-1.66712747464848,-1.65622744096082,-1.64814547719462,
-1.64243757267111,-1.62899360781887,-1.61728109210313,-1.61175268037231,
-1.60417666831167,-1.58353889221248,-1.57580174480183,-1.56938458299859,
-1.56423392904341,-1.54116632969256,-1.53581047383477,-1.53012761438281,
-1.51835316704718,-1.50377957088101,-1.49486795150478,-1.48978962379479,
-1.48382162476493,-1.46785015792272,-1.46210900183348,-1.45710386272981,
-1.45172301747603,-1.42952426827573,-1.42161170300879,-1.41537759326571,
-1.41082162980847,-1.40247391369265,-1.38876003207578,-1.38323377596955,
-1.37845252841154,-1.37334193458513,-1.3626827351202,-1.3483496471966,-1.34212107811774,
-1.33685971551491,-1.33230430814372,-1.3216514476077,-1.30967694883718,
-1.30435959610382,-1.29975527169422,-1.29481794690037,-1.2842053260138,
-1.27046886466486,-1.26230124198716,-1.25791300532331,-1.25246407651647,
-1.24245049601483,-1.23109500981515,-1.22581569534866,-1.22127092577752,
-1.21649755031245,-1.20597673592743,-1.19276104990642,-1.18699793818544,
-1.18214792478359,-1.17754136916297,-1.16646900262159,-1.14704014866058,
-1.14261167216771,-1.1377750265953,-1.13209365258579,-1.11948644571785,
-1.10919367696915,-1.10462395084307,-1.09968366141108,-1.08517547188672,
-1.06997765473393,-1.06510120098665,-1.0606500005824,-1.04935850990902,
-1.03150359941975,-1.02700605695584,-1.02160217029774,-1.01522712964587,
-1.00046230866128,-0.990911070885307,-0.986158745480183,-0.98139507987467,
-0.975719480081178,-0.962083468164042,-0.953955001953389,-0.949319869462239,
-0.94342315872656,-0.92738731581423,-0.91368226802068,-0.908353529354358,
-0.903742287718806,-0.898596623649472,-0.887515002696023,-0.877130058730485,
-0.872195218684388,-0.866145181709486,-0.851040400037946,-0.835407299386497,
-0.829790394065256,-0.824959791337494,-0.813731759798563,-0.799566971887483,
-0.794271584240714,-0.787490397253317,-0.779183255750064,-0.760336475939653,
-0.753074670747068,-0.748025261177741,-0.739172294288363,-0.724810587804851,
-0.718786017632848,-0.712382003253458,-0.694981768167063,-0.678671288174418,
-0.672343519043225,-0.666675285513522,-0.651141806748008,-0.643185979594139,
-0.636589194049217,-0.625072717792037,-0.60409709119821,-0.595806831686027,
-0.58981951476737,-0.5843561154383,-0.569891543895224,-0.562747028476868,
-0.553956616726265,-0.542955873544897,-0.520207904882434,-0.51313018313803,
-0.501814099198623,-0.489317266067134,-0.480801531073975,-0.461865586957671,
-0.441772150354699,-0.433644352633433,-0.423367939937679,-0.411008574535974,
-0.400547184327938,-0.388296277949455,-0.359851495711931,-0.35084867425318,
-0.342376920864329,-0.330234453560913,-0.314445598905012,-0.289223046175026,
-0.275676731870157,-0.265710680204558,-0.249661255292412,-0.223368235202192,
-0.198086384719217,-0.184067733214858,-0.159711123721348,-0.115000186891252,
-0.0973065370727581,-0.0573775607030809,-0.0287912440975278,-7.10237341792967E-5),
 .UNSPECIFIED.);
#2218=B_SPLINE_CURVE_WITH_KNOTS('',3,(#25763,#25764,#25765,#25766,#25767,
#25768,#25769,#25770,#25771,#25772,#25773,#25774,#25775,#25776,#25777,#25778,
#25779,#25780,#25781,#25782,#25783,#25784,#25785,#25786,#25787,#25788,#25789,
#25790,#25791,#25792,#25793,#25794,#25795,#25796,#25797,#25798,#25799,#25800,
#25801,#25802,#25803,#25804,#25805,#25806,#25807,#25808,#25809,#25810,#25811,
#25812,#25813,#25814,#25815,#25816,#25817,#25818,#25819,#25820,#25821,#25822,
#25823,#25824,#25825,#25826,#25827,#25828,#25829,#25830,#25831,#25832,#25833,
#25834,#25835,#25836,#25837,#25838,#25839,#25840,#25841,#25842,#25843,#25844,
#25845,#25846,#25847,#25848,#25849,#25850,#25851,#25852,#25853,#25854,#25855,
#25856,#25857,#25858,#25859,#25860,#25861,#25862,#25863,#25864,#25865,#25866,
#25867,#25868,#25869,#25870,#25871,#25872,#25873,#25874,#25875,#25876,#25877,
#25878,#25879,#25880),.UNSPECIFIED.,.F.,.F.,(4,2,2,2,2,2,2,2,2,2,2,2,2,
2,2,2,2,2,2,2,2,2,2,2,2,2,2,2,2,2,2,2,2,2,2,2,2,2,2,2,2,2,2,2,2,2,2,2,2,
2,2,2,2,2,2,2,2,2,4),(3.16667141335679E-5,0.0284893424911215,0.0571031677616148,
0.100536752903684,0.152083753002382,0.211276158594342,0.292188579082734,
0.399230061028865,0.503318852891491,0.587315507677329,0.66191283307897,
0.716273687751307,0.75975594936003,0.814048448551261,0.886012735934177,
0.971046167155236,1.06848597901879,1.19863510422438,1.37984377711638,1.57239515517755,
1.72626212591233,1.86298572050433,1.96198100642033,2.04139080933292,2.1368540562863,
2.25441211833114,2.39263076571147,2.55067957440204,2.74511452244579,2.97317398670225,
3.2012334509587,3.39566839900244,3.553717207693,3.69193585507333,3.80949391711816,
3.90495716407152,3.98436696698408,4.08336225290006,4.22008584749205,4.37395281822682,
4.56650419628796,4.74771286917995,4.87786199438553,4.97530180624906,5.0603352374701,
5.132299524853,5.18659202404421,5.23007428565291,5.28443514032522,5.35903246572685,
5.44302912051267,5.54711791237526,5.65415939432137,5.73507181480991,5.79426422040202,
5.84581122050084,5.88924480564302,5.91787547025432,5.9463098192052),
 .UNSPECIFIED.);
#2219=B_SPLINE_CURVE_WITH_KNOTS('',3,(#26026,#26027,#26028,#26029,#26030,
#26031,#26032,#26033,#26034,#26035,#26036,#26037,#26038,#26039,#26040,#26041,
#26042,#26043,#26044,#26045,#26046,#26047,#26048,#26049,#26050,#26051,#26052,
#26053,#26054,#26055,#26056,#26057,#26058,#26059,#26060,#26061,#26062,#26063,
#26064,#26065,#26066,#26067),.UNSPECIFIED.,.F.,.F.,(4,2,2,2,2,2,2,2,2,2,
2,2,2,2,2,2,2,2,2,2,4),(9.56954942354073E-5,0.0404351915602284,0.0809863227547807,
0.138729359916234,0.168045397626004,0.227812484620681,0.28784359795065,
0.346677928601178,0.375266441944433,0.434868223533285,0.464254085500563,
0.4930185317878,0.551407924605979,0.611332955424245,0.67040124768131,0.729413323150459,
0.788742910316018,0.817389104247561,0.87571192621649,0.91217639806824,0.948381630678781),
 .UNSPECIFIED.);
#2220=B_SPLINE_CURVE_WITH_KNOTS('',3,(#26069,#26070,#26071,#26072,#26073,
#26074,#26075,#26076,#26077,#26078,#26079,#26080,#26081,#26082,#26083,#26084,
#26085,#26086,#26087,#26088,#26089,#26090,#26091,#26092,#26093,#26094,#26095,
#26096,#26097,#26098,#26099,#26100,#26101,#26102,#26103,#26104,#26105,#26106,
#26107,#26108,#26109,#26110,#26111,#26112,#26113,#26114,#26115,#26116,#26117,
#26118,#26119,#26120,#26121,#26122,#26123,#26124,#26125,#26126,#26127,#26128,
#26129,#26130,#26131,#26132,#26133,#26134,#26135,#26136,#26137,#26138,#26139,
#26140,#26141,#26142,#26143,#26144,#26145,#26146,#26147,#26148,#26149,#26150,
#26151,#26152,#26153,#26154,#26155,#26156,#26157,#26158,#26159,#26160,#26161,
#26162,#26163,#26164,#26165,#26166,#26167,#26168,#26169,#26170),
 .UNSPECIFIED.,.F.,.F.,(4,2,2,2,2,2,2,2,2,2,2,2,2,2,2,2,2,2,2,2,2,2,2,2,
2,2,2,2,2,2,2,2,2,2,2,2,2,2,2,2,2,2,2,2,2,2,2,2,2,2,4),(-7.78033786116235,
-7.63085234138336,-7.49045462844376,-7.20406581382073,-6.99070882568832,
-6.77843585057195,-6.60078812217249,-6.41801603037867,-6.25219399969925,
-5.88201230226676,-5.68258509740488,-5.46562698484506,-5.09957693944957,
-4.89523762533434,-4.61995314186142,-4.25199639905186,-3.99742607058464,
-3.76323524666776,-3.42400292432898,-3.16991835794728,-2.92737133189385,
-2.63147231877444,-2.3304031238569,-1.91401229014332,-1.67248413718354,
-1.47051455546473,-1.31855523977063,-1.16408569562622,-1.10125811890718,
-1.01972820676982,-0.927975008243967,-0.813026949460111,-0.714310817432307,
-0.680192283916462,-0.640249373549641,-0.578742392923274,-0.539156183889252,
-0.507633333247703,-0.467186258890576,-0.428733937720528,-0.394809054534059,
-0.363669767787403,-0.33739791138586,-0.278612503104019,-0.24018447220225,
-0.20459026029123,-0.160285767953291,-0.0967339395859139,-0.07327066611358,
-0.0366392212630044,-1.00000000013978E-6),.UNSPECIFIED.);
#2221=B_SPLINE_CURVE_WITH_KNOTS('',3,(#26171,#26172,#26173,#26174,#26175,
#26176,#26177,#26178,#26179,#26180,#26181,#26182,#26183,#26184,#26185,#26186,
#26187,#26188,#26189,#26190,#26191,#26192,#26193,#26194,#26195,#26196,#26197,
#26198),.UNSPECIFIED.,.F.,.F.,(4,2,2,2,2,2,2,2,2,2,2,2,2,4),(6.03863816781982E-5,
0.0235321054586779,0.0469894124433013,0.0625955451438476,0.120830736051024,
0.148200482152788,0.177426809763754,0.234689944472845,0.262841817837877,
0.31782697095527,0.362416306428818,0.390301942764782,0.40453484142027,0.418742436141258),
 .UNSPECIFIED.);
#2222=B_SPLINE_CURVE_WITH_KNOTS('',3,(#26200,#26201,#26202,#26203,#26204,
#26205,#26206,#26207,#26208,#26209,#26210,#26211,#26212,#26213,#26214,#26215,
#26216,#26217,#26218,#26219,#26220,#26221,#26222,#26223,#26224,#26225,#26226,
#26227,#26228,#26229,#26230,#26231,#26232,#26233,#26234,#26235),
 .UNSPECIFIED.,.F.,.F.,(4,2,2,2,2,2,2,2,2,2,2,2,2,2,2,2,2,4),(-1.03451909507685,
-0.985628237457854,-0.936696563950415,-0.861017278353068,-0.772400298280665,
-0.674466741047526,-0.58240655627606,-0.502283935464647,-0.434648703401253,
-0.399451972244463,-0.330651356045544,-0.267309498328652,-0.211812516712395,
-0.183464606668581,-0.124444898378072,-0.0613612600492961,-0.0312461969758679,
-7.37969285442371E-5),.UNSPECIFIED.);
#2223=B_SPLINE_CURVE_WITH_KNOTS('',3,(#26518,#26519,#26520,#26521,#26522,
#26523,#26524,#26525,#26526,#26527,#26528,#26529,#26530,#26531,#26532,#26533,
#26534,#26535,#26536,#26537,#26538,#26539,#26540,#26541,#26542,#26543,#26544,
#26545,#26546,#26547,#26548,#26549,#26550,#26551,#26552,#26553,#26554,#26555,
#26556,#26557,#26558,#26559,#26560,#26561,#26562,#26563,#26564,#26565,#26566,
#26567,#26568,#26569,#26570,#26571,#26572,#26573,#26574,#26575,#26576,#26577,
#26578,#26579,#26580,#26581,#26582,#26583,#26584,#26585,#26586,#26587,#26588,
#26589,#26590,#26591,#26592,#26593,#26594,#26595,#26596,#26597,#26598,#26599,
#26600,#26601,#26602,#26603,#26604,#26605,#26606,#26607,#26608,#26609,#26610,
#26611,#26612,#26613,#26614,#26615,#26616,#26617,#26618,#26619,#26620,#26621,
#26622,#26623,#26624,#26625,#26626,#26627,#26628,#26629,#26630,#26631,#26632,
#26633,#26634,#26635,#26636,#26637,#26638,#26639,#26640,#26641,#26642,#26643,
#26644,#26645,#26646,#26647),.UNSPECIFIED.,.F.,.F.,(4,2,2,2,2,2,2,2,2,2,
2,2,2,2,2,2,2,2,2,2,2,2,2,2,2,2,2,2,2,2,2,2,2,2,2,2,2,2,2,2,2,2,2,2,2,2,
2,2,2,2,2,2,2,2,2,2,2,2,2,2,2,2,2,2,4),(4.96401988677343E-5,0.0286909851214567,
0.0556526802951698,0.113832141356971,0.161351607238736,0.218507559614986,
0.258398640746192,0.306095729471452,0.362010325096549,0.401932827379239,
0.449679229549262,0.506640699165884,0.546568564241865,0.594128809564416,
0.649775741136893,0.689741624015701,0.737661250020149,0.79515538238638,
0.835112826235051,0.882602298743163,0.937613137963498,0.977626467674421,
1.02576982630798,1.08415873336359,1.12414091063929,1.17148371887183,1.22517859760727,
1.26524992889356,1.31382300234001,1.37387784361501,1.41387374553324,1.46091668317935,
1.50925514688824,1.58269800618146,1.65896058403542,1.71319604759754,1.75314524331709,
1.79263146105731,1.83759108160969,1.90438845857931,1.96972763829277,2.01044088449258,
2.06296596817368,2.10925651439416,2.14980073822217,2.2105683732106,2.25789865056263,
2.29847153891689,2.35552271586138,2.40210594727478,2.44260893906244,2.50196302289595,
2.54893131404076,2.5894265700774,2.64731488333339,2.69394136940077,2.73438961727687,
2.79305667135409,2.83992515335308,2.88034576054228,2.93909733066414,2.98576859062926,
3.04660814582191,3.07498707993905,3.10514224167434),.UNSPECIFIED.);
#2224=B_SPLINE_CURVE_WITH_KNOTS('',3,(#26650,#26651,#26652,#26653,#26654,
#26655,#26656,#26657,#26658,#26659,#26660,#26661,#26662,#26663,#26664,#26665,
#26666,#26667,#26668,#26669,#26670,#26671,#26672,#26673,#26674,#26675,#26676,
#26677,#26678,#26679,#26680,#26681,#26682,#26683,#26684,#26685,#26686,#26687,
#26688,#26689,#26690,#26691,#26692,#26693,#26694,#26695,#26696,#26697,#26698,
#26699,#26700,#26701,#26702,#26703,#26704,#26705,#26706,#26707,#26708,#26709,
#26710,#26711,#26712,#26713,#26714,#26715,#26716,#26717,#26718,#26719,#26720,
#26721,#26722,#26723,#26724,#26725,#26726,#26727,#26728,#26729,#26730,#26731,
#26732,#26733,#26734,#26735,#26736,#26737,#26738,#26739,#26740,#26741,#26742,
#26743,#26744,#26745,#26746,#26747,#26748,#26749,#26750,#26751,#26752,#26753,
#26754,#26755,#26756,#26757,#26758,#26759,#26760,#26761,#26762,#26763,#26764,
#26765,#26766,#26767),.UNSPECIFIED.,.F.,.F.,(4,2,2,2,2,2,2,2,2,2,2,2,2,
2,2,2,2,2,2,2,2,2,2,2,2,2,2,2,2,2,2,2,2,2,2,2,2,2,2,2,2,2,2,2,2,2,2,2,2,
2,2,2,2,2,2,2,2,2,4),(-5.94661143749944,-5.91817587231828,-5.88954389637305,
-5.84610834802751,-5.79455901799797,-5.73536393690187,-5.65444785916197,
-5.54740153892753,-5.44330804223854,-5.35930759079344,-5.2847068935834,
-5.23034358179366,-5.18685935478129,-5.13256440156231,-5.06059686138459,
-4.97555958664179,-4.87811537048653,-4.74796036252415,-4.56674349897742,
-4.37418341756985,-4.2203094920287,-4.08357971751308,-3.98457995699775,
-3.90516656475212,-3.80969900284799,-3.69213562716397,-3.55391073228339,
-3.3958547797668,-3.20141104323893,-2.97334127066598,-2.74527149809304,
-2.55082776156515,-2.39277180904853,-2.25454691416793,-2.13698353848388,
-2.04151597657974,-1.9621025843341,-1.86310282381876,-1.7263730493031,-1.57249912376192,
-1.37993904235428,-1.19872217880751,-1.06856717084512,-0.971122954689846,
-0.886085679947027,-0.814118139769293,-0.759823186550277,-0.716338959537862,
-0.661975647748049,-0.587374950537876,-0.50337449909263,-0.399281002403463,
-0.29223468216884,-0.211318604428868,-0.152123523332738,-0.100574193303159,
-0.0571386449575849,-0.0285066862366441,-7.10380286812318E-5),
 .UNSPECIFIED.);
#2225=B_SPLINE_CURVE_WITH_KNOTS('',3,(#26910,#26911,#26912,#26913,#26914,
#26915,#26916,#26917,#26918,#26919,#26920,#26921,#26922,#26923,#26924,#26925,
#26926,#26927,#26928,#26929,#26930,#26931,#26932,#26933,#26934,#26935,#26936,
#26937,#26938,#26939,#26940,#26941,#26942,#26943,#26944,#26945,#26946,#26947,
#26948,#26949,#26950,#26951,#26952,#26953,#26954,#26955,#26956,#26957,#26958,
#26959,#26960,#26961,#26962,#26963,#26964,#26965,#26966,#26967,#26968,#26969,
#26970,#26971,#26972,#26973,#26974,#26975,#26976,#26977,#26978,#26979,#26980,
#26981,#26982,#26983,#26984,#26985,#26986,#26987,#26988,#26989,#26990,#26991,
#26992,#26993,#26994,#26995,#26996,#26997,#26998,#26999,#27000,#27001,#27002,
#27003,#27004,#27005,#27006,#27007,#27008,#27009,#27010,#27011,#27012,#27013,
#27014,#27015,#27016,#27017,#27018,#27019,#27020,#27021,#27022,#27023,#27024,
#27025,#27026,#27027),.UNSPECIFIED.,.F.,.F.,(4,2,2,2,2,2,2,2,2,2,2,2,2,
2,2,2,2,2,2,2,2,2,2,2,2,2,2,2,2,2,2,2,2,2,2,2,2,2,2,2,2,2,2,2,2,2,2,2,2,
2,2,2,2,2,2,2,2,2,4),(7.10380286801851E-5,0.0285066862366488,0.0571386449575934,
0.100574193303156,0.15212352333273,0.211318604428867,0.292234682168843,
0.399281002403465,0.503374499092633,0.587374950537879,0.661975647748052,
0.716338959537883,0.759823186550319,0.814118139769361,0.886085679947134,
0.971122954689997,1.06856717084532,1.19872217880778,1.37993904235465,1.5724991237624,
1.72637304930366,1.86310282381939,1.9621025843348,2.0415159765805,2.1369835384847,
2.25454691416883,2.39277180904952,2.55082776156624,2.74527149809426,2.97334127066737,
3.20141104324048,3.3958547797685,3.55391073228522,3.69213562716592,3.80969900285004,
3.90516656475422,3.98457995699989,4.08357971751527,4.22030949203095,4.37418341757216,
4.56674349897983,4.74796036252663,4.87811537048906,4.97555958664437,5.06059686138721,
5.13256440156495,5.18685935478398,5.2303435817964,5.28470689358622,5.35930759079635,
5.44330804224156,5.54740153893068,5.65444785916525,5.73536393690522,5.79455901800137,
5.84610834803096,5.88954389637653,5.9181758550974,5.94661148928436),
 .UNSPECIFIED.);
#2226=B_SPLINE_CURVE_WITH_KNOTS('',3,(#27170,#27171,#27172,#27173,#27174,
#27175,#27176,#27177,#27178,#27179,#27180,#27181,#27182,#27183,#27184,#27185,
#27186,#27187,#27188,#27189,#27190,#27191,#27192,#27193,#27194,#27195,#27196,
#27197,#27198,#27199,#27200,#27201,#27202,#27203,#27204,#27205,#27206,#27207,
#27208,#27209,#27210,#27211),.UNSPECIFIED.,.F.,.F.,(4,2,2,2,2,2,2,2,2,2,
2,2,2,2,2,2,2,2,2,2,4),(9.56954942354455E-5,0.0404351999983261,0.0809863391999001,
0.138729373521468,0.168045411658336,0.227812497843943,0.287843613795308,
0.346677944888803,0.375266460404388,0.434868243739065,0.464254106674541,
0.49301855332279,0.551407950994098,0.611332985371951,0.670401283775956,
0.729413371370902,0.788742981688662,0.817389185685092,0.875712032112295,
0.912199298092506,0.948381011938093),.UNSPECIFIED.);
#2227=B_SPLINE_CURVE_WITH_KNOTS('',3,(#27353,#27354,#27355,#27356,#27357,
#27358,#27359,#27360,#27361,#27362,#27363,#27364,#27365,#27366,#27367,#27368,
#27369,#27370,#27371,#27372,#27373,#27374,#27375,#27376,#27377,#27378,#27379,
#27380,#27381,#27382,#27383,#27384,#27385,#27386,#27387,#27388,#27389,#27390,
#27391,#27392,#27393,#27394,#27395,#27396,#27397,#27398,#27399,#27400,#27401,
#27402,#27403,#27404,#27405,#27406,#27407,#27408,#27409,#27410,#27411,#27412,
#27413,#27414,#27415,#27416,#27417,#27418,#27419,#27420,#27421,#27422,#27423,
#27424,#27425,#27426,#27427,#27428,#27429,#27430,#27431,#27432,#27433,#27434,
#27435,#27436,#27437,#27438,#27439,#27440,#27441,#27442,#27443,#27444,#27445,
#27446,#27447,#27448,#27449,#27450,#27451,#27452,#27453,#27454,#27455,#27456,
#27457,#27458,#27459,#27460,#27461,#27462,#27463,#27464,#27465,#27466,#27467,
#27468,#27469,#27470,#27471,#27472,#27473,#27474,#27475,#27476,#27477,#27478,
#27479,#27480,#27481,#27482),.UNSPECIFIED.,.F.,.F.,(4,2,2,2,2,2,2,2,2,2,
2,2,2,2,2,2,2,2,2,2,2,2,2,2,2,2,2,2,2,2,2,2,2,2,2,2,2,2,2,2,2,2,2,2,2,2,
2,2,2,2,2,2,2,2,2,2,2,2,2,2,2,2,2,2,4),(4.96401988677452E-5,0.0286909851214136,
0.0556526802950926,0.113832141356949,0.161351607239005,0.218507559615801,
0.258398640747191,0.306095729472568,0.362010325097728,0.40193282738061,
0.449679229551041,0.506640699167879,0.546568564244047,0.594128809566736,
0.64977574113961,0.6897416240186,0.737661250023257,0.795155382389599,0.835112826238453,
0.882602298746813,0.937613137967583,0.977626467678681,1.02576982631241,
1.08415873336806,1.12414091064394,1.17148371887674,1.22517859761275,1.26524992889922,
1.31382300234579,1.3738778436207,1.41387374553911,1.46091668318551,1.509255146879,
1.582698006183,1.65896058405076,1.71319604762296,1.75314524334271,1.79263146107175,
1.83759108162834,1.904388458596,1.96972763830814,2.01044088450079,2.06296596815001,
2.10925651435982,2.14980073818021,2.2105683731605,2.25789865050626,2.29847153885315,
2.35552271578088,2.40210594718442,2.44260893896451,2.50196302279135,2.54893131392834,
2.58942656995753,2.64731488319995,2.69394136925823,2.73438961712682,2.79305667119477,
2.83992515318539,2.88034576036712,2.93909733047707,2.98576859043333,3.04660814561508,
3.07498707972723,3.10514224145725),.UNSPECIFIED.);
#2228=B_SPLINE_CURVE_WITH_KNOTS('',3,(#27485,#27486,#27487,#27488,#27489,
#27490,#27491,#27492,#27493,#27494,#27495,#27496,#27497,#27498,#27499,#27500,
#27501,#27502,#27503,#27504,#27505,#27506,#27507,#27508,#27509,#27510,#27511,
#27512,#27513,#27514,#27515,#27516,#27517,#27518,#27519,#27520,#27521,#27522,
#27523,#27524,#27525,#27526,#27527,#27528,#27529,#27530,#27531,#27532,#27533,
#27534,#27535,#27536,#27537,#27538,#27539,#27540,#27541,#27542,#27543,#27544,
#27545,#27546,#27547,#27548,#27549,#27550,#27551,#27552,#27553,#27554,#27555,
#27556,#27557,#27558,#27559,#27560,#27561,#27562,#27563,#27564,#27565,#27566,
#27567,#27568,#27569,#27570,#27571,#27572,#27573,#27574,#27575,#27576,#27577,
#27578,#27579,#27580,#27581,#27582,#27583,#27584,#27585,#27586,#27587,#27588,
#27589,#27590,#27591,#27592,#27593,#27594,#27595,#27596,#27597,#27598,#27599,
#27600,#27601,#27602),.UNSPECIFIED.,.F.,.F.,(4,2,2,2,2,2,2,2,2,2,2,2,2,
2,2,2,2,2,2,2,2,2,2,2,2,2,2,2,2,2,2,2,2,2,2,2,2,2,2,2,2,2,2,2,2,2,2,2,2,
2,2,2,2,2,2,2,2,2,4),(-5.9466114892713,-5.91817585508441,-5.88954389636361,
-5.84610834801816,-5.79455901798872,-5.73536393689273,-5.65444785915298,
-5.54740153891873,-5.44330804222993,-5.35930759078498,-5.28470689357507,
-5.23034358178543,-5.18685935477315,-5.13256440155427,-5.06059686137668,
-4.97555958663403,-4.87811537047895,-4.74796036251681,-4.56674349897041,
-4.37418341756319,-4.22030949202233,-4.08357971750696,-3.9845799569918,
-3.90516656474632,-3.80969900284236,-3.69213562715855,-3.55391073227822,
-3.39585477976192,-3.20141104323441,-2.97334127066188,-2.74527149808934,
-2.5508277615618,-2.39277180904547,-2.25454691416512,-2.13698353848128,
-2.04151597657729,-1.96210258433177,-1.86310282381656,-1.72637304930109,
-1.57249912376012,-1.37993904235275,-1.19872217880622,-1.06856717084401,
-0.971122954688863,-0.886085679946156,-0.814118139768516,-0.759823186549577,
-0.716338959537225,-0.661975647747492,-0.587374950537428,-0.503374499092306,
-0.399281002403298,-0.292234682168818,-0.211318604428862,-0.152123523332728,
-0.100574193303159,-0.0571386449575935,-0.0285066862366491,-7.10380286809763E-5),
 .UNSPECIFIED.);
#2229=B_SPLINE_CURVE_WITH_KNOTS('',3,(#27745,#27746,#27747,#27748,#27749,
#27750,#27751,#27752,#27753,#27754,#27755,#27756,#27757,#27758,#27759,#27760,
#27761,#27762,#27763,#27764,#27765,#27766,#27767,#27768,#27769,#27770,#27771,
#27772,#27773,#27774,#27775,#27776,#27777,#27778,#27779,#27780,#27781,#27782,
#27783,#27784,#27785,#27786,#27787,#27788,#27789,#27790,#27791,#27792,#27793,
#27794,#27795,#27796,#27797,#27798,#27799,#27800,#27801,#27802,#27803,#27804,
#27805,#27806,#27807,#27808,#27809,#27810,#27811,#27812,#27813,#27814,#27815,
#27816,#27817,#27818,#27819,#27820,#27821,#27822,#27823,#27824,#27825,#27826,
#27827,#27828,#27829,#27830,#27831,#27832,#27833,#27834,#27835,#27836,#27837,
#27838,#27839,#27840,#27841,#27842,#27843,#27844,#27845,#27846,#27847,#27848,
#27849,#27850,#27851,#27852,#27853,#27854,#27855,#27856,#27857,#27858,#27859,
#27860,#27861,#27862),.UNSPECIFIED.,.F.,.F.,(4,2,2,2,2,2,2,2,2,2,2,2,2,
2,2,2,2,2,2,2,2,2,2,2,2,2,2,2,2,2,2,2,2,2,2,2,2,2,2,2,2,2,2,2,2,2,2,2,2,
2,2,2,2,2,2,2,2,2,4),(7.1038028680126E-5,0.0285066862366493,0.0571386449575946,
0.100574193303158,0.152123523332732,0.21131860442887,0.292234682168858,
0.399281002403533,0.503374499092753,0.587374950538041,0.661975647748252,
0.716338959538097,0.75982318655054,0.814118139769595,0.886085679947392,
0.971122954690285,1.06856717084564,1.19872217880814,1.37993904235504,1.57249912376282,
1.72637304930411,1.86310282381987,1.9621025843353,2.04151597658101,2.13698353848521,
2.25454691416929,2.39277180904992,2.55082776156657,2.7452714980945,2.97334127066752,
3.20141104324053,3.39585477976846,3.55391073228511,3.69213562716574,3.80969900284981,
3.90516656475396,3.9845799569996,4.08357971751495,4.22030949203059,4.37418341757175,
4.56674349897935,4.74796036252611,4.87811537048849,4.97555958664375,5.06059686138656,
5.13256440156429,5.18685935478327,5.23034358179564,5.28470689358539,5.35930759079546,
5.44330804224058,5.54740153892958,5.65444785916408,5.73536393690415,5.7945590180004,
5.84610834803006,5.8895438963757,5.91817585509662,5.94661148928363),
 .UNSPECIFIED.);
#2230=B_SPLINE_CURVE_WITH_KNOTS('',3,(#28005,#28006,#28007,#28008,#28009,
#28010,#28011,#28012,#28013,#28014,#28015,#28016,#28017,#28018,#28019,#28020,
#28021,#28022,#28023,#28024,#28025,#28026,#28027,#28028,#28029,#28030,#28031,
#28032,#28033,#28034,#28035,#28036,#28037,#28038,#28039,#28040,#28041,#28042,
#28043,#28044,#28045,#28046),.UNSPECIFIED.,.F.,.F.,(4,2,2,2,2,2,2,2,2,2,
2,2,2,2,2,2,2,2,2,2,4),(4.96665808836377E-5,0.0404121485248788,0.0809389875253708,
0.138678740779869,0.167993113958696,0.227756805017511,0.287784512376069,
0.34661550188191,0.3752023945415,0.434800793278714,0.464184987531579,0.492947800522654,
0.551333883846547,0.611255516075695,0.670320462148153,0.729329203272392,
0.788655454004735,0.817300035390535,0.875619579999266,0.912104776589651,
0.948284438308318),.UNSPECIFIED.);
#2231=B_SPLINE_CURVE_WITH_KNOTS('',3,(#28188,#28189,#28190,#28191,#28192,
#28193,#28194,#28195,#28196,#28197,#28198,#28199,#28200,#28201,#28202,#28203,
#28204,#28205,#28206,#28207,#28208,#28209,#28210,#28211,#28212,#28213,#28214,
#28215,#28216,#28217,#28218,#28219,#28220,#28221,#28222,#28223,#28224,#28225,
#28226,#28227,#28228,#28229,#28230,#28231,#28232,#28233,#28234,#28235,#28236,
#28237,#28238,#28239,#28240,#28241,#28242,#28243,#28244,#28245,#28246,#28247,
#28248,#28249,#28250,#28251,#28252,#28253,#28254,#28255,#28256,#28257,#28258,
#28259,#28260,#28261,#28262,#28263,#28264,#28265,#28266,#28267,#28268,#28269,
#28270,#28271,#28272,#28273,#28274,#28275,#28276,#28277,#28278,#28279,#28280,
#28281,#28282,#28283,#28284,#28285,#28286,#28287,#28288,#28289,#28290,#28291,
#28292,#28293,#28294,#28295,#28296,#28297,#28298,#28299,#28300,#28301,#28302,
#28303),.UNSPECIFIED.,.F.,.F.,(4,2,2,2,2,2,2,2,2,2,2,2,2,2,2,2,2,2,2,2,
2,2,2,2,2,2,2,2,2,2,2,2,2,2,2,2,2,2,2,2,2,2,2,2,2,2,2,2,2,2,2,2,2,2,2,2,
2,4),(9.57215647317225E-5,0.028805838183546,0.0558568013553045,0.114080987998557,
0.161249463922362,0.217422313166586,0.257152574756385,0.304825366934254,
0.361477483325091,0.401213970266859,0.448514553663052,0.503904602332678,
0.543680699307756,0.591367734962095,0.648551016184757,0.688318941212196,
0.735595502996825,0.790419031076046,0.830240895728071,0.878133663029185,
0.936150773297636,0.97594415736791,1.02308308630774,1.07668824732422,1.11656640699563,
1.16485993428889,1.22443813629381,1.29181371179871,1.36063223184655,1.41041636122522,
1.45043902605067,1.49894607576938,1.54456678430888,1.58437861540954,1.64336805299861,
1.68967717074328,1.72949835552286,1.78598579990277,1.8317887234759,1.87155356665554,
1.92955337883068,1.97560054878039,2.01534998788364,2.07236198886952,2.11819652479389,
2.15790547535948,2.21546473932318,2.26137161495789,2.30105577117442,2.35820280734624,
2.40400591908383,2.44365534073145,2.50099895654661,2.54681681861997,2.58643864421989,
2.64357124839567,2.6892861687949,2.74198047995337),.UNSPECIFIED.);
#2232=B_SPLINE_CURVE_WITH_KNOTS('',3,(#28305,#28306,#28307,#28308),
 .UNSPECIFIED.,.F.,.F.,(4,4),(0.,0.0129000141117776),.UNSPECIFIED.);
#2233=B_SPLINE_CURVE_WITH_KNOTS('',3,(#28310,#28311,#28312,#28313,#28314,
#28315,#28316,#28317,#28318,#28319,#28320,#28321,#28322,#28323),
 .UNSPECIFIED.,.F.,.F.,(4,2,2,2,2,2,4),(6.18255457422751E-5,0.0445222550398773,
0.0815855333793703,0.138348319078884,0.188225454345152,0.235381542690196,
0.275928945498945),.UNSPECIFIED.);
#2234=B_SPLINE_CURVE_WITH_KNOTS('',3,(#28325,#28326,#28327,#28328,#28329,
#28330),.UNSPECIFIED.,.F.,.F.,(4,2,4),(-0.0363675439270173,-0.0181932738790337,
-8.99968048774418E-6),.UNSPECIFIED.);
#2235=B_SPLINE_CURVE_WITH_KNOTS('',3,(#28331,#28332,#28333,#28334,#28335,
#28336,#28337,#28338,#28339,#28340,#28341,#28342,#28343,#28344,#28345,#28346,
#28347,#28348,#28349,#28350,#28351,#28352,#28353,#28354,#28355,#28356,#28357,
#28358,#28359,#28360,#28361,#28362,#28363,#28364,#28365,#28366,#28367,#28368,
#28369,#28370,#28371,#28372,#28373,#28374,#28375,#28376,#28377,#28378,#28379,
#28380,#28381,#28382,#28383,#28384,#28385,#28386,#28387,#28388,#28389,#28390,
#28391,#28392,#28393,#28394,#28395,#28396,#28397,#28398,#28399,#28400,#28401,
#28402,#28403,#28404,#28405,#28406,#28407,#28408,#28409,#28410,#28411,#28412,
#28413,#28414,#28415,#28416,#28417,#28418,#28419,#28420,#28421,#28422,#28423,
#28424,#28425,#28426,#28427,#28428,#28429,#28430,#28431,#28432,#28433,#28434,
#28435,#28436,#28437,#28438,#28439,#28440,#28441,#28442,#28443,#28444,#28445,
#28446,#28447,#28448),.UNSPECIFIED.,.F.,.F.,(4,2,2,2,2,2,2,2,2,2,2,2,2,
2,2,2,2,2,2,2,2,2,2,2,2,2,2,2,2,2,2,2,2,2,2,2,2,2,2,2,2,2,2,2,2,2,2,2,2,
2,2,2,2,2,2,2,2,2,4),(-5.94660785390406,-5.91817223520138,-5.8895402920717,
-5.84610476737843,-5.79455546541942,-5.73536041655725,-5.65444438287918,
-5.5473981209355,-5.44330468092936,-5.35930427522568,-5.28470361863854,
-5.23034033645167,-5.18685613311811,-5.1325612094648,-5.06059370847615,
-4.97555648003939,-4.87811231694623,-4.74795737985823,-4.56674061499099,
-4.37418063843972,-4.2203067966888,-4.08357709662776,-3.98457739002157,
-3.90516404101956,-3.80969653110115,-3.69213321943482,-3.55390839982292,
-3.39585253337379,-3.2014089027279,-2.97333925434758,-2.74526960596726,
-2.55082597532136,-2.3927701088722,-2.2545452892603,-2.13698197759396,-2.04151446767552,
-1.96210111867348,-1.86310141206725,-1.72637171200613,-1.57249787025512,
-1.37993789370372,-1.1987211288364,-1.06856619174833,-0.971122028655101,
-0.886084800218291,-0.814117299229607,-0.759822375576234,-0.71633817224261,
-0.661974890055658,-0.587374233468364,-0.503373827764516,-0.399280387758161,
-0.292234125814284,-0.211318092136195,-0.152123043274046,-0.100573741315045,
-0.0571382166217848,-0.0285064768322595,-7.04304336443412E-5),
 .UNSPECIFIED.);
#2236=B_SPLINE_CURVE_WITH_KNOTS('',3,(#28591,#28592,#28593,#28594,#28595,
#28596,#28597,#28598,#28599,#28600),.UNSPECIFIED.,.F.,.F.,(4,2,2,2,4),(-0.148755444895566,
-0.114171890294938,-0.0747141917985825,-0.0422804484276971,-4.41324122456156E-5),
 .UNSPECIFIED.);
#2237=B_SPLINE_CURVE_WITH_KNOTS('',3,(#28601,#28602,#28603,#28604),
 .UNSPECIFIED.,.F.,.F.,(4,4),(-0.00253843258531285,0.),.UNSPECIFIED.);
#2238=B_SPLINE_CURVE_WITH_KNOTS('',3,(#28605,#28606,#28607,#28608,#28609,
#28610,#28611,#28612,#28613,#28614,#28615,#28616,#28617,#28618,#28619,#28620,
#28621,#28622,#28623,#28624,#28625,#28626,#28627,#28628,#28629,#28630,#28631,
#28632,#28633,#28634,#28635,#28636,#28637,#28638),.UNSPECIFIED.,.F.,.F.,
(4,2,2,2,2,2,2,2,2,2,2,2,2,2,2,2,4),(-0.724835095226849,-0.684778550647567,
-0.631527667737965,-0.579128159920059,-0.525654533425143,-0.499826397983904,
-0.443357906433312,-0.417075199883106,-0.362131833684399,-0.306553522094715,
-0.279403621248859,-0.221291231076379,-0.170661187182406,-0.111573179077511,
-0.0622487991085858,-0.031596946474214,-2.64178122616785E-5),
 .UNSPECIFIED.);
#2239=B_SPLINE_CURVE_WITH_KNOTS('',3,(#28640,#28641,#28642,#28643,#28644,
#28645,#28646,#28647,#28648,#28649,#28650,#28651,#28652,#28653,#28654,#28655,
#28656,#28657,#28658,#28659,#28660,#28661,#28662,#28663,#28664,#28665,#28666,
#28667,#28668,#28669,#28670,#28671,#28672,#28673,#28674,#28675,#28676,#28677,
#28678,#28679,#28680,#28681,#28682,#28683,#28684,#28685,#28686,#28687,#28688,
#28689,#28690,#28691,#28692,#28693,#28694,#28695,#28696,#28697,#28698,#28699,
#28700,#28701,#28702,#28703,#28704,#28705,#28706,#28707,#28708,#28709,#28710,
#28711,#28712,#28713,#28714,#28715,#28716,#28717,#28718,#28719,#28720,#28721,
#28722,#28723,#28724,#28725,#28726,#28727,#28728,#28729,#28730,#28731,#28732,
#28733,#28734,#28735,#28736,#28737,#28738,#28739,#28740,#28741,#28742,#28743,
#28744,#28745,#28746,#28747,#28748,#28749,#28750,#28751,#28752,#28753,#28754,
#28755,#28756,#28757),.UNSPECIFIED.,.F.,.F.,(4,2,2,2,2,2,2,2,2,2,2,2,2,
2,2,2,2,2,2,2,2,2,2,2,2,2,2,2,2,2,2,2,2,2,2,2,2,2,2,2,2,2,2,2,2,2,2,2,2,
2,2,2,2,2,2,2,2,2,4),(7.10380286804536E-5,0.0285066862366494,0.0571386449575948,
0.100574193303159,0.152123523332733,0.21131860442887,0.292234682168856,
0.399281002403517,0.503374499092718,0.58737495053799,0.661975647748188,
0.716338959538033,0.75982318655048,0.814118139769539,0.88608567994734,0.971122954690238,
1.0685671708456,1.19872217880811,1.37993904235503,1.57249912376283,1.72637304930414,
1.8631028238199,1.96210258433533,2.04151597658104,2.13698353848524,2.25454691416934,
2.39277180905,2.55082776156668,2.74527149809465,2.97334127066772,3.20141104324078,
3.39585477976875,3.55391073228543,3.69213562716609,3.80969900285018,3.90516656475433,
3.98457995699997,4.08357971751531,4.22030949203093,4.37418341757207,4.56674349897965,
4.74796036252637,4.87811537048874,4.975559586644,5.0605968613868,5.13256440156451,
5.18685935478351,5.23034358179591,5.28470689358571,5.35930759079585,5.44330804224105,
5.54740153893017,5.65444785916474,5.73536393690472,5.79455901800088,5.84610834803048,
5.88954389637607,5.91817569303648,5.94661170936932),.UNSPECIFIED.);
#2240=B_SPLINE_CURVE_WITH_KNOTS('',3,(#28758,#28759,#28760,#28761,#28762,
#28763),.UNSPECIFIED.,.F.,.F.,(4,2,4),(-0.0225817708757373,-0.0112843508253838,
-2.98243785195915E-5),.UNSPECIFIED.);
#2241=B_SPLINE_CURVE_WITH_KNOTS('',3,(#28774,#28775,#28776,#28777,#28778,
#28779),.UNSPECIFIED.,.F.,.F.,(4,2,4),(-0.00584242467456242,-0.00295752748558409,
-6.89218742153712E-5),.UNSPECIFIED.);
#2242=B_SPLINE_CURVE_WITH_KNOTS('',3,(#28958,#28959,#28960,#28961,#28962,
#28963),.UNSPECIFIED.,.F.,.F.,(4,2,4),(0.716974528647988,0.741226803621157,
0.765479078593388),.UNSPECIFIED.);
#2243=B_SPLINE_CURVE_WITH_KNOTS('',3,(#28965,#28966,#28967,#28968,#28969,
#28970,#28971,#28972,#28973,#28974,#28975,#28976,#28977,#28978,#28979),
 .UNSPECIFIED.,.F.,.F.,(4,3,2,2,2,2,4),(-0.00535406387047143,0.,0.00280519627261519,
0.0127729727608755,0.022681421764352,0.0323964936700699,0.0339100227105242),
 .UNSPECIFIED.);
#2244=B_SPLINE_CURVE_WITH_KNOTS('',3,(#28981,#28982,#28983,#28984),
 .UNSPECIFIED.,.F.,.F.,(4,4),(-0.907105856924628,-0.889730448331648),
 .UNSPECIFIED.);
#2245=B_SPLINE_CURVE_WITH_KNOTS('',3,(#28988,#28989,#28990,#28991),
 .UNSPECIFIED.,.F.,.F.,(4,4),(-0.70632843047102,-0.688953021878057),
 .UNSPECIFIED.);
#2246=B_SPLINE_CURVE_WITH_KNOTS('',3,(#28993,#28994,#28995,#28996,#28997,
#28998,#28999,#29000,#29001,#29002,#29003,#29004,#29005,#29006,#29007),
 .UNSPECIFIED.,.F.,.F.,(4,2,2,2,3,2,4),(-0.0339185312885629,-0.0292377700958602,
-0.0195230415801756,-0.00979953953065908,0.,0.00316958312039792,0.00534140243914174),
 .UNSPECIFIED.);
#2247=B_SPLINE_CURVE_WITH_KNOTS('',3,(#29016,#29017,#29018,#29019,#29020,
#29021,#29022,#29023,#29024,#29025,#29026,#29027,#29028,#29029,#29030),
 .UNSPECIFIED.,.F.,.F.,(4,3,2,2,2,2,4),(-0.00535406387034717,0.,0.00280519627249134,
0.0127729727607225,0.0226814217641763,0.0323964936698689,0.0339100227105453),
 .UNSPECIFIED.);
#2248=B_SPLINE_CURVE_WITH_KNOTS('',3,(#29032,#29033,#29034,#29035),
 .UNSPECIFIED.,.F.,.F.,(4,4),(-0.907105856925505,-0.889730448332538),
 .UNSPECIFIED.);
#2249=B_SPLINE_CURVE_WITH_KNOTS('',3,(#29039,#29040,#29041,#29042),
 .UNSPECIFIED.,.F.,.F.,(4,4),(-0.706328430471259,-0.688953021878271),
 .UNSPECIFIED.);
#2250=B_SPLINE_CURVE_WITH_KNOTS('',3,(#29044,#29045,#29046,#29047,#29048,
#29049,#29050,#29051,#29052,#29053,#29054,#29055,#29056,#29057,#29058),
 .UNSPECIFIED.,.F.,.F.,(4,2,2,2,3,2,4),(-0.0339185312884587,-0.0292377700958738,
-0.0195230415801824,-0.00979953953066153,0.,0.00316958312052598,0.00534140243929431),
 .UNSPECIFIED.);
#2251=B_SPLINE_CURVE_WITH_KNOTS('',3,(#29060,#29061,#29062,#29063,#29064,
#29065),.UNSPECIFIED.,.F.,.F.,(4,2,4),(-0.765479078594523,-0.74122680362135,
-0.716974528649115),.UNSPECIFIED.);
#2252=B_SPLINE_CURVE_WITH_KNOTS('',3,(#29067,#29068,#29069,#29070,#29071,
#29072,#29073,#29074,#29075,#29076,#29077,#29078,#29079,#29080,#29081),
 .UNSPECIFIED.,.F.,.F.,(4,3,2,2,2,2,4),(-0.0053540638702789,0.,0.00280519627268264,
0.0127729727609155,0.0226814217643626,0.0323964936700513,0.0339100227106541),
 .UNSPECIFIED.);
#2253=B_SPLINE_CURVE_WITH_KNOTS('',3,(#29083,#29084,#29085,#29086),
 .UNSPECIFIED.,.F.,.F.,(4,4),(0.688953021878874,0.706328430471897),
 .UNSPECIFIED.);
#2254=B_SPLINE_CURVE_WITH_KNOTS('',3,(#29090,#29091,#29092,#29093),
 .UNSPECIFIED.,.F.,.F.,(4,4),(-0.706328430472139,-0.688953021879099),
 .UNSPECIFIED.);
#2255=B_SPLINE_CURVE_WITH_KNOTS('',3,(#29095,#29096,#29097,#29098,#29099,
#29100,#29101,#29102,#29103,#29104,#29105,#29106,#29107,#29108,#29109),
 .UNSPECIFIED.,.F.,.F.,(4,2,2,2,3,2,4),(-0.0339185312885506,-0.0292377700958903,
-0.0195230415801947,-0.00979953953066585,0.,0.00316958312070759,0.00534140243922694),
 .UNSPECIFIED.);
#2256=B_SPLINE_CURVE_WITH_KNOTS('',3,(#29113,#29114,#29115,#29116,#29117,
#29118,#29119,#29120,#29121,#29122,#29123,#29124,#29125,#29126,#29127),
 .UNSPECIFIED.,.F.,.F.,(4,3,2,2,2,2,4),(-0.00535406387039295,0.,0.00280519627280415,
0.0127729727610477,0.0226814217644997,0.0323964936701972,0.0339100227105755),
 .UNSPECIFIED.);
#2257=B_SPLINE_CURVE_WITH_KNOTS('',3,(#29129,#29130,#29131,#29132),
 .UNSPECIFIED.,.F.,.F.,(4,4),(-0.907105856924454,-0.889730448331417),
 .UNSPECIFIED.);
#2258=B_SPLINE_CURVE_WITH_KNOTS('',3,(#29136,#29137,#29138,#29139),
 .UNSPECIFIED.,.F.,.F.,(4,4),(-0.706328430471901,-0.688953021878885),
 .UNSPECIFIED.);
#2259=B_SPLINE_CURVE_WITH_KNOTS('',3,(#29140,#29141,#29142,#29143,#29144,
#29145,#29146,#29147,#29148,#29149,#29150,#29151,#29152,#29153,#29154),
 .UNSPECIFIED.,.F.,.F.,(4,2,2,2,3,2,4),(-0.0339185312886601,-0.0292377700958805,
-0.0195230415801892,-0.00979953953066422,0.,0.00316958312058088,0.00534140243907669),
 .UNSPECIFIED.);
#2674=LINE('',#25157,#3139);
#2675=LINE('',#25201,#3140);
#2676=LINE('',#25762,#3141);
#2677=LINE('',#26022,#3142);
#2678=LINE('',#26024,#3143);
#2679=LINE('',#26376,#3144);
#2680=LINE('',#26649,#3145);
#2681=LINE('',#26909,#3146);
#2682=LINE('',#27169,#3147);
#2683=LINE('',#27484,#3148);
#2684=LINE('',#27744,#3149);
#2685=LINE('',#28004,#3150);
#2686=LINE('',#28772,#3151);
#2687=LINE('',#28925,#3152);
#2688=LINE('',#29157,#3153);
#2689=LINE('',#29159,#3154);
#2690=LINE('',#29160,#3155);
#2691=LINE('',#29164,#3156);
#2692=LINE('',#29168,#3157);
#2693=LINE('',#29172,#3158);
#2694=LINE('',#29176,#3159);
#2695=LINE('',#29180,#3160);
#2696=LINE('',#29183,#3161);
#2697=LINE('',#29187,#3162);
#2698=LINE('',#29191,#3163);
#2699=LINE('',#29195,#3164);
#2700=LINE('',#29199,#3165);
#2701=LINE('',#29203,#3166);
#2702=LINE('',#29207,#3167);
#2703=LINE('',#29211,#3168);
#2704=LINE('',#29212,#3169);
#2705=LINE('',#29213,#3170);
#2706=LINE('',#29216,#3171);
#2707=LINE('',#29218,#3172);
#2708=LINE('',#29222,#3173);
#2709=LINE('',#29224,#3174);
#2710=LINE('',#29228,#3175);
#2711=LINE('',#29230,#3176);
#2712=LINE('',#29234,#3177);
#2713=LINE('',#29237,#3178);
#2714=LINE('',#29238,#3179);
#2715=LINE('',#29240,#3180);
#2716=LINE('',#29242,#3181);
#2717=LINE('',#29245,#3182);
#2718=LINE('',#29246,#3183);
#2719=LINE('',#29248,#3184);
#2720=LINE('',#29250,#3185);
#2721=LINE('',#29253,#3186);
#2722=LINE('',#29255,#3187);
#2723=LINE('',#29257,#3188);
#2724=LINE('',#29259,#3189);
#2725=LINE('',#29261,#3190);
#2726=LINE('',#29263,#3191);
#2727=LINE('',#29265,#3192);
#2728=LINE('',#29267,#3193);
#2729=LINE('',#29269,#3194);
#2730=LINE('',#29272,#3195);
#2731=LINE('',#29274,#3196);
#3139=VECTOR('',#11284,1.393148400081);
#3140=VECTOR('',#11293,0.02886751345948);
#3141=VECTOR('',#11296,0.05773502691896);
#3142=VECTOR('',#11297,0.442264973080985);
#3143=VECTOR('',#11298,0.442264973080985);
#3144=VECTOR('',#11301,0.442264973080985);
#3145=VECTOR('',#11302,0.442264973080985);
#3146=VECTOR('',#11303,0.05773502691896);
#3147=VECTOR('',#11304,0.442264973080985);
#3148=VECTOR('',#11305,0.442264973080985);
#3149=VECTOR('',#11306,0.05773502691896);
#3150=VECTOR('',#11307,0.442264973080985);
#3151=VECTOR('',#11320,0.290824116479001);
#3152=VECTOR('',#11329,3.);
#3153=VECTOR('',#11350,1.48424358004605);
#3154=VECTOR('',#11351,0.2394366603764);
#3155=VECTOR('',#11352,1.48424358004605);
#3156=VECTOR('',#11357,1.50481684780505);
#3157=VECTOR('',#11360,0.4019026509541);
#3158=VECTOR('',#11363,0.2394366603764);
#3159=VECTOR('',#11366,0.4019026509541);
#3160=VECTOR('',#11369,0.4019026509541);
#3161=VECTOR('',#11372,0.4019026509541);
#3162=VECTOR('',#11375,0.4019026509541);
#3163=VECTOR('',#11378,0.2394366603764);
#3164=VECTOR('',#11381,0.4019026509541);
#3165=VECTOR('',#11384,0.4019026509541);
#3166=VECTOR('',#11387,0.2394366603764);
#3167=VECTOR('',#11390,0.4019026509541);
#3168=VECTOR('',#11395,0.2218939514837);
#3169=VECTOR('',#11396,1.50481684780505);
#3170=VECTOR('',#11397,1.51143779167605);
#3171=VECTOR('',#11400,0.2218939514837);
#3172=VECTOR('',#11401,0.2218939514837);
#3173=VECTOR('',#11406,0.2218939514837);
#3174=VECTOR('',#11407,0.2218939514837);
#3175=VECTOR('',#11412,0.2218939514837);
#3176=VECTOR('',#11413,0.2218939514837);
#3177=VECTOR('',#11418,0.2218939514837);
#3178=VECTOR('',#11423,1.51143779167605);
#3179=VECTOR('',#11424,1.50481684780505);
#3180=VECTOR('',#11427,1.48424358004605);
#3181=VECTOR('',#11430,1.48424358004605);
#3182=VECTOR('',#11435,1.48424358004605);
#3183=VECTOR('',#11436,1.48424358004605);
#3184=VECTOR('',#11439,1.50481684780505);
#3185=VECTOR('',#11442,1.51143779167605);
#3186=VECTOR('',#11447,1.50481684780505);
#3187=VECTOR('',#11450,1.51143779167605);
#3188=VECTOR('',#11453,1.51143779167605);
#3189=VECTOR('',#11456,1.50481684780505);
#3190=VECTOR('',#11459,1.48424358004605);
#3191=VECTOR('',#11462,1.48424358004605);
#3192=VECTOR('',#11465,1.50481684780505);
#3193=VECTOR('',#11468,1.51143779167605);
#3194=VECTOR('',#11471,1.51143779167605);
#3195=VECTOR('',#11476,1.51143779167605);
#3196=VECTOR('',#11479,1.50481684780505);
#3771=VERTEX_POINT('',#25155);
#3772=VERTEX_POINT('',#25156);
#3773=VERTEX_POINT('',#25158);
#3774=VERTEX_POINT('',#25177);
#3775=VERTEX_POINT('',#25178);
#3776=VERTEX_POINT('',#25200);
#3777=VERTEX_POINT('',#25202);
#3778=VERTEX_POINT('',#25204);
#3779=VERTEX_POINT('',#25362);
#3780=VERTEX_POINT('',#25761);
#3781=VERTEX_POINT('',#26021);
#3782=VERTEX_POINT('',#26023);
#3783=VERTEX_POINT('',#26025);
#3784=VERTEX_POINT('',#26068);
#3785=VERTEX_POINT('',#26517);
#3786=VERTEX_POINT('',#26648);
#3787=VERTEX_POINT('',#26908);
#3788=VERTEX_POINT('',#27168);
#3789=VERTEX_POINT('',#27352);
#3790=VERTEX_POINT('',#27483);
#3791=VERTEX_POINT('',#27743);
#3792=VERTEX_POINT('',#28003);
#3793=VERTEX_POINT('',#28187);
#3794=VERTEX_POINT('',#28304);
#3795=VERTEX_POINT('',#28309);
#3796=VERTEX_POINT('',#28324);
#3797=VERTEX_POINT('',#28589);
#3798=VERTEX_POINT('',#28590);
#3799=VERTEX_POINT('',#28639);
#3800=VERTEX_POINT('',#28765);
#3801=VERTEX_POINT('',#28768);
#3802=VERTEX_POINT('',#28921);
#3803=VERTEX_POINT('',#28924);
#3804=VERTEX_POINT('',#28926);
#3805=VERTEX_POINT('',#28956);
#3806=VERTEX_POINT('',#28957);
#3807=VERTEX_POINT('',#28964);
#3808=VERTEX_POINT('',#28980);
#3809=VERTEX_POINT('',#28985);
#3810=VERTEX_POINT('',#28987);
#3811=VERTEX_POINT('',#28992);
#3812=VERTEX_POINT('',#29008);
#3813=VERTEX_POINT('',#29013);
#3814=VERTEX_POINT('',#29015);
#3815=VERTEX_POINT('',#29031);
#3816=VERTEX_POINT('',#29036);
#3817=VERTEX_POINT('',#29038);
#3818=VERTEX_POINT('',#29043);
#3819=VERTEX_POINT('',#29059);
#3820=VERTEX_POINT('',#29066);
#3821=VERTEX_POINT('',#29082);
#3822=VERTEX_POINT('',#29087);
#3823=VERTEX_POINT('',#29089);
#3824=VERTEX_POINT('',#29094);
#3825=VERTEX_POINT('',#29110);
#3826=VERTEX_POINT('',#29112);
#3827=VERTEX_POINT('',#29128);
#3828=VERTEX_POINT('',#29133);
#3829=VERTEX_POINT('',#29135);
#3830=VERTEX_POINT('',#29156);
#3831=VERTEX_POINT('',#29158);
#3832=VERTEX_POINT('',#29162);
#3833=VERTEX_POINT('',#29166);
#3834=VERTEX_POINT('',#29167);
#3835=VERTEX_POINT('',#29169);
#3836=VERTEX_POINT('',#29171);
#3837=VERTEX_POINT('',#29173);
#3838=VERTEX_POINT('',#29175);
#3839=VERTEX_POINT('',#29177);
#3840=VERTEX_POINT('',#29179);
#3841=VERTEX_POINT('',#29182);
#3842=VERTEX_POINT('',#29184);
#3843=VERTEX_POINT('',#29186);
#3844=VERTEX_POINT('',#29188);
#3845=VERTEX_POINT('',#29190);
#3846=VERTEX_POINT('',#29192);
#3847=VERTEX_POINT('',#29194);
#3848=VERTEX_POINT('',#29196);
#3849=VERTEX_POINT('',#29198);
#3850=VERTEX_POINT('',#29200);
#3851=VERTEX_POINT('',#29202);
#3852=VERTEX_POINT('',#29204);
#3853=VERTEX_POINT('',#29206);
#3854=VERTEX_POINT('',#29210);
#3855=VERTEX_POINT('',#29215);
#3856=VERTEX_POINT('',#29217);
#3857=VERTEX_POINT('',#29221);
#3858=VERTEX_POINT('',#29223);
#3859=VERTEX_POINT('',#29227);
#3860=VERTEX_POINT('',#29229);
#3861=VERTEX_POINT('',#29233);
#4834=EDGE_CURVE('',#3771,#3772,#2674,.T.);
#4835=EDGE_CURVE('',#3773,#3771,#2213,.T.);
#4836=EDGE_CURVE('',#3773,#3772,#1874,.T.);
#4837=EDGE_CURVE('',#3774,#3775,#1875,.T.);
#4838=EDGE_CURVE('',#3775,#3774,#2214,.T.);
#4839=EDGE_CURVE('',#3776,#3774,#2675,.T.);
#4840=EDGE_CURVE('',#3776,#3777,#1876,.T.);
#4841=EDGE_CURVE('',#3778,#3777,#2215,.T.);
#4842=EDGE_CURVE('',#3775,#3778,#2216,.T.);
#4843=EDGE_CURVE('',#3778,#3779,#2217,.T.);
#4844=EDGE_CURVE('',#3779,#3780,#2676,.T.);
#4845=EDGE_CURVE('',#3776,#3780,#2218,.T.);
#4846=EDGE_CURVE('',#3781,#3776,#2677,.T.);
#4847=EDGE_CURVE('',#3780,#3782,#2678,.T.);
#4848=EDGE_CURVE('',#3782,#3783,#2219,.T.);
#4849=EDGE_CURVE('',#3784,#3783,#2220,.F.);
#4850=EDGE_CURVE('',#3781,#3784,#2221,.T.);
#4851=EDGE_CURVE('',#3777,#3781,#2222,.T.);
#4852=EDGE_CURVE('',#3783,#3779,#2679,.T.);
#4853=EDGE_CURVE('',#3782,#3785,#2223,.T.);
#4854=EDGE_CURVE('',#3785,#3786,#2680,.T.);
#4855=EDGE_CURVE('',#3779,#3786,#2224,.T.);
#4856=EDGE_CURVE('',#3786,#3787,#2681,.T.);
#4857=EDGE_CURVE('',#3780,#3787,#2225,.T.);
#4858=EDGE_CURVE('',#3787,#3788,#2682,.T.);
#4859=EDGE_CURVE('',#3788,#3785,#2226,.T.);
#4860=EDGE_CURVE('',#3788,#3789,#2227,.T.);
#4861=EDGE_CURVE('',#3789,#3790,#2683,.T.);
#4862=EDGE_CURVE('',#3786,#3790,#2228,.T.);
#4863=EDGE_CURVE('',#3790,#3791,#2684,.T.);
#4864=EDGE_CURVE('',#3787,#3791,#2229,.T.);
#4865=EDGE_CURVE('',#3791,#3792,#2685,.T.);
#4866=EDGE_CURVE('',#3792,#3789,#2230,.T.);
#4867=EDGE_CURVE('',#3792,#3793,#2231,.T.);
#4868=EDGE_CURVE('',#3794,#3793,#2232,.T.);
#4869=EDGE_CURVE('',#3795,#3794,#2233,.T.);
#4870=EDGE_CURVE('',#3795,#3796,#2234,.T.);
#4871=EDGE_CURVE('',#3790,#3796,#2235,.T.);
#4872=EDGE_CURVE('',#3797,#3798,#2236,.T.);
#4873=EDGE_CURVE('',#3797,#3773,#2237,.T.);
#4874=EDGE_CURVE('',#3771,#3794,#2238,.T.);
#4875=EDGE_CURVE('',#3791,#3799,#2239,.T.);
#4876=EDGE_CURVE('',#3799,#3798,#2240,.T.);
#4877=EDGE_CURVE('',#3800,#3798,#1877,.T.);
#4878=EDGE_CURVE('',#3772,#3800,#1878,.T.);
#4879=EDGE_CURVE('',#3772,#3801,#1879,.T.);
#4880=EDGE_CURVE('',#3801,#3801,#1880,.T.);
#4881=EDGE_CURVE('',#3800,#3795,#2686,.T.);
#4882=EDGE_CURVE('',#3796,#3799,#2241,.T.);
#4883=EDGE_CURVE('',#3802,#3802,#1881,.T.);
#4884=EDGE_CURVE('',#3802,#3803,#2687,.T.);
#4885=EDGE_CURVE('',#3803,#3804,#1882,.T.);
#4886=EDGE_CURVE('',#3804,#3803,#1883,.T.);
#4887=EDGE_CURVE('',#3805,#3806,#2242,.F.);
#4888=EDGE_CURVE('',#3806,#3807,#2243,.T.);
#4889=EDGE_CURVE('',#3807,#3808,#2244,.T.);
#4890=EDGE_CURVE('',#3809,#3808,#1884,.T.);
#4891=EDGE_CURVE('',#3809,#3810,#2245,.T.);
#4892=EDGE_CURVE('',#3810,#3811,#2246,.T.);
#4893=EDGE_CURVE('',#3811,#3812,#65,.T.);
#4894=EDGE_CURVE('',#3812,#3804,#63,.T.);
#4895=EDGE_CURVE('',#3812,#3813,#66,.T.);
#4896=EDGE_CURVE('',#3813,#3814,#2247,.T.);
#4897=EDGE_CURVE('',#3814,#3815,#2248,.T.);
#4898=EDGE_CURVE('',#3816,#3815,#1885,.T.);
#4899=EDGE_CURVE('',#3816,#3817,#2249,.T.);
#4900=EDGE_CURVE('',#3817,#3818,#2250,.T.);
#4901=EDGE_CURVE('',#3818,#3819,#2251,.T.);
#4902=EDGE_CURVE('',#3819,#3820,#2252,.T.);
#4903=EDGE_CURVE('',#3820,#3821,#2253,.T.);
#4904=EDGE_CURVE('',#3821,#3822,#1886,.T.);
#4905=EDGE_CURVE('',#3822,#3823,#2254,.T.);
#4906=EDGE_CURVE('',#3823,#3824,#2255,.T.);
#4907=EDGE_CURVE('',#3824,#3825,#67,.T.);
#4908=EDGE_CURVE('',#3825,#3826,#2256,.T.);
#4909=EDGE_CURVE('',#3826,#3827,#2257,.T.);
#4910=EDGE_CURVE('',#3827,#3828,#1887,.T.);
#4911=EDGE_CURVE('',#3828,#3829,#2258,.T.);
#4912=EDGE_CURVE('',#3829,#3805,#2259,.T.);
#4913=EDGE_CURVE('',#3811,#3830,#2688,.T.);
#4914=EDGE_CURVE('',#3831,#3830,#2689,.T.);
#4915=EDGE_CURVE('',#3813,#3831,#2690,.T.);
#4916=EDGE_CURVE('',#3830,#3832,#68,.T.);
#4917=EDGE_CURVE('',#3810,#3832,#2691,.T.);
#4918=EDGE_CURVE('',#3833,#3834,#2692,.T.);
#4919=EDGE_CURVE('',#3834,#3835,#69,.T.);
#4920=EDGE_CURVE('',#3835,#3836,#2693,.T.);
#4921=EDGE_CURVE('',#3836,#3837,#70,.T.);
#4922=EDGE_CURVE('',#3837,#3838,#2694,.T.);
#4923=EDGE_CURVE('',#3838,#3839,#71,.T.);
#4924=EDGE_CURVE('',#3839,#3840,#2695,.T.);
#4925=EDGE_CURVE('',#3840,#3831,#72,.T.);
#4926=EDGE_CURVE('',#3832,#3841,#2696,.T.);
#4927=EDGE_CURVE('',#3841,#3842,#73,.T.);
#4928=EDGE_CURVE('',#3842,#3843,#2697,.T.);
#4929=EDGE_CURVE('',#3843,#3844,#74,.T.);
#4930=EDGE_CURVE('',#3844,#3845,#2698,.T.);
#4931=EDGE_CURVE('',#3845,#3846,#75,.T.);
#4932=EDGE_CURVE('',#3846,#3847,#2699,.T.);
#4933=EDGE_CURVE('',#3847,#3848,#76,.T.);
#4934=EDGE_CURVE('',#3848,#3849,#2700,.T.);
#4935=EDGE_CURVE('',#3849,#3850,#77,.T.);
#4936=EDGE_CURVE('',#3850,#3851,#2701,.T.);
#4937=EDGE_CURVE('',#3851,#3852,#78,.T.);
#4938=EDGE_CURVE('',#3852,#3853,#2702,.T.);
#4939=EDGE_CURVE('',#3853,#3833,#79,.T.);
#4940=EDGE_CURVE('',#3854,#3821,#2703,.T.);
#4941=EDGE_CURVE('',#3820,#3834,#2704,.T.);
#4942=EDGE_CURVE('',#3833,#3854,#2705,.T.);
#4943=EDGE_CURVE('',#3816,#3855,#2706,.T.);
#4944=EDGE_CURVE('',#3856,#3815,#2707,.T.);
#4945=EDGE_CURVE('',#3856,#3855,#80,.T.);
#4946=EDGE_CURVE('',#3809,#3857,#2708,.T.);
#4947=EDGE_CURVE('',#3858,#3808,#2709,.T.);
#4948=EDGE_CURVE('',#3858,#3857,#81,.T.);
#4949=EDGE_CURVE('',#3828,#3859,#2710,.T.);
#4950=EDGE_CURVE('',#3860,#3827,#2711,.T.);
#4951=EDGE_CURVE('',#3860,#3859,#82,.T.);
#4952=EDGE_CURVE('',#3822,#3861,#2712,.T.);
#4953=EDGE_CURVE('',#3854,#3861,#83,.T.);
#4954=EDGE_CURVE('',#3838,#3855,#2713,.T.);
#4955=EDGE_CURVE('',#3817,#3837,#2714,.T.);
#4956=EDGE_CURVE('',#3818,#3836,#2715,.T.);
#4957=EDGE_CURVE('',#3819,#3835,#2716,.T.);
#4958=EDGE_CURVE('',#3824,#3851,#2717,.T.);
#4959=EDGE_CURVE('',#3825,#3850,#2718,.T.);
#4960=EDGE_CURVE('',#3823,#3852,#2719,.T.);
#4961=EDGE_CURVE('',#3853,#3861,#2720,.T.);
#4962=EDGE_CURVE('',#3826,#3849,#2721,.T.);
#4963=EDGE_CURVE('',#3848,#3860,#2722,.T.);
#4964=EDGE_CURVE('',#3847,#3859,#2723,.T.);
#4965=EDGE_CURVE('',#3829,#3846,#2724,.T.);
#4966=EDGE_CURVE('',#3805,#3845,#2725,.T.);
#4967=EDGE_CURVE('',#3806,#3844,#2726,.T.);
#4968=EDGE_CURVE('',#3807,#3843,#2727,.T.);
#4969=EDGE_CURVE('',#3842,#3858,#2728,.T.);
#4970=EDGE_CURVE('',#3841,#3857,#2729,.T.);
#4971=EDGE_CURVE('',#3839,#3856,#2730,.T.);
#4972=EDGE_CURVE('',#3814,#3840,#2731,.T.);
#6776=ORIENTED_EDGE('',*,*,#4834,.F.);
#6777=ORIENTED_EDGE('',*,*,#4835,.F.);
#6778=ORIENTED_EDGE('',*,*,#4836,.T.);
#6779=ORIENTED_EDGE('',*,*,#4837,.T.);
#6780=ORIENTED_EDGE('',*,*,#4838,.T.);
#6781=ORIENTED_EDGE('',*,*,#4837,.F.);
#6782=ORIENTED_EDGE('',*,*,#4839,.F.);
#6783=ORIENTED_EDGE('',*,*,#4840,.T.);
#6784=ORIENTED_EDGE('',*,*,#4841,.F.);
#6785=ORIENTED_EDGE('',*,*,#4842,.F.);
#6786=ORIENTED_EDGE('',*,*,#4839,.T.);
#6787=ORIENTED_EDGE('',*,*,#4838,.F.);
#6788=ORIENTED_EDGE('',*,*,#4842,.T.);
#6789=ORIENTED_EDGE('',*,*,#4843,.T.);
#6790=ORIENTED_EDGE('',*,*,#4844,.T.);
#6791=ORIENTED_EDGE('',*,*,#4845,.F.);
#6792=ORIENTED_EDGE('',*,*,#4846,.T.);
#6793=ORIENTED_EDGE('',*,*,#4845,.T.);
#6794=ORIENTED_EDGE('',*,*,#4847,.T.);
#6795=ORIENTED_EDGE('',*,*,#4848,.T.);
#6796=ORIENTED_EDGE('',*,*,#4849,.F.);
#6797=ORIENTED_EDGE('',*,*,#4850,.F.);
#6798=ORIENTED_EDGE('',*,*,#4851,.F.);
#6799=ORIENTED_EDGE('',*,*,#4840,.F.);
#6800=ORIENTED_EDGE('',*,*,#4846,.F.);
#6801=ORIENTED_EDGE('',*,*,#4851,.T.);
#6802=ORIENTED_EDGE('',*,*,#4850,.T.);
#6803=ORIENTED_EDGE('',*,*,#4849,.T.);
#6804=ORIENTED_EDGE('',*,*,#4852,.T.);
#6805=ORIENTED_EDGE('',*,*,#4843,.F.);
#6806=ORIENTED_EDGE('',*,*,#4841,.T.);
#6807=ORIENTED_EDGE('',*,*,#4848,.F.);
#6808=ORIENTED_EDGE('',*,*,#4853,.T.);
#6809=ORIENTED_EDGE('',*,*,#4854,.T.);
#6810=ORIENTED_EDGE('',*,*,#4855,.F.);
#6811=ORIENTED_EDGE('',*,*,#4852,.F.);
#6812=ORIENTED_EDGE('',*,*,#4844,.F.);
#6813=ORIENTED_EDGE('',*,*,#4855,.T.);
#6814=ORIENTED_EDGE('',*,*,#4856,.T.);
#6815=ORIENTED_EDGE('',*,*,#4857,.F.);
#6816=ORIENTED_EDGE('',*,*,#4853,.F.);
#6817=ORIENTED_EDGE('',*,*,#4847,.F.);
#6818=ORIENTED_EDGE('',*,*,#4857,.T.);
#6819=ORIENTED_EDGE('',*,*,#4858,.T.);
#6820=ORIENTED_EDGE('',*,*,#4859,.T.);
#6821=ORIENTED_EDGE('',*,*,#4859,.F.);
#6822=ORIENTED_EDGE('',*,*,#4860,.T.);
#6823=ORIENTED_EDGE('',*,*,#4861,.T.);
#6824=ORIENTED_EDGE('',*,*,#4862,.F.);
#6825=ORIENTED_EDGE('',*,*,#4854,.F.);
#6826=ORIENTED_EDGE('',*,*,#4856,.F.);
#6827=ORIENTED_EDGE('',*,*,#4862,.T.);
#6828=ORIENTED_EDGE('',*,*,#4863,.T.);
#6829=ORIENTED_EDGE('',*,*,#4864,.F.);
#6830=ORIENTED_EDGE('',*,*,#4860,.F.);
#6831=ORIENTED_EDGE('',*,*,#4858,.F.);
#6832=ORIENTED_EDGE('',*,*,#4864,.T.);
#6833=ORIENTED_EDGE('',*,*,#4865,.T.);
#6834=ORIENTED_EDGE('',*,*,#4866,.T.);
#6835=ORIENTED_EDGE('',*,*,#4867,.T.);
#6836=ORIENTED_EDGE('',*,*,#4868,.F.);
#6837=ORIENTED_EDGE('',*,*,#4869,.F.);
#6838=ORIENTED_EDGE('',*,*,#4870,.T.);
#6839=ORIENTED_EDGE('',*,*,#4871,.F.);
#6840=ORIENTED_EDGE('',*,*,#4861,.F.);
#6841=ORIENTED_EDGE('',*,*,#4866,.F.);
#6842=ORIENTED_EDGE('',*,*,#4872,.F.);
#6843=ORIENTED_EDGE('',*,*,#4873,.T.);
#6844=ORIENTED_EDGE('',*,*,#4835,.T.);
#6845=ORIENTED_EDGE('',*,*,#4874,.T.);
#6846=ORIENTED_EDGE('',*,*,#4868,.T.);
#6847=ORIENTED_EDGE('',*,*,#4867,.F.);
#6848=ORIENTED_EDGE('',*,*,#4865,.F.);
#6849=ORIENTED_EDGE('',*,*,#4875,.T.);
#6850=ORIENTED_EDGE('',*,*,#4876,.T.);
#6851=ORIENTED_EDGE('',*,*,#4836,.F.);
#6852=ORIENTED_EDGE('',*,*,#4873,.F.);
#6853=ORIENTED_EDGE('',*,*,#4872,.T.);
#6854=ORIENTED_EDGE('',*,*,#4877,.F.);
#6855=ORIENTED_EDGE('',*,*,#4878,.F.);
#6856=ORIENTED_EDGE('',*,*,#4879,.T.);
#6857=ORIENTED_EDGE('',*,*,#4880,.T.);
#6858=ORIENTED_EDGE('',*,*,#4879,.F.);
#6859=ORIENTED_EDGE('',*,*,#4834,.T.);
#6860=ORIENTED_EDGE('',*,*,#4878,.T.);
#6861=ORIENTED_EDGE('',*,*,#4881,.T.);
#6862=ORIENTED_EDGE('',*,*,#4869,.T.);
#6863=ORIENTED_EDGE('',*,*,#4874,.F.);
#6864=ORIENTED_EDGE('',*,*,#4870,.F.);
#6865=ORIENTED_EDGE('',*,*,#4881,.F.);
#6866=ORIENTED_EDGE('',*,*,#4877,.T.);
#6867=ORIENTED_EDGE('',*,*,#4876,.F.);
#6868=ORIENTED_EDGE('',*,*,#4882,.F.);
#6869=ORIENTED_EDGE('',*,*,#4863,.F.);
#6870=ORIENTED_EDGE('',*,*,#4871,.T.);
#6871=ORIENTED_EDGE('',*,*,#4882,.T.);
#6872=ORIENTED_EDGE('',*,*,#4875,.F.);
#6873=ORIENTED_EDGE('',*,*,#4883,.T.);
#6874=ORIENTED_EDGE('',*,*,#4880,.F.);
#6875=ORIENTED_EDGE('',*,*,#4883,.F.);
#6876=ORIENTED_EDGE('',*,*,#4884,.T.);
#6877=ORIENTED_EDGE('',*,*,#4885,.T.);
#6878=ORIENTED_EDGE('',*,*,#4886,.T.);
#6879=ORIENTED_EDGE('',*,*,#4884,.F.);
#6880=ORIENTED_EDGE('',*,*,#4887,.T.);
#6881=ORIENTED_EDGE('',*,*,#4888,.T.);
#6882=ORIENTED_EDGE('',*,*,#4889,.T.);
#6883=ORIENTED_EDGE('',*,*,#4890,.F.);
#6884=ORIENTED_EDGE('',*,*,#4891,.T.);
#6885=ORIENTED_EDGE('',*,*,#4892,.T.);
#6886=ORIENTED_EDGE('',*,*,#4893,.T.);
#6887=ORIENTED_EDGE('',*,*,#4894,.T.);
#6888=ORIENTED_EDGE('',*,*,#4885,.F.);
#6889=ORIENTED_EDGE('',*,*,#4886,.F.);
#6890=ORIENTED_EDGE('',*,*,#4894,.F.);
#6891=ORIENTED_EDGE('',*,*,#4895,.T.);
#6892=ORIENTED_EDGE('',*,*,#4896,.T.);
#6893=ORIENTED_EDGE('',*,*,#4897,.T.);
#6894=ORIENTED_EDGE('',*,*,#4898,.F.);
#6895=ORIENTED_EDGE('',*,*,#4899,.T.);
#6896=ORIENTED_EDGE('',*,*,#4900,.T.);
#6897=ORIENTED_EDGE('',*,*,#4901,.T.);
#6898=ORIENTED_EDGE('',*,*,#4902,.T.);
#6899=ORIENTED_EDGE('',*,*,#4903,.T.);
#6900=ORIENTED_EDGE('',*,*,#4904,.T.);
#6901=ORIENTED_EDGE('',*,*,#4905,.T.);
#6902=ORIENTED_EDGE('',*,*,#4906,.T.);
#6903=ORIENTED_EDGE('',*,*,#4907,.T.);
#6904=ORIENTED_EDGE('',*,*,#4908,.T.);
#6905=ORIENTED_EDGE('',*,*,#4909,.T.);
#6906=ORIENTED_EDGE('',*,*,#4910,.T.);
#6907=ORIENTED_EDGE('',*,*,#4911,.T.);
#6908=ORIENTED_EDGE('',*,*,#4912,.T.);
#6909=ORIENTED_EDGE('',*,*,#4913,.T.);
#6910=ORIENTED_EDGE('',*,*,#4914,.F.);
#6911=ORIENTED_EDGE('',*,*,#4915,.F.);
#6912=ORIENTED_EDGE('',*,*,#4895,.F.);
#6913=ORIENTED_EDGE('',*,*,#4893,.F.);
#6914=ORIENTED_EDGE('',*,*,#4916,.F.);
#6915=ORIENTED_EDGE('',*,*,#4913,.F.);
#6916=ORIENTED_EDGE('',*,*,#4892,.F.);
#6917=ORIENTED_EDGE('',*,*,#4917,.T.);
#6918=ORIENTED_EDGE('',*,*,#4918,.T.);
#6919=ORIENTED_EDGE('',*,*,#4919,.T.);
#6920=ORIENTED_EDGE('',*,*,#4920,.T.);
#6921=ORIENTED_EDGE('',*,*,#4921,.T.);
#6922=ORIENTED_EDGE('',*,*,#4922,.T.);
#6923=ORIENTED_EDGE('',*,*,#4923,.T.);
#6924=ORIENTED_EDGE('',*,*,#4924,.T.);
#6925=ORIENTED_EDGE('',*,*,#4925,.T.);
#6926=ORIENTED_EDGE('',*,*,#4914,.T.);
#6927=ORIENTED_EDGE('',*,*,#4916,.T.);
#6928=ORIENTED_EDGE('',*,*,#4926,.T.);
#6929=ORIENTED_EDGE('',*,*,#4927,.T.);
#6930=ORIENTED_EDGE('',*,*,#4928,.T.);
#6931=ORIENTED_EDGE('',*,*,#4929,.T.);
#6932=ORIENTED_EDGE('',*,*,#4930,.T.);
#6933=ORIENTED_EDGE('',*,*,#4931,.T.);
#6934=ORIENTED_EDGE('',*,*,#4932,.T.);
#6935=ORIENTED_EDGE('',*,*,#4933,.T.);
#6936=ORIENTED_EDGE('',*,*,#4934,.T.);
#6937=ORIENTED_EDGE('',*,*,#4935,.T.);
#6938=ORIENTED_EDGE('',*,*,#4936,.T.);
#6939=ORIENTED_EDGE('',*,*,#4937,.T.);
#6940=ORIENTED_EDGE('',*,*,#4938,.T.);
#6941=ORIENTED_EDGE('',*,*,#4939,.T.);
#6942=ORIENTED_EDGE('',*,*,#4940,.T.);
#6943=ORIENTED_EDGE('',*,*,#4903,.F.);
#6944=ORIENTED_EDGE('',*,*,#4941,.T.);
#6945=ORIENTED_EDGE('',*,*,#4918,.F.);
#6946=ORIENTED_EDGE('',*,*,#4942,.T.);
#6947=ORIENTED_EDGE('',*,*,#4943,.F.);
#6948=ORIENTED_EDGE('',*,*,#4898,.T.);
#6949=ORIENTED_EDGE('',*,*,#4944,.F.);
#6950=ORIENTED_EDGE('',*,*,#4945,.T.);
#6951=ORIENTED_EDGE('',*,*,#4946,.F.);
#6952=ORIENTED_EDGE('',*,*,#4890,.T.);
#6953=ORIENTED_EDGE('',*,*,#4947,.F.);
#6954=ORIENTED_EDGE('',*,*,#4948,.T.);
#6955=ORIENTED_EDGE('',*,*,#4949,.F.);
#6956=ORIENTED_EDGE('',*,*,#4910,.F.);
#6957=ORIENTED_EDGE('',*,*,#4950,.F.);
#6958=ORIENTED_EDGE('',*,*,#4951,.T.);
#6959=ORIENTED_EDGE('',*,*,#4952,.F.);
#6960=ORIENTED_EDGE('',*,*,#4904,.F.);
#6961=ORIENTED_EDGE('',*,*,#4940,.F.);
#6962=ORIENTED_EDGE('',*,*,#4953,.T.);
#6963=ORIENTED_EDGE('',*,*,#4943,.T.);
#6964=ORIENTED_EDGE('',*,*,#4954,.F.);
#6965=ORIENTED_EDGE('',*,*,#4922,.F.);
#6966=ORIENTED_EDGE('',*,*,#4955,.F.);
#6967=ORIENTED_EDGE('',*,*,#4899,.F.);
#6968=ORIENTED_EDGE('',*,*,#4921,.F.);
#6969=ORIENTED_EDGE('',*,*,#4956,.F.);
#6970=ORIENTED_EDGE('',*,*,#4900,.F.);
#6971=ORIENTED_EDGE('',*,*,#4955,.T.);
#6972=ORIENTED_EDGE('',*,*,#4957,.F.);
#6973=ORIENTED_EDGE('',*,*,#4901,.F.);
#6974=ORIENTED_EDGE('',*,*,#4956,.T.);
#6975=ORIENTED_EDGE('',*,*,#4920,.F.);
#6976=ORIENTED_EDGE('',*,*,#4919,.F.);
#6977=ORIENTED_EDGE('',*,*,#4941,.F.);
#6978=ORIENTED_EDGE('',*,*,#4902,.F.);
#6979=ORIENTED_EDGE('',*,*,#4957,.T.);
#6980=ORIENTED_EDGE('',*,*,#4958,.T.);
#6981=ORIENTED_EDGE('',*,*,#4936,.F.);
#6982=ORIENTED_EDGE('',*,*,#4959,.F.);
#6983=ORIENTED_EDGE('',*,*,#4907,.F.);
#6984=ORIENTED_EDGE('',*,*,#4937,.F.);
#6985=ORIENTED_EDGE('',*,*,#4958,.F.);
#6986=ORIENTED_EDGE('',*,*,#4906,.F.);
#6987=ORIENTED_EDGE('',*,*,#4960,.T.);
#6988=ORIENTED_EDGE('',*,*,#4952,.T.);
#6989=ORIENTED_EDGE('',*,*,#4961,.F.);
#6990=ORIENTED_EDGE('',*,*,#4938,.F.);
#6991=ORIENTED_EDGE('',*,*,#4960,.F.);
#6992=ORIENTED_EDGE('',*,*,#4905,.F.);
#6993=ORIENTED_EDGE('',*,*,#4953,.F.);
#6994=ORIENTED_EDGE('',*,*,#4942,.F.);
#6995=ORIENTED_EDGE('',*,*,#4939,.F.);
#6996=ORIENTED_EDGE('',*,*,#4961,.T.);
#6997=ORIENTED_EDGE('',*,*,#4935,.F.);
#6998=ORIENTED_EDGE('',*,*,#4962,.F.);
#6999=ORIENTED_EDGE('',*,*,#4908,.F.);
#7000=ORIENTED_EDGE('',*,*,#4959,.T.);
#7001=ORIENTED_EDGE('',*,*,#4950,.T.);
#7002=ORIENTED_EDGE('',*,*,#4909,.F.);
#7003=ORIENTED_EDGE('',*,*,#4962,.T.);
#7004=ORIENTED_EDGE('',*,*,#4934,.F.);
#7005=ORIENTED_EDGE('',*,*,#4963,.T.);
#7006=ORIENTED_EDGE('',*,*,#4951,.F.);
#7007=ORIENTED_EDGE('',*,*,#4963,.F.);
#7008=ORIENTED_EDGE('',*,*,#4933,.F.);
#7009=ORIENTED_EDGE('',*,*,#4964,.T.);
#7010=ORIENTED_EDGE('',*,*,#4949,.T.);
#7011=ORIENTED_EDGE('',*,*,#4964,.F.);
#7012=ORIENTED_EDGE('',*,*,#4932,.F.);
#7013=ORIENTED_EDGE('',*,*,#4965,.F.);
#7014=ORIENTED_EDGE('',*,*,#4911,.F.);
#7015=ORIENTED_EDGE('',*,*,#4931,.F.);
#7016=ORIENTED_EDGE('',*,*,#4966,.F.);
#7017=ORIENTED_EDGE('',*,*,#4912,.F.);
#7018=ORIENTED_EDGE('',*,*,#4965,.T.);
#7019=ORIENTED_EDGE('',*,*,#4966,.T.);
#7020=ORIENTED_EDGE('',*,*,#4930,.F.);
#7021=ORIENTED_EDGE('',*,*,#4967,.F.);
#7022=ORIENTED_EDGE('',*,*,#4887,.F.);
#7023=ORIENTED_EDGE('',*,*,#4929,.F.);
#7024=ORIENTED_EDGE('',*,*,#4968,.F.);
#7025=ORIENTED_EDGE('',*,*,#4888,.F.);
#7026=ORIENTED_EDGE('',*,*,#4967,.T.);
#7027=ORIENTED_EDGE('',*,*,#4947,.T.);
#7028=ORIENTED_EDGE('',*,*,#4889,.F.);
#7029=ORIENTED_EDGE('',*,*,#4968,.T.);
#7030=ORIENTED_EDGE('',*,*,#4928,.F.);
#7031=ORIENTED_EDGE('',*,*,#4969,.T.);
#7032=ORIENTED_EDGE('',*,*,#4948,.F.);
#7033=ORIENTED_EDGE('',*,*,#4969,.F.);
#7034=ORIENTED_EDGE('',*,*,#4927,.F.);
#7035=ORIENTED_EDGE('',*,*,#4970,.T.);
#7036=ORIENTED_EDGE('',*,*,#4946,.T.);
#7037=ORIENTED_EDGE('',*,*,#4970,.F.);
#7038=ORIENTED_EDGE('',*,*,#4926,.F.);
#7039=ORIENTED_EDGE('',*,*,#4917,.F.);
#7040=ORIENTED_EDGE('',*,*,#4891,.F.);
#7041=ORIENTED_EDGE('',*,*,#4945,.F.);
#7042=ORIENTED_EDGE('',*,*,#4971,.F.);
#7043=ORIENTED_EDGE('',*,*,#4923,.F.);
#7044=ORIENTED_EDGE('',*,*,#4954,.T.);
#7045=ORIENTED_EDGE('',*,*,#4944,.T.);
#7046=ORIENTED_EDGE('',*,*,#4897,.F.);
#7047=ORIENTED_EDGE('',*,*,#4972,.T.);
#7048=ORIENTED_EDGE('',*,*,#4924,.F.);
#7049=ORIENTED_EDGE('',*,*,#4971,.T.);
#7050=ORIENTED_EDGE('',*,*,#4925,.F.);
#7051=ORIENTED_EDGE('',*,*,#4972,.F.);
#7052=ORIENTED_EDGE('',*,*,#4896,.F.);
#7053=ORIENTED_EDGE('',*,*,#4915,.T.);
#8492=CYLINDRICAL_SURFACE('',#9709,1.116987298108);
#8493=CYLINDRICAL_SURFACE('',#9721,3.);
#8494=CYLINDRICAL_SURFACE('',#9732,0.25);
#8495=CYLINDRICAL_SURFACE('',#9756,0.25);
#8496=CYLINDRICAL_SURFACE('',#9758,0.25);
#8497=CYLINDRICAL_SURFACE('',#9760,0.25);
#8498=CYLINDRICAL_SURFACE('',#9762,0.25);
#8499=CYLINDRICAL_SURFACE('',#9763,0.25);
#8500=CYLINDRICAL_SURFACE('',#9765,0.25);
#8501=CYLINDRICAL_SURFACE('',#9767,0.25);
#8502=CYLINDRICAL_SURFACE('',#9769,0.25);
#8503=CYLINDRICAL_SURFACE('',#9771,0.25);
#8504=CYLINDRICAL_SURFACE('',#9773,0.25);
#8505=CYLINDRICAL_SURFACE('',#9775,0.25);
#8793=ADVANCED_FACE('',(#730),#199,.T.);
#8794=ADVANCED_FACE('',(#731),#438,.T.);
#8795=ADVANCED_FACE('',(#732),#8492,.T.);
#8796=ADVANCED_FACE('',(#733),#358,.F.);
#8797=ADVANCED_FACE('',(#734),#359,.F.);
#8798=ADVANCED_FACE('',(#735),#200,.T.);
#8799=ADVANCED_FACE('',(#736),#360,.F.);
#8800=ADVANCED_FACE('',(#737),#361,.F.);
#8801=ADVANCED_FACE('',(#738),#362,.F.);
#8802=ADVANCED_FACE('',(#739),#363,.F.);
#8803=ADVANCED_FACE('',(#740),#364,.F.);
#8804=ADVANCED_FACE('',(#741),#365,.F.);
#8805=ADVANCED_FACE('',(#742),#366,.F.);
#8806=ADVANCED_FACE('',(#743),#367,.F.);
#8807=ADVANCED_FACE('',(#744),#368,.F.);
#8808=ADVANCED_FACE('',(#745),#209,.F.);
#8809=ADVANCED_FACE('',(#746),#201,.T.);
#8810=ADVANCED_FACE('',(#747),#439,.F.);
#8811=ADVANCED_FACE('',(#748),#369,.F.);
#8812=ADVANCED_FACE('',(#749,#299),#440,.T.);
#8813=ADVANCED_FACE('',(#750),#8493,.T.);
#8814=ADVANCED_FACE('',(#751),#127,.F.);
#8815=ADVANCED_FACE('',(#752),#441,.F.);
#8816=ADVANCED_FACE('',(#753),#8494,.F.);
#8817=ADVANCED_FACE('',(#754),#442,.T.);
#8818=ADVANCED_FACE('',(#755),#443,.F.);
#8819=ADVANCED_FACE('',(#756),#444,.F.);
#8820=ADVANCED_FACE('',(#757),#445,.F.);
#8821=ADVANCED_FACE('',(#758),#446,.F.);
#8822=ADVANCED_FACE('',(#759),#447,.F.);
#8823=ADVANCED_FACE('',(#760),#448,.F.);
#8824=ADVANCED_FACE('',(#761),#8495,.F.);
#8825=ADVANCED_FACE('',(#762),#449,.F.);
#8826=ADVANCED_FACE('',(#763),#8496,.F.);
#8827=ADVANCED_FACE('',(#764),#450,.F.);
#8828=ADVANCED_FACE('',(#765),#8497,.F.);
#8829=ADVANCED_FACE('',(#766),#451,.F.);
#8830=ADVANCED_FACE('',(#767),#8498,.T.);
#8831=ADVANCED_FACE('',(#768),#8499,.F.);
#8832=ADVANCED_FACE('',(#769),#452,.F.);
#8833=ADVANCED_FACE('',(#770),#8500,.T.);
#8834=ADVANCED_FACE('',(#771),#453,.F.);
#8835=ADVANCED_FACE('',(#772),#8501,.F.);
#8836=ADVANCED_FACE('',(#773),#454,.F.);
#8837=ADVANCED_FACE('',(#774),#8502,.F.);
#8838=ADVANCED_FACE('',(#775),#455,.F.);
#8839=ADVANCED_FACE('',(#776),#8503,.T.);
#8840=ADVANCED_FACE('',(#777),#456,.F.);
#8841=ADVANCED_FACE('',(#778),#8504,.T.);
#8842=ADVANCED_FACE('',(#779),#457,.F.);
#8843=ADVANCED_FACE('',(#780),#8505,.F.);
#9122=CLOSED_SHELL('',(#8793,#8794,#8795,#8796,#8797,#8798,#8799,#8800,
#8801,#8802,#8803,#8804,#8805,#8806,#8807,#8808,#8809,#8810,#8811,#8812,
#8813,#8814,#8815,#8816,#8817,#8818,#8819,#8820,#8821,#8822,#8823,#8824,
#8825,#8826,#8827,#8828,#8829,#8830,#8831,#8832,#8833,#8834,#8835,#8836,
#8837,#8838,#8839,#8840,#8841,#8842,#8843));
#9704=AXIS2_PLACEMENT_3D('',#25153,#11280,#11281);
#9705=AXIS2_PLACEMENT_3D('',#25154,#11282,#11283);
#9706=AXIS2_PLACEMENT_3D('',#25175,#11285,#11286);
#9707=AXIS2_PLACEMENT_3D('',#25176,#11287,#11288);
#9708=AXIS2_PLACEMENT_3D('',#25179,#11289,#11290);
#9709=AXIS2_PLACEMENT_3D('',#25199,#11291,#11292);
#9710=AXIS2_PLACEMENT_3D('',#25203,#11294,#11295);
#9711=AXIS2_PLACEMENT_3D('',#26199,#11299,#11300);
#9712=AXIS2_PLACEMENT_3D('',#28764,#11308,#11309);
#9713=AXIS2_PLACEMENT_3D('',#28766,#11310,#11311);
#9714=AXIS2_PLACEMENT_3D('',#28767,#11312,#11313);
#9715=AXIS2_PLACEMENT_3D('',#28769,#11314,#11315);
#9716=AXIS2_PLACEMENT_3D('',#28770,#11316,#11317);
#9717=AXIS2_PLACEMENT_3D('',#28771,#11318,#11319);
#9718=AXIS2_PLACEMENT_3D('',#28773,#11321,#11322);
#9719=AXIS2_PLACEMENT_3D('',#28920,#11323,#11324);
#9720=AXIS2_PLACEMENT_3D('',#28922,#11325,#11326);
#9721=AXIS2_PLACEMENT_3D('',#28923,#11327,#11328);
#9722=AXIS2_PLACEMENT_3D('',#28927,#11330,#11331);
#9723=AXIS2_PLACEMENT_3D('',#28928,#11332,#11333);
#9724=AXIS2_PLACEMENT_3D('',#28986,#11334,#11335);
#9725=AXIS2_PLACEMENT_3D('',#29009,#11336,#11337);
#9726=AXIS2_PLACEMENT_3D('',#29014,#11338,#11339);
#9727=AXIS2_PLACEMENT_3D('',#29037,#11340,#11341);
#9728=AXIS2_PLACEMENT_3D('',#29088,#11342,#11343);
#9729=AXIS2_PLACEMENT_3D('',#29111,#11344,#11345);
#9730=AXIS2_PLACEMENT_3D('',#29134,#11346,#11347);
#9731=AXIS2_PLACEMENT_3D('',#29155,#11348,#11349);
#9732=AXIS2_PLACEMENT_3D('',#29161,#11353,#11354);
#9733=AXIS2_PLACEMENT_3D('',#29163,#11355,#11356);
#9734=AXIS2_PLACEMENT_3D('',#29165,#11358,#11359);
#9735=AXIS2_PLACEMENT_3D('',#29170,#11361,#11362);
#9736=AXIS2_PLACEMENT_3D('',#29174,#11364,#11365);
#9737=AXIS2_PLACEMENT_3D('',#29178,#11367,#11368);
#9738=AXIS2_PLACEMENT_3D('',#29181,#11370,#11371);
#9739=AXIS2_PLACEMENT_3D('',#29185,#11373,#11374);
#9740=AXIS2_PLACEMENT_3D('',#29189,#11376,#11377);
#9741=AXIS2_PLACEMENT_3D('',#29193,#11379,#11380);
#9742=AXIS2_PLACEMENT_3D('',#29197,#11382,#11383);
#9743=AXIS2_PLACEMENT_3D('',#29201,#11385,#11386);
#9744=AXIS2_PLACEMENT_3D('',#29205,#11388,#11389);
#9745=AXIS2_PLACEMENT_3D('',#29208,#11391,#11392);
#9746=AXIS2_PLACEMENT_3D('',#29209,#11393,#11394);
#9747=AXIS2_PLACEMENT_3D('',#29214,#11398,#11399);
#9748=AXIS2_PLACEMENT_3D('',#29219,#11402,#11403);
#9749=AXIS2_PLACEMENT_3D('',#29220,#11404,#11405);
#9750=AXIS2_PLACEMENT_3D('',#29225,#11408,#11409);
#9751=AXIS2_PLACEMENT_3D('',#29226,#11410,#11411);
#9752=AXIS2_PLACEMENT_3D('',#29231,#11414,#11415);
#9753=AXIS2_PLACEMENT_3D('',#29232,#11416,#11417);
#9754=AXIS2_PLACEMENT_3D('',#29235,#11419,#11420);
#9755=AXIS2_PLACEMENT_3D('',#29236,#11421,#11422);
#9756=AXIS2_PLACEMENT_3D('',#29239,#11425,#11426);
#9757=AXIS2_PLACEMENT_3D('',#29241,#11428,#11429);
#9758=AXIS2_PLACEMENT_3D('',#29243,#11431,#11432);
#9759=AXIS2_PLACEMENT_3D('',#29244,#11433,#11434);
#9760=AXIS2_PLACEMENT_3D('',#29247,#11437,#11438);
#9761=AXIS2_PLACEMENT_3D('',#29249,#11440,#11441);
#9762=AXIS2_PLACEMENT_3D('',#29251,#11443,#11444);
#9763=AXIS2_PLACEMENT_3D('',#29252,#11445,#11446);
#9764=AXIS2_PLACEMENT_3D('',#29254,#11448,#11449);
#9765=AXIS2_PLACEMENT_3D('',#29256,#11451,#11452);
#9766=AXIS2_PLACEMENT_3D('',#29258,#11454,#11455);
#9767=AXIS2_PLACEMENT_3D('',#29260,#11457,#11458);
#9768=AXIS2_PLACEMENT_3D('',#29262,#11460,#11461);
#9769=AXIS2_PLACEMENT_3D('',#29264,#11463,#11464);
#9770=AXIS2_PLACEMENT_3D('',#29266,#11466,#11467);
#9771=AXIS2_PLACEMENT_3D('',#29268,#11469,#11470);
#9772=AXIS2_PLACEMENT_3D('',#29270,#11472,#11473);
#9773=AXIS2_PLACEMENT_3D('',#29271,#11474,#11475);
#9774=AXIS2_PLACEMENT_3D('',#29273,#11477,#11478);
#9775=AXIS2_PLACEMENT_3D('',#29275,#11480,#11481);
#11280=DIRECTION('axis',(0.,0.,1.));
#11281=DIRECTION('refdir',(1.,0.,0.));
#11282=DIRECTION('center_axis',(0.,0.,1.));
#11283=DIRECTION('ref_axis',(0.,1.,0.));
#11284=DIRECTION('',(-4.18853873767699E-17,0.342020143325669,-0.939692620785908));
#11285=DIRECTION('center_axis',(0.,0.,1.));
#11286=DIRECTION('ref_axis',(-0.901991229138518,0.431754354416009,0.));
#11287=DIRECTION('center_axis',(0.,0.,1.));
#11288=DIRECTION('ref_axis',(0.,1.,0.));
#11289=DIRECTION('center_axis',(0.,0.,1.));
#11290=DIRECTION('ref_axis',(0.,1.,0.));
#11291=DIRECTION('center_axis',(0.,0.,1.));
#11292=DIRECTION('ref_axis',(-0.180387890266709,-0.983595551558223,0.));
#11293=DIRECTION('',(0.,0.,1.));
#11294=DIRECTION('center_axis',(0.,0.,1.));
#11295=DIRECTION('ref_axis',(0.,1.,0.));
#11296=DIRECTION('',(0.,0.,-1.));
#11297=DIRECTION('',(0.,-0.866025403784429,0.500000000000017));
#11298=DIRECTION('',(0.,-0.866025403784429,-0.500000000000017));
#11299=DIRECTION('center_axis',(0.,0.,-1.));
#11300=DIRECTION('ref_axis',(0.,-1.,0.));
#11301=DIRECTION('',(0.,0.866025403784429,-0.500000000000017));
#11302=DIRECTION('',(0.,-0.866025403784429,-0.500000000000017));
#11303=DIRECTION('',(0.,0.,-1.));
#11304=DIRECTION('',(0.,0.866025403784429,-0.500000000000017));
#11305=DIRECTION('',(0.,0.866025403784429,-0.500000000000017));
#11306=DIRECTION('',(0.,0.,-1.));
#11307=DIRECTION('',(0.,-0.866025403784429,-0.500000000000017));
#11308=DIRECTION('center_axis',(0.,0.,1.));
#11309=DIRECTION('ref_axis',(0.,1.,0.));
#11310=DIRECTION('center_axis',(1.,0.,0.));
#11311=DIRECTION('ref_axis',(0.,-0.939692620785897,0.342020143325699));
#11312=DIRECTION('center_axis',(0.,0.,1.));
#11313=DIRECTION('ref_axis',(-0.901991229138518,0.431754354416009,0.));
#11314=DIRECTION('center_axis',(-1.,-1.22464679914735E-16,0.));
#11315=DIRECTION('ref_axis',(1.22464679914735E-16,-1.,0.));
#11316=DIRECTION('center_axis',(0.,0.,1.));
#11317=DIRECTION('ref_axis',(0.,1.,0.));
#11318=DIRECTION('center_axis',(0.,0.,1.));
#11319=DIRECTION('ref_axis',(0.,1.,0.));
#11320=DIRECTION('',(0.,0.342020143325699,0.939692620785897));
#11321=DIRECTION('center_axis',(1.,0.,0.));
#11322=DIRECTION('ref_axis',(0.,-1.,0.));
#11323=DIRECTION('center_axis',(0.,0.,1.));
#11324=DIRECTION('ref_axis',(0.,1.,0.));
#11325=DIRECTION('center_axis',(0.,0.,1.));
#11326=DIRECTION('ref_axis',(0.,1.,0.));
#11327=DIRECTION('center_axis',(0.,0.,1.));
#11328=DIRECTION('ref_axis',(0.,1.,0.));
#11329=DIRECTION('',(0.,0.,-1.));
#11330=DIRECTION('center_axis',(0.,0.,1.));
#11331=DIRECTION('ref_axis',(0.,1.,0.));
#11332=DIRECTION('center_axis',(0.,0.,1.));
#11333=DIRECTION('ref_axis',(0.,1.,0.));
#11334=DIRECTION('center_axis',(0.,0.,-1.));
#11335=DIRECTION('ref_axis',(0.889042601598659,-0.457824477876279,0.));
#11336=DIRECTION('center_axis',(0.996194698083924,0.,0.0871557428370583));
#11337=DIRECTION('ref_axis',(-1.12154994191049E-8,-0.999999999999992,1.28193744829457E-7));
#11338=DIRECTION('center_axis',(0.996194698083924,0.,0.0871557428370583));
#11339=DIRECTION('ref_axis',(-1.12154994191049E-8,-0.999999999999992,1.28193744829457E-7));
#11340=DIRECTION('center_axis',(0.,0.,-1.));
#11341=DIRECTION('ref_axis',(0.457824477876279,0.889042601598659,0.));
#11342=DIRECTION('center_axis',(0.,0.,1.));
#11343=DIRECTION('ref_axis',(-0.457824477876279,0.889042601598659,0.));
#11344=DIRECTION('center_axis',(-0.996194698083924,0.,0.0871557428370583));
#11345=DIRECTION('ref_axis',(-1.12154878567642E-8,-0.999999999999992,-1.28193612671298E-7));
#11346=DIRECTION('center_axis',(0.,0.,1.));
#11347=DIRECTION('ref_axis',(-0.889042601598659,-0.457824477876279,0.));
#11348=DIRECTION('center_axis',(0.996194698091745,0.,0.087155742747664));
#11349=DIRECTION('ref_axis',(0.,-1.,0.));
#11350=DIRECTION('',(-0.0868265938642471,0.0868265938642471,0.992432509138967));
#11351=DIRECTION('',(0.,-1.,0.));
#11352=DIRECTION('',(-0.0868265938642471,-0.0868265938642471,0.992432509138967));
#11353=DIRECTION('center_axis',(-0.0868265938642471,0.0868265938642471,
0.992432509138967));
#11354=DIRECTION('ref_axis',(5.403663627668E-16,-0.996194698091746,0.0871557427476577));
#11355=DIRECTION('center_axis',(0.,0.,-1.));
#11356=DIRECTION('ref_axis',(0.707106781186546,-0.707106781186549,0.));
#11357=DIRECTION('',(-0.0868265938642471,0.0868265938642471,0.992432509138967));
#11358=DIRECTION('center_axis',(0.,0.,-1.));
#11359=DIRECTION('ref_axis',(0.,1.,0.));
#11360=DIRECTION('',(0.,1.,0.));
#11361=DIRECTION('center_axis',(0.,0.,-1.));
#11362=DIRECTION('ref_axis',(-0.707106781186546,0.707106781186549,0.));
#11363=DIRECTION('',(1.,0.,0.));
#11364=DIRECTION('center_axis',(0.,0.,-1.));
#11365=DIRECTION('ref_axis',(0.707106781186549,0.707106781186546,0.));
#11366=DIRECTION('',(0.,-1.,0.));
#11367=DIRECTION('center_axis',(0.,0.,1.));
#11368=DIRECTION('ref_axis',(-0.707106781186546,-0.707106781186549,0.));
#11369=DIRECTION('',(1.,0.,0.));
#11370=DIRECTION('center_axis',(0.,0.,-1.));
#11371=DIRECTION('ref_axis',(0.707106781186549,0.707106781186546,0.));
#11372=DIRECTION('',(-1.,0.,0.));
#11373=DIRECTION('center_axis',(0.,0.,1.));
#11374=DIRECTION('ref_axis',(-0.707106781186549,0.707106781186546,0.));
#11375=DIRECTION('',(0.,-1.,0.));
#11376=DIRECTION('center_axis',(0.,0.,-1.));
#11377=DIRECTION('ref_axis',(0.707106781186546,-0.707106781186549,0.));
#11378=DIRECTION('',(-1.,0.,0.));
#11379=DIRECTION('center_axis',(0.,0.,-1.));
#11380=DIRECTION('ref_axis',(-0.707106781186549,-0.707106781186546,0.));
#11381=DIRECTION('',(0.,1.,0.));
#11382=DIRECTION('center_axis',(0.,0.,1.));
#11383=DIRECTION('ref_axis',(0.707106781186546,0.707106781186549,0.));
#11384=DIRECTION('',(-1.,0.,0.));
#11385=DIRECTION('center_axis',(0.,0.,-1.));
#11386=DIRECTION('ref_axis',(-0.707106781186549,-0.707106781186546,0.));
#11387=DIRECTION('',(0.,1.,0.));
#11388=DIRECTION('center_axis',(0.,0.,-1.));
#11389=DIRECTION('ref_axis',(-0.707106781186546,0.707106781186549,0.));
#11390=DIRECTION('',(1.,0.,0.));
#11391=DIRECTION('center_axis',(0.,0.,1.));
#11392=DIRECTION('ref_axis',(0.707106781186549,-0.707106781186546,0.));
#11393=DIRECTION('center_axis',(-0.996194698091745,0.,0.087155742747664));
#11394=DIRECTION('ref_axis',(0.,1.,0.));
#11395=DIRECTION('',(0.,1.,0.));
#11396=DIRECTION('',(0.0868265938642471,-0.0868265938642471,0.992432509138967));
#11397=DIRECTION('',(-0.0868265938642471,0.0868265938642471,-0.992432509138967));
#11398=DIRECTION('center_axis',(0.,0.,1.));
#11399=DIRECTION('ref_axis',(0.,1.,0.));
#11400=DIRECTION('',(0.,-1.,0.));
#11401=DIRECTION('',(1.,0.,0.));
#11402=DIRECTION('center_axis',(0.,0.,-1.));
#11403=DIRECTION('ref_axis',(-0.707106781186546,-0.707106781186549,0.));
#11404=DIRECTION('center_axis',(0.,0.,1.));
#11405=DIRECTION('ref_axis',(0.,1.,0.));
#11406=DIRECTION('',(-1.,0.,0.));
#11407=DIRECTION('',(0.,-1.,0.));
#11408=DIRECTION('center_axis',(0.,0.,-1.));
#11409=DIRECTION('ref_axis',(-0.707106781186549,0.707106781186546,0.));
#11410=DIRECTION('center_axis',(0.,0.,1.));
#11411=DIRECTION('ref_axis',(0.,1.,0.));
#11412=DIRECTION('',(0.,1.,0.));
#11413=DIRECTION('',(-1.,0.,0.));
#11414=DIRECTION('center_axis',(0.,0.,-1.));
#11415=DIRECTION('ref_axis',(0.707106781186546,0.707106781186549,0.));
#11416=DIRECTION('center_axis',(0.,0.,1.));
#11417=DIRECTION('ref_axis',(0.,1.,0.));
#11418=DIRECTION('',(1.,0.,0.));
#11419=DIRECTION('center_axis',(0.,0.,-1.));
#11420=DIRECTION('ref_axis',(0.707106781186549,-0.707106781186546,0.));
#11421=DIRECTION('center_axis',(0.996194698091745,0.,0.087155742747664));
#11422=DIRECTION('ref_axis',(0.,-1.,0.));
#11423=DIRECTION('',(0.0868265938642471,0.0868265938642471,-0.992432509138967));
#11424=DIRECTION('',(-0.0868265938642471,-0.0868265938642471,0.992432509138967));
#11425=DIRECTION('center_axis',(-0.0868265938642471,-0.0868265938642471,
0.992432509138967));
#11426=DIRECTION('ref_axis',(0.996194698091746,5.403663627668E-16,0.0871557427476577));
#11427=DIRECTION('',(-0.0868265938642471,-0.0868265938642471,0.992432509138967));
#11428=DIRECTION('center_axis',(0.,0.996194698091745,0.087155742747664));
#11429=DIRECTION('ref_axis',(1.,0.,0.));
#11430=DIRECTION('',(0.0868265938642471,-0.0868265938642471,0.992432509138967));
#11431=DIRECTION('center_axis',(0.0868265938642471,-0.0868265938642471,
0.992432509138967));
#11432=DIRECTION('ref_axis',(-5.403663627668E-16,0.996194698091746,0.0871557427476577));
#11433=DIRECTION('center_axis',(-0.996194698091745,0.,0.087155742747664));
#11434=DIRECTION('ref_axis',(0.,1.,0.));
#11435=DIRECTION('',(0.0868265938642471,-0.0868265938642471,0.992432509138967));
#11436=DIRECTION('',(0.0868265938642471,0.0868265938642471,0.992432509138967));
#11437=DIRECTION('center_axis',(0.0868265938642471,-0.0868265938642471,
0.992432509138967));
#11438=DIRECTION('ref_axis',(-5.403663627668E-16,0.996194698091746,0.0871557427476577));
#11439=DIRECTION('',(0.0868265938642471,-0.0868265938642471,0.992432509138967));
#11440=DIRECTION('center_axis',(0.,0.996194698091745,0.087155742747664));
#11441=DIRECTION('ref_axis',(1.,0.,0.));
#11442=DIRECTION('',(-0.0868265938642471,0.0868265938642471,-0.992432509138967));
#11443=DIRECTION('center_axis',(-0.0868265938642471,0.0868265938642471,
-0.992432509138967));
#11444=DIRECTION('ref_axis',(0.996194698091746,-5.403663627668E-16,-0.0871557427476577));
#11445=DIRECTION('center_axis',(0.0868265938642471,0.0868265938642471,0.992432509138967));
#11446=DIRECTION('ref_axis',(-0.996194698091746,-5.403663627668E-16,0.0871557427476577));
#11447=DIRECTION('',(0.0868265938642471,0.0868265938642471,0.992432509138967));
#11448=DIRECTION('center_axis',(0.,-0.996194698091745,0.087155742747664));
#11449=DIRECTION('ref_axis',(-1.,0.,0.));
#11450=DIRECTION('',(-0.0868265938642471,-0.0868265938642471,-0.992432509138967));
#11451=DIRECTION('center_axis',(-0.0868265938642471,-0.0868265938642471,
-0.992432509138967));
#11452=DIRECTION('ref_axis',(5.403663627668E-16,0.996194698091746,-0.0871557427476577));
#11453=DIRECTION('',(-0.0868265938642471,-0.0868265938642471,-0.992432509138967));
#11454=DIRECTION('center_axis',(-0.996194698091745,0.,0.087155742747664));
#11455=DIRECTION('ref_axis',(0.,1.,0.));
#11456=DIRECTION('',(0.0868265938642471,0.0868265938642471,0.992432509138967));
#11457=DIRECTION('center_axis',(0.0868265938642471,0.0868265938642471,0.992432509138967));
#11458=DIRECTION('ref_axis',(-0.996194698091746,-5.403663627668E-16,0.0871557427476577));
#11459=DIRECTION('',(0.0868265938642372,0.0868265938642472,0.992432509138968));
#11460=DIRECTION('center_axis',(0.,-0.996194698091745,0.087155742747664));
#11461=DIRECTION('ref_axis',(-1.,0.,0.));
#11462=DIRECTION('',(-0.0868265938642471,0.0868265938642471,0.992432509138967));
#11463=DIRECTION('center_axis',(-0.0868265938642471,0.0868265938642471,
0.992432509138967));
#11464=DIRECTION('ref_axis',(5.403663627668E-16,-0.996194698091746,0.0871557427476577));
#11465=DIRECTION('',(-0.0868265938642471,0.0868265938642471,0.992432509138967));
#11466=DIRECTION('center_axis',(0.996194698091745,0.,0.087155742747664));
#11467=DIRECTION('ref_axis',(0.,-1.,0.));
#11468=DIRECTION('',(0.0868265938642471,-0.0868265938642471,-0.992432509138967));
#11469=DIRECTION('center_axis',(0.0868265938642471,-0.0868265938642471,
-0.992432509138967));
#11470=DIRECTION('ref_axis',(-0.996194698091746,5.403663627668E-16,-0.0871557427476577));
#11471=DIRECTION('',(0.0868265938642471,-0.0868265938642471,-0.992432509138967));
#11472=DIRECTION('center_axis',(0.,-0.996194698091745,0.087155742747664));
#11473=DIRECTION('ref_axis',(-1.,0.,0.));
#11474=DIRECTION('center_axis',(0.0868265938642471,0.0868265938642471,-0.992432509138967));
#11475=DIRECTION('ref_axis',(-5.403663627668E-16,-0.996194698091746,-0.0871557427476577));
#11476=DIRECTION('',(0.0868265938642471,0.0868265938642471,-0.992432509138967));
#11477=DIRECTION('center_axis',(0.,0.996194698091745,0.087155742747664));
#11478=DIRECTION('ref_axis',(1.,0.,0.));
#11479=DIRECTION('',(-0.0868265938642471,-0.0868265938642471,0.992432509138967));
#11480=DIRECTION('center_axis',(-0.0868265938642471,-0.0868265938642471,
0.992432509138967));
#11481=DIRECTION('ref_axis',(0.996194698091746,5.403663627668E-16,0.0871557427476577));
#25153=CARTESIAN_POINT('',(0.,0.,0.));
#25154=CARTESIAN_POINT('Origin',(0.,0.,-6.89357235801));
#25155=CARTESIAN_POINT('',(-1.03412062617695E-14,-1.37969296796376,-6.93054085392112));
#25156=CARTESIAN_POINT('',(1.63050934631669E-16,-1.331411920116,-7.06319194267));
#25157=CARTESIAN_POINT('',(1.70611472889645E-16,-1.393148400081,-6.89357235801));
#25158=CARTESIAN_POINT('',(-1.20239717356391,0.571750590758655,-7.06319194267005));
#25159=CARTESIAN_POINT('Ctrl Pts',(-1.20239717356391,0.571750590758656,
-7.06319194267005));
#25160=CARTESIAN_POINT('Ctrl Pts',(-1.26030469923467,0.455247401086438,
-7.05696595606331));
#25161=CARTESIAN_POINT('Ctrl Pts',(-1.30086063595672,0.330766210654013,
-7.05076352264625));
#25162=CARTESIAN_POINT('Ctrl Pts',(-1.34734301081266,0.060099744643785,
-7.03707105795902));
#25163=CARTESIAN_POINT('Ctrl Pts',(-1.34870825310244,-0.0856619352215133,
-7.02959898147411));
#25164=CARTESIAN_POINT('Ctrl Pts',(-1.31385805616803,-0.311224915923542,
-7.01860006937098));
#25165=CARTESIAN_POINT('Ctrl Pts',(-1.29345890223884,-0.392254545151923,
-7.01471383675719));
#25166=CARTESIAN_POINT('Ctrl Pts',(-1.21199792405986,-0.623330282323326,
-7.00312293352462));
#25167=CARTESIAN_POINT('Ctrl Pts',(-1.13128222774601,-0.765171563245202,
-6.99520004112136));
#25168=CARTESIAN_POINT('Ctrl Pts',(-0.91224190618221,-1.02781571641453,
-6.97811271159856));
#25169=CARTESIAN_POINT('Ctrl Pts',(-0.770549270084647,-1.14145066385306,
-6.9698410678562));
#25170=CARTESIAN_POINT('Ctrl Pts',(-0.462335849194596,-1.30185701421122,
-6.95353112872913));
#25171=CARTESIAN_POINT('Ctrl Pts',(-0.300584338674426,-1.35146726655285,
-6.94528925745892));
#25172=CARTESIAN_POINT('Ctrl Pts',(-0.0895408850961822,-1.37594598073772,
-6.93485347223636));
#25173=CARTESIAN_POINT('Ctrl Pts',(-0.0447547005702977,-1.37891813490286,
-6.9326696902598));
#25174=CARTESIAN_POINT('Ctrl Pts',(-2.1941503253841E-14,-1.37969296796376,
-6.93054085392112));
#25175=CARTESIAN_POINT('Origin',(0.,0.,-7.06319194267));
#25176=CARTESIAN_POINT('Origin',(0.,0.,0.));
#25177=CARTESIAN_POINT('',(-1.56243020438409E-6,1.11698728404643,-6.50503918006705E-18));
#25178=CARTESIAN_POINT('',(0.396369471088371,1.04429491357745,0.));
#25179=CARTESIAN_POINT('Origin',(0.,0.,0.));
#25180=CARTESIAN_POINT('Ctrl Pts',(0.396304186491244,1.0441270568326,-3.46944695195361E-18));
#25181=CARTESIAN_POINT('Ctrl Pts',(0.375051486067047,1.05226594471596,1.97766776596492E-18));
#25182=CARTESIAN_POINT('Ctrl Pts',(0.353598170411701,1.05972570838993,1.11865001012778E-17));
#25183=CARTESIAN_POINT('Ctrl Pts',(0.331925748890776,1.06650339612009,1.04083408558608E-17));
#25184=CARTESIAN_POINT('Ctrl Pts',(0.32239163755152,1.06948503014652,1.00660137707996E-17));
#25185=CARTESIAN_POINT('Ctrl Pts',(0.312814080654242,1.07233474927852,-1.11256302644907E-18));
#25186=CARTESIAN_POINT('Ctrl Pts',(0.303195534691942,1.07505027411597,0.));
#25187=CARTESIAN_POINT('Ctrl Pts',(0.278245422830036,1.08209423364204,2.88594264373481E-18));
#25188=CARTESIAN_POINT('Ctrl Pts',(0.253025137328642,1.08823279472093,5.24541165579042E-18));
#25189=CARTESIAN_POINT('Ctrl Pts',(0.227630604189116,1.09346325276002,3.46944695195361E-18));
#25190=CARTESIAN_POINT('Ctrl Pts',(0.201257125734747,1.09889534208581,1.62501978351495E-18));
#25191=CARTESIAN_POINT('Ctrl Pts',(0.17468865526933,1.10335050639761,-1.22639140354306E-17));
#25192=CARTESIAN_POINT('Ctrl Pts',(0.147988322547862,1.10683727158896,-1.38777878078145E-17));
#25193=CARTESIAN_POINT('Ctrl Pts',(0.123448118283646,1.11004194813399,-1.53610948678466E-17));
#25194=CARTESIAN_POINT('Ctrl Pts',(0.098802275556219,1.11242704532112,-1.21825797392063E-17));
#25195=CARTESIAN_POINT('Ctrl Pts',(0.0741337916335476,1.11399860667177,
-1.38777878078145E-17));
#25196=CARTESIAN_POINT('Ctrl Pts',(0.0494653077108761,1.11557016802241,
-1.55729958764226E-17));
#25197=CARTESIAN_POINT('Ctrl Pts',(0.0247654680032384,1.11633121467664,
-6.35703025728058E-19));
#25198=CARTESIAN_POINT('Ctrl Pts',(3.76960662823445E-6,1.11628565725144,
0.));
#25199=CARTESIAN_POINT('Origin',(0.,0.,0.));
#25200=CARTESIAN_POINT('',(-5.22672044210748E-8,1.11698648602171,-0.0288570210841246));
#25201=CARTESIAN_POINT('',(0.,1.116987298108,-0.02886751345948));
#25202=CARTESIAN_POINT('',(0.744968168489605,0.832275826917867,-0.0288675134594948));
#25203=CARTESIAN_POINT('Origin',(0.,0.,-0.02886751345948));
#25204=CARTESIAN_POINT('',(0.741143876287569,0.835683180862249,-0.0288670915312841));
#25205=CARTESIAN_POINT('Ctrl Pts',(0.741143755062205,0.835683044173541,
-0.028867407977449));
#25206=CARTESIAN_POINT('Ctrl Pts',(0.742421161214912,0.834550230034564,
-0.0288674431381309));
#25207=CARTESIAN_POINT('Ctrl Pts',(0.743695970158679,0.833414486969343,
-0.0288674782988128));
#25208=CARTESIAN_POINT('Ctrl Pts',(0.744968168489605,0.832275826917867,
-0.0288675134594948));
#25209=CARTESIAN_POINT('Ctrl Pts',(0.396369471088371,1.04429491357745,0.));
#25210=CARTESIAN_POINT('Ctrl Pts',(0.43828755116425,1.02838461179134,-0.003194245975093));
#25211=CARTESIAN_POINT('Ctrl Pts',(0.479311242034271,1.00992758066369,-0.00639321053358202));
#25212=CARTESIAN_POINT('Ctrl Pts',(0.519226227239376,0.988971561310726,
-0.0096049957435327));
#25213=CARTESIAN_POINT('Ctrl Pts',(0.547511184299327,0.974121496742234,
-0.0118809631848942));
#25214=CARTESIAN_POINT('Ctrl Pts',(0.575237639768719,0.958011828605387,
-0.0141633685999232));
#25215=CARTESIAN_POINT('Ctrl Pts',(0.602193922372281,0.940756665664665,
-0.0164435627914911));
#25216=CARTESIAN_POINT('Ctrl Pts',(0.613277634633324,0.933661797879479,
-0.0173811184882584));
#25217=CARTESIAN_POINT('Ctrl Pts',(0.624231431056695,0.926373805934684,
-0.0183183003473072));
#25218=CARTESIAN_POINT('Ctrl Pts',(0.635041961763314,0.918902786443926,
-0.019254507123577));
#25219=CARTESIAN_POINT('Ctrl Pts',(0.672142748844026,0.893262907059214,
-0.0224674861356659));
#25220=CARTESIAN_POINT('Ctrl Pts',(0.70755889976264,0.865468750629288,-0.0256689806051503));
#25221=CARTESIAN_POINT('Ctrl Pts',(0.741143876287569,0.835683180862249,
-0.0288670915312841));
#25222=CARTESIAN_POINT('Ctrl Pts',(-0.4755900604755,1.010680324589,0.07987340093689));
#25223=CARTESIAN_POINT('Ctrl Pts',(-0.2348081643589,1.123983684464,0.06091506760356));
#25224=CARTESIAN_POINT('Ctrl Pts',(0.329952574922,1.170452920957,0.02299840093689));
#25225=CARTESIAN_POINT('Ctrl Pts',(1.016551442463,0.6677408946503,-0.03387659906311));
#25226=CARTESIAN_POINT('Ctrl Pts',(1.205358893105,-0.1619074151071,-0.09075159906311));
#25227=CARTESIAN_POINT('Ctrl Pts',(0.8042879589087,-0.9122802996697,-0.1476265990631));
#25228=CARTESIAN_POINT('Ctrl Pts',(0.009550993186476,-1.216158607898,-0.2045015990631));
#25229=CARTESIAN_POINT('Ctrl Pts',(-0.7898556864549,-0.9248023542725,-0.2613765990631));
#25230=CARTESIAN_POINT('Ctrl Pts',(-1.202679571961,-0.180814804896,-0.3182515990631));
#25231=CARTESIAN_POINT('Ctrl Pts',(-1.026867975908,0.6516702524068,-0.3751265990631));
#25232=CARTESIAN_POINT('Ctrl Pts',(-0.348469933747,1.165204139133,-0.4320015990631));
#25233=CARTESIAN_POINT('Ctrl Pts',(0.5004819949382,1.108444747226,-0.4888765990631));
#25234=CARTESIAN_POINT('Ctrl Pts',(1.104479823299,0.5091721726955,-0.5457515990631));
#25235=CARTESIAN_POINT('Ctrl Pts',(1.167905052019,-0.3393077836576,-0.6026265990631));
#25236=CARTESIAN_POINT('Ctrl Pts',(0.6597150647482,-1.02171816845,-0.6595015990631));
#25237=CARTESIAN_POINT('Ctrl Pts',(-0.1713634724997,-1.204062516105,-0.7163765990631));
#25238=CARTESIAN_POINT('Ctrl Pts',(-0.9185704929214,-0.7970948701029,-0.7732515990631));
#25239=CARTESIAN_POINT('Ctrl Pts',(-1.216195700701,0.,-0.8301265990631));
#25240=CARTESIAN_POINT('Ctrl Pts',(-0.9185704929214,0.7970948701029,-0.8870015990631));
#25241=CARTESIAN_POINT('Ctrl Pts',(-0.1713634724997,1.204062516105,-0.9438765990631));
#25242=CARTESIAN_POINT('Ctrl Pts',(0.6597150647482,1.02171816845,-1.000751599063));
#25243=CARTESIAN_POINT('Ctrl Pts',(1.167905052019,0.3393077836576,-1.057626599063));
#25244=CARTESIAN_POINT('Ctrl Pts',(1.104479823299,-0.5091721726955,-1.114501599063));
#25245=CARTESIAN_POINT('Ctrl Pts',(0.5004819949382,-1.108444747226,-1.171376599063));
#25246=CARTESIAN_POINT('Ctrl Pts',(-0.348469933747,-1.165204139133,-1.228251599063));
#25247=CARTESIAN_POINT('Ctrl Pts',(-1.026867975908,-0.6516702524068,-1.285126599063));
#25248=CARTESIAN_POINT('Ctrl Pts',(-1.202679571961,0.180814804896,-1.342001599063));
#25249=CARTESIAN_POINT('Ctrl Pts',(-0.7898556864549,0.9248023542725,-1.398876599063));
#25250=CARTESIAN_POINT('Ctrl Pts',(0.009550993186476,1.216158607898,-1.455751599063));
#25251=CARTESIAN_POINT('Ctrl Pts',(0.8042879589087,0.9122802996697,-1.512626599063));
#25252=CARTESIAN_POINT('Ctrl Pts',(1.205358893105,0.161907415107,-1.569501599063));
#25253=CARTESIAN_POINT('Ctrl Pts',(1.016551442463,-0.6677408946503,-1.626376599063));
#25254=CARTESIAN_POINT('Ctrl Pts',(0.329952574922,-1.170452920957,-1.683251599063));
#25255=CARTESIAN_POINT('Ctrl Pts',(-0.2348081643589,-1.123983684464,-1.72116826573));
#25256=CARTESIAN_POINT('Ctrl Pts',(-0.4755900604755,-1.010680324589,-1.740126599063));
#25257=CARTESIAN_POINT('Ctrl Pts',(-0.4755900604755,1.010680324589,0.0499578003123));
#25258=CARTESIAN_POINT('Ctrl Pts',(-0.2348081643589,1.123983684464,0.03099946697896));
#25259=CARTESIAN_POINT('Ctrl Pts',(0.329952574922,1.170452920957,-0.006917199687702));
#25260=CARTESIAN_POINT('Ctrl Pts',(1.016551442463,0.6677408946503,-0.0637921996877));
#25261=CARTESIAN_POINT('Ctrl Pts',(1.205358893105,-0.1619074151071,-0.1206671996877));
#25262=CARTESIAN_POINT('Ctrl Pts',(0.8042879589087,-0.9122802996697,-0.1775421996877));
#25263=CARTESIAN_POINT('Ctrl Pts',(0.009550993186476,-1.216158607898,-0.2344171996877));
#25264=CARTESIAN_POINT('Ctrl Pts',(-0.7898556864549,-0.9248023542725,-0.2912921996877));
#25265=CARTESIAN_POINT('Ctrl Pts',(-1.202679571961,-0.180814804896,-0.3481671996877));
#25266=CARTESIAN_POINT('Ctrl Pts',(-1.026867975908,0.6516702524068,-0.4050421996877));
#25267=CARTESIAN_POINT('Ctrl Pts',(-0.348469933747,1.165204139133,-0.4619171996877));
#25268=CARTESIAN_POINT('Ctrl Pts',(0.5004819949382,1.108444747226,-0.5187921996877));
#25269=CARTESIAN_POINT('Ctrl Pts',(1.104479823299,0.5091721726955,-0.5756671996877));
#25270=CARTESIAN_POINT('Ctrl Pts',(1.167905052019,-0.3393077836576,-0.6325421996877));
#25271=CARTESIAN_POINT('Ctrl Pts',(0.6597150647482,-1.02171816845,-0.6894171996877));
#25272=CARTESIAN_POINT('Ctrl Pts',(-0.1713634724997,-1.204062516105,-0.7462921996877));
#25273=CARTESIAN_POINT('Ctrl Pts',(-0.9185704929214,-0.7970948701029,-0.8031671996877));
#25274=CARTESIAN_POINT('Ctrl Pts',(-1.216195700701,0.,-0.8600421996877));
#25275=CARTESIAN_POINT('Ctrl Pts',(-0.9185704929214,0.7970948701029,-0.9169171996877));
#25276=CARTESIAN_POINT('Ctrl Pts',(-0.1713634724997,1.204062516105,-0.9737921996877));
#25277=CARTESIAN_POINT('Ctrl Pts',(0.6597150647482,1.02171816845,-1.030667199688));
#25278=CARTESIAN_POINT('Ctrl Pts',(1.167905052019,0.3393077836576,-1.087542199688));
#25279=CARTESIAN_POINT('Ctrl Pts',(1.104479823299,-0.5091721726955,-1.144417199688));
#25280=CARTESIAN_POINT('Ctrl Pts',(0.5004819949382,-1.108444747226,-1.201292199688));
#25281=CARTESIAN_POINT('Ctrl Pts',(-0.348469933747,-1.165204139133,-1.258167199688));
#25282=CARTESIAN_POINT('Ctrl Pts',(-1.026867975908,-0.6516702524068,-1.315042199688));
#25283=CARTESIAN_POINT('Ctrl Pts',(-1.202679571961,0.180814804896,-1.371917199688));
#25284=CARTESIAN_POINT('Ctrl Pts',(-0.7898556864549,0.9248023542725,-1.428792199688));
#25285=CARTESIAN_POINT('Ctrl Pts',(0.009550993186476,1.216158607898,-1.485667199688));
#25286=CARTESIAN_POINT('Ctrl Pts',(0.8042879589087,0.9122802996697,-1.542542199688));
#25287=CARTESIAN_POINT('Ctrl Pts',(1.205358893105,0.161907415107,-1.599417199688));
#25288=CARTESIAN_POINT('Ctrl Pts',(1.016551442463,-0.6677408946503,-1.656292199688));
#25289=CARTESIAN_POINT('Ctrl Pts',(0.329952574922,-1.170452920957,-1.713167199688));
#25290=CARTESIAN_POINT('Ctrl Pts',(-0.2348081643589,-1.123983684464,-1.751083866354));
#25291=CARTESIAN_POINT('Ctrl Pts',(-0.4755900604755,-1.010680324589,-1.770042199688));
#25292=CARTESIAN_POINT('Ctrl Pts',(-0.4755900604755,1.010680324589,0.0200421996877));
#25293=CARTESIAN_POINT('Ctrl Pts',(-0.2348081643589,1.123983684464,0.001083866354369));
#25294=CARTESIAN_POINT('Ctrl Pts',(0.329952574922,1.170452920957,-0.0368328003123));
#25295=CARTESIAN_POINT('Ctrl Pts',(1.016551442463,0.6677408946503,-0.0937078003123));
#25296=CARTESIAN_POINT('Ctrl Pts',(1.205358893105,-0.1619074151071,-0.1505828003123));
#25297=CARTESIAN_POINT('Ctrl Pts',(0.8042879589087,-0.9122802996697,-0.2074578003123));
#25298=CARTESIAN_POINT('Ctrl Pts',(0.009550993186476,-1.216158607898,-0.2643328003123));
#25299=CARTESIAN_POINT('Ctrl Pts',(-0.7898556864549,-0.9248023542725,-0.3212078003123));
#25300=CARTESIAN_POINT('Ctrl Pts',(-1.202679571961,-0.180814804896,-0.3780828003123));
#25301=CARTESIAN_POINT('Ctrl Pts',(-1.026867975908,0.6516702524068,-0.4349578003123));
#25302=CARTESIAN_POINT('Ctrl Pts',(-0.348469933747,1.165204139133,-0.4918328003123));
#25303=CARTESIAN_POINT('Ctrl Pts',(0.5004819949382,1.108444747226,-0.5487078003123));
#25304=CARTESIAN_POINT('Ctrl Pts',(1.104479823299,0.5091721726955,-0.6055828003123));
#25305=CARTESIAN_POINT('Ctrl Pts',(1.167905052019,-0.3393077836576,-0.6624578003123));
#25306=CARTESIAN_POINT('Ctrl Pts',(0.6597150647482,-1.02171816845,-0.7193328003123));
#25307=CARTESIAN_POINT('Ctrl Pts',(-0.1713634724997,-1.204062516105,-0.7762078003123));
#25308=CARTESIAN_POINT('Ctrl Pts',(-0.9185704929214,-0.7970948701029,-0.8330828003123));
#25309=CARTESIAN_POINT('Ctrl Pts',(-1.216195700701,0.,-0.8899578003123));
#25310=CARTESIAN_POINT('Ctrl Pts',(-0.9185704929214,0.7970948701029,-0.9468328003123));
#25311=CARTESIAN_POINT('Ctrl Pts',(-0.1713634724997,1.204062516105,-1.003707800312));
#25312=CARTESIAN_POINT('Ctrl Pts',(0.6597150647482,1.02171816845,-1.060582800312));
#25313=CARTESIAN_POINT('Ctrl Pts',(1.167905052019,0.3393077836576,-1.117457800312));
#25314=CARTESIAN_POINT('Ctrl Pts',(1.104479823299,-0.5091721726955,-1.174332800312));
#25315=CARTESIAN_POINT('Ctrl Pts',(0.5004819949382,-1.108444747226,-1.231207800312));
#25316=CARTESIAN_POINT('Ctrl Pts',(-0.348469933747,-1.165204139133,-1.288082800312));
#25317=CARTESIAN_POINT('Ctrl Pts',(-1.026867975908,-0.6516702524068,-1.344957800312));
#25318=CARTESIAN_POINT('Ctrl Pts',(-1.202679571961,0.180814804896,-1.401832800312));
#25319=CARTESIAN_POINT('Ctrl Pts',(-0.7898556864549,0.9248023542725,-1.458707800312));
#25320=CARTESIAN_POINT('Ctrl Pts',(0.009550993186476,1.216158607898,-1.515582800312));
#25321=CARTESIAN_POINT('Ctrl Pts',(0.8042879589087,0.9122802996697,-1.572457800312));
#25322=CARTESIAN_POINT('Ctrl Pts',(1.205358893105,0.161907415107,-1.629332800312));
#25323=CARTESIAN_POINT('Ctrl Pts',(1.016551442463,-0.6677408946503,-1.686207800312));
#25324=CARTESIAN_POINT('Ctrl Pts',(0.329952574922,-1.170452920957,-1.743082800312));
#25325=CARTESIAN_POINT('Ctrl Pts',(-0.2348081643589,-1.123983684464,-1.780999466979));
#25326=CARTESIAN_POINT('Ctrl Pts',(-0.4755900604755,-1.010680324589,-1.799957800312));
#25327=CARTESIAN_POINT('Ctrl Pts',(-0.4755900604755,1.010680324589,-0.009873400936894));
#25328=CARTESIAN_POINT('Ctrl Pts',(-0.2348081643589,1.123983684464,-0.02883173427023));
#25329=CARTESIAN_POINT('Ctrl Pts',(0.329952574922,1.170452920957,-0.06674840093689));
#25330=CARTESIAN_POINT('Ctrl Pts',(1.016551442463,0.6677408946503,-0.1236234009369));
#25331=CARTESIAN_POINT('Ctrl Pts',(1.205358893105,-0.1619074151071,-0.1804984009369));
#25332=CARTESIAN_POINT('Ctrl Pts',(0.8042879589087,-0.9122802996697,-0.2373734009369));
#25333=CARTESIAN_POINT('Ctrl Pts',(0.009550993186476,-1.216158607898,-0.2942484009369));
#25334=CARTESIAN_POINT('Ctrl Pts',(-0.7898556864549,-0.9248023542725,-0.3511234009369));
#25335=CARTESIAN_POINT('Ctrl Pts',(-1.202679571961,-0.180814804896,-0.4079984009369));
#25336=CARTESIAN_POINT('Ctrl Pts',(-1.026867975908,0.6516702524068,-0.4648734009369));
#25337=CARTESIAN_POINT('Ctrl Pts',(-0.348469933747,1.165204139133,-0.5217484009369));
#25338=CARTESIAN_POINT('Ctrl Pts',(0.5004819949382,1.108444747226,-0.5786234009369));
#25339=CARTESIAN_POINT('Ctrl Pts',(1.104479823299,0.5091721726955,-0.6354984009369));
#25340=CARTESIAN_POINT('Ctrl Pts',(1.167905052019,-0.3393077836576,-0.6923734009369));
#25341=CARTESIAN_POINT('Ctrl Pts',(0.6597150647482,-1.02171816845,-0.7492484009369));
#25342=CARTESIAN_POINT('Ctrl Pts',(-0.1713634724997,-1.204062516105,-0.8061234009369));
#25343=CARTESIAN_POINT('Ctrl Pts',(-0.9185704929214,-0.7970948701029,-0.8629984009369));
#25344=CARTESIAN_POINT('Ctrl Pts',(-1.216195700701,0.,-0.9198734009369));
#25345=CARTESIAN_POINT('Ctrl Pts',(-0.9185704929214,0.7970948701029,-0.9767484009369));
#25346=CARTESIAN_POINT('Ctrl Pts',(-0.1713634724997,1.204062516105,-1.033623400937));
#25347=CARTESIAN_POINT('Ctrl Pts',(0.6597150647482,1.02171816845,-1.090498400937));
#25348=CARTESIAN_POINT('Ctrl Pts',(1.167905052019,0.3393077836576,-1.147373400937));
#25349=CARTESIAN_POINT('Ctrl Pts',(1.104479823299,-0.5091721726955,-1.204248400937));
#25350=CARTESIAN_POINT('Ctrl Pts',(0.5004819949382,-1.108444747226,-1.261123400937));
#25351=CARTESIAN_POINT('Ctrl Pts',(-0.348469933747,-1.165204139133,-1.317998400937));
#25352=CARTESIAN_POINT('Ctrl Pts',(-1.026867975908,-0.6516702524068,-1.374873400937));
#25353=CARTESIAN_POINT('Ctrl Pts',(-1.202679571961,0.180814804896,-1.431748400937));
#25354=CARTESIAN_POINT('Ctrl Pts',(-0.7898556864549,0.9248023542725,-1.488623400937));
#25355=CARTESIAN_POINT('Ctrl Pts',(0.009550993186476,1.216158607898,-1.545498400937));
#25356=CARTESIAN_POINT('Ctrl Pts',(0.8042879589087,0.9122802996697,-1.602373400937));
#25357=CARTESIAN_POINT('Ctrl Pts',(1.205358893105,0.161907415107,-1.659248400937));
#25358=CARTESIAN_POINT('Ctrl Pts',(1.016551442463,-0.6677408946503,-1.716123400937));
#25359=CARTESIAN_POINT('Ctrl Pts',(0.329952574922,-1.170452920957,-1.772998400937));
#25360=CARTESIAN_POINT('Ctrl Pts',(-0.2348081643589,-1.123983684464,-1.810915067604));
#25361=CARTESIAN_POINT('Ctrl Pts',(-0.4755900604755,-1.010680324589,-1.829873400937));
#25362=CARTESIAN_POINT('',(-2.15930259232053E-7,-1.11698671802919,-1.72115688661164));
#25363=CARTESIAN_POINT('Ctrl Pts',(0.740620592381851,0.835100532381467,
-0.0289497923354185));
#25364=CARTESIAN_POINT('Ctrl Pts',(0.796513037593552,0.78575378038458,-0.0342379290094453));
#25365=CARTESIAN_POINT('Ctrl Pts',(0.847573706129219,0.730904938153316,
-0.0395198235207524));
#25366=CARTESIAN_POINT('Ctrl Pts',(0.937932038832867,0.611387739176731,
-0.0501654329640508));
#25367=CARTESIAN_POINT('Ctrl Pts',(0.976471692706948,0.547333781599408,
-0.0554686789503681));
#25368=CARTESIAN_POINT('Ctrl Pts',(1.07054282678602,0.347984998632784,-0.0712031170738671));
#25369=CARTESIAN_POINT('Ctrl Pts',(1.10692249141229,0.203705684354229,-0.0816458765147045));
#25370=CARTESIAN_POINT('Ctrl Pts',(1.11904805235499,-0.0154853388500362,
-0.0972795741575819));
#25371=CARTESIAN_POINT('Ctrl Pts',(1.11588709227651,-0.0896747963869567,
-0.102518788484517));
#25372=CARTESIAN_POINT('Ctrl Pts',(1.08408659534245,-0.304356884899151,
-0.117921494634144));
#25373=CARTESIAN_POINT('Ctrl Pts',(1.03491689765162,-0.44140768856942,-0.128213717020561));
#25374=CARTESIAN_POINT('Ctrl Pts',(0.922288204707351,-0.633839472617977,
-0.144171751854915));
#25375=CARTESIAN_POINT('Ctrl Pts',(0.874557139837676,-0.698734383013323,
-0.149887101737748));
#25376=CARTESIAN_POINT('Ctrl Pts',(0.783538064083952,-0.797877565125105,
-0.15940176580863));
#25377=CARTESIAN_POINT('Ctrl Pts',(0.743769537021436,-0.835216308994231,
-0.16320369762073));
#25378=CARTESIAN_POINT('Ctrl Pts',(0.609333310871143,-0.943213119675615,
-0.175413924763073));
#25379=CARTESIAN_POINT('Ctrl Pts',(0.505701125475829,-1.00190544590687,
-0.183912879967629));
#25380=CARTESIAN_POINT('Ctrl Pts',(0.338835264532409,-1.06519787069243,
-0.196754094088973));
#25381=CARTESIAN_POINT('Ctrl Pts',(0.280161418331052,-1.08225571508646,
-0.201126888360145));
#25382=CARTESIAN_POINT('Ctrl Pts',(0.166767234429943,-1.1054758958236,-0.209363530411052));
#25383=CARTESIAN_POINT('Ctrl Pts',(0.112216529106593,-1.11255230532458,
-0.213229703934488));
#25384=CARTESIAN_POINT('Ctrl Pts',(0.0155582567028527,-1.1176927898296,
-0.219985145048376));
#25385=CARTESIAN_POINT('Ctrl Pts',(-0.0261352680459435,-1.11746162510164,
-0.222900761849483));
#25386=CARTESIAN_POINT('Ctrl Pts',(-0.177573634087521,-1.10788343875008,
-0.233664111859182));
#25387=CARTESIAN_POINT('Ctrl Pts',(-0.286247895212034,-1.08436597991008,
-0.24165713859263));
#25388=CARTESIAN_POINT('Ctrl Pts',(-0.450861460083075,-1.02313527330091,
-0.254340207177392));
#25389=CARTESIAN_POINT('Ctrl Pts',(-0.51049221102398,-0.994918085478592,
-0.259067571762949));
#25390=CARTESIAN_POINT('Ctrl Pts',(-0.611962301082644,-0.935521283217812,
-0.26739773754997));
#25391=CARTESIAN_POINT('Ctrl Pts',(-0.654909200479519,-0.906212039991709,
-0.271007441322454));
#25392=CARTESIAN_POINT('Ctrl Pts',(-0.720486485784318,-0.854171918393593,
-0.27681705109175));
#25393=CARTESIAN_POINT('Ctrl Pts',(-0.744409975919507,-0.833384416568187,
-0.279028283477932));
#25394=CARTESIAN_POINT('Ctrl Pts',(-0.797415126573322,-0.78306490151451,
-0.28419168642247));
#25395=CARTESIAN_POINT('Ctrl Pts',(-0.825746397084472,-0.752916952833451,
-0.287145498045552));
#25396=CARTESIAN_POINT('Ctrl Pts',(-0.906307501998842,-0.657079240397088,
-0.296161096764032));
#25397=CARTESIAN_POINT('Ctrl Pts',(-0.95309135752645,-0.586758490236072,
-0.302291570980455));
#25398=CARTESIAN_POINT('Ctrl Pts',(-1.01396989453065,-0.469115707118331,
-0.31187257893077));
#25399=CARTESIAN_POINT('Ctrl Pts',(-1.03355083743677,-0.424544687971698,
-0.315366605579132));
#25400=CARTESIAN_POINT('Ctrl Pts',(-1.0611465833909,-0.348799117113008,
-0.321085587964228));
#25401=CARTESIAN_POINT('Ctrl Pts',(-1.07083161179222,-0.318223021558651,
-0.323337980172478));
#25402=CARTESIAN_POINT('Ctrl Pts',(-1.09122343952725,-0.242564219693662,
-0.328779074897701));
#25403=CARTESIAN_POINT('Ctrl Pts',(-1.10048332412199,-0.197016748616113,
-0.331949207493977));
#25404=CARTESIAN_POINT('Ctrl Pts',(-1.110725571907,-0.121555091669843,-0.33727414443887));
#25405=CARTESIAN_POINT('Ctrl Pts',(-1.11349198406646,-0.0920543665529969,
-0.339368823000687));
#25406=CARTESIAN_POINT('Ctrl Pts',(-1.12012845133126,0.0327543760934407,
-0.348289261762931));
#25407=CARTESIAN_POINT('Ctrl Pts',(-1.1127994297416,0.128668562976753,-0.355293552486537));
#25408=CARTESIAN_POINT('Ctrl Pts',(-1.08655137401299,0.257792290211094,
-0.364878848852288));
#25409=CARTESIAN_POINT('Ctrl Pts',(-1.07759883804518,0.293116723581185,
-0.367517256533893));
#25410=CARTESIAN_POINT('Ctrl Pts',(-1.05805452229903,0.357178531877852,
-0.372327604097815));
#25411=CARTESIAN_POINT('Ctrl Pts',(-1.04795109721,0.386073149841699,-0.374507185489659));
#25412=CARTESIAN_POINT('Ctrl Pts',(-1.0175200545425,0.462895426666191,-0.380327548221617));
#25413=CARTESIAN_POINT('Ctrl Pts',(-0.994996800918248,0.509943087123585,
-0.383888402299322));
#25414=CARTESIAN_POINT('Ctrl Pts',(-0.957808633509514,0.575132092030043,
-0.389050136992139));
#25415=CARTESIAN_POINT('Ctrl Pts',(-0.945775473484694,0.594746751850922,
-0.390639417979559));
#25416=CARTESIAN_POINT('Ctrl Pts',(-0.918972123963961,0.635414431956283,
-0.394046456069751));
#25417=CARTESIAN_POINT('Ctrl Pts',(-0.904102140831624,0.656307674801286,
-0.395860186837375));
#25418=CARTESIAN_POINT('Ctrl Pts',(-0.864419170168452,0.708122030191015,
-0.400520097901616));
#25419=CARTESIAN_POINT('Ctrl Pts',(-0.838616852196583,0.738279114415411,
-0.403388573069705));
#25420=CARTESIAN_POINT('Ctrl Pts',(-0.766615948283921,0.81395937577478,
-0.410996633990166));
#25421=CARTESIAN_POINT('Ctrl Pts',(-0.717859140651418,0.857083532914942,
-0.415768526697806));
#25422=CARTESIAN_POINT('Ctrl Pts',(-0.642324639692028,0.913254617456444,
-0.422620821016675));
#25423=CARTESIAN_POINT('Ctrl Pts',(-0.618136110596605,0.929839550100437,
-0.424743759666412));
#25424=CARTESIAN_POINT('Ctrl Pts',(-0.571547575405974,0.959208007243405,
-0.428696605919632));
#25425=CARTESIAN_POINT('Ctrl Pts',(-0.549280650991451,0.972210891789697,
-0.430531230944641));
#25426=CARTESIAN_POINT('Ctrl Pts',(-0.501644505646967,0.99788130458919,
-0.434339845932671));
#25427=CARTESIAN_POINT('Ctrl Pts',(-0.476187622254524,1.01038588750128,
-0.436305190782293));
#25428=CARTESIAN_POINT('Ctrl Pts',(-0.406811798847217,1.04122235706574,
-0.441518550975112));
#25429=CARTESIAN_POINT('Ctrl Pts',(-0.362069063403444,1.0577586346472,-0.44474463696738));
#25430=CARTESIAN_POINT('Ctrl Pts',(-0.294776566884945,1.0776203242097,-0.449630402816247));
#25431=CARTESIAN_POINT('Ctrl Pts',(-0.272987925983213,1.08330968819,-0.451216618470544));
#25432=CARTESIAN_POINT('Ctrl Pts',(-0.223057022975575,1.09470834215462,
-0.454860393124103));
#25433=CARTESIAN_POINT('Ctrl Pts',(-0.194821349741637,1.09999085887876,
-0.456927201131256));
#25434=CARTESIAN_POINT('Ctrl Pts',(-0.0931781543481861,1.11496777184189,
-0.46438190893784));
#25435=CARTESIAN_POINT('Ctrl Pts',(-0.0188366922385358,1.11845687542912,
-0.469862803532103));
#25436=CARTESIAN_POINT('Ctrl Pts',(0.0943035999676855,1.11281577179903,
-0.478149447988595));
#25437=CARTESIAN_POINT('Ctrl Pts',(0.133409495312111,1.10884394569154,-0.481003024371444));
#25438=CARTESIAN_POINT('Ctrl Pts',(0.193849994240431,1.09953214938452,-0.485381356799469));
#25439=CARTESIAN_POINT('Ctrl Pts',(0.215403711020003,1.09557212007282,-0.486936282678626));
#25440=CARTESIAN_POINT('Ctrl Pts',(0.265430644698985,1.08486824357358,-0.490527020210655));
#25441=CARTESIAN_POINT('Ctrl Pts',(0.293797943223853,1.07763668945462,-0.492543598331562));
#25442=CARTESIAN_POINT('Ctrl Pts',(0.362926550960593,1.05707599620361,-0.497475075268599));
#25443=CARTESIAN_POINT('Ctrl Pts',(0.403299989728691,1.04247899272945,-0.500375401266443));
#25444=CARTESIAN_POINT('Ctrl Pts',(0.46237447012572,1.01703013432772,-0.50482221989358));
#25445=CARTESIAN_POINT('Ctrl Pts',(0.481763037883008,1.00797464499185,-0.50631873474349));
#25446=CARTESIAN_POINT('Ctrl Pts',(0.520940399942042,0.988240293911177,
-0.509423131274058));
#25447=CARTESIAN_POINT('Ctrl Pts',(0.540687957619948,0.977509607233441,
-0.511030894978789));
#25448=CARTESIAN_POINT('Ctrl Pts',(0.616055873729977,0.933519250921083,
-0.517328719525424));
#25449=CARTESIAN_POINT('Ctrl Pts',(0.669139138037821,0.895916512002932,
-0.52211865957522));
#25450=CARTESIAN_POINT('Ctrl Pts',(0.746534674753097,0.830544427725234,
-0.529584863943384));
#25451=CARTESIAN_POINT('Ctrl Pts',(0.773301769277264,0.805638507562068,
-0.532271589876185));
#25452=CARTESIAN_POINT('Ctrl Pts',(0.817732022702937,0.760144206774835,
-0.53690078853131));
#25453=CARTESIAN_POINT('Ctrl Pts',(0.835964059413658,0.740099905122851,
-0.538856517829673));
#25454=CARTESIAN_POINT('Ctrl Pts',(0.865813983208456,0.704835474509298,
-0.542151255585573));
#25455=CARTESIAN_POINT('Ctrl Pts',(0.877802803978707,0.689926363970315,
-0.543502813257041));
#25456=CARTESIAN_POINT('Ctrl Pts',(0.916735854119235,0.638912579792595,
-0.547986394647336));
#25457=CARTESIAN_POINT('Ctrl Pts',(0.941926713330494,0.601468666821261,
-0.5510414088158));
#25458=CARTESIAN_POINT('Ctrl Pts',(0.984605045342404,0.528772744682739,
-0.55677181495935));
#25459=CARTESIAN_POINT('Ctrl Pts',(1.00268914759296,0.493821064837415,-0.559449931570309));
#25460=CARTESIAN_POINT('Ctrl Pts',(1.02643518423323,0.440924121022262,-0.563510354774685));
#25461=CARTESIAN_POINT('Ctrl Pts',(1.03360688090292,0.423766066163042,-0.564827083396981));
#25462=CARTESIAN_POINT('Ctrl Pts',(1.04955405200274,0.382686262624412,-0.567976954224737));
#25463=CARTESIAN_POINT('Ctrl Pts',(1.05793864438942,0.358615900422101,-0.569820553652917));
#25464=CARTESIAN_POINT('Ctrl Pts',(1.08604334092431,0.268009456343316,-0.576741532772031));
#25465=CARTESIAN_POINT('Ctrl Pts',(1.10038794189382,0.199794477894304,-0.581916754293019));
#25466=CARTESIAN_POINT('Ctrl Pts',(1.11147624895963,0.105037384972042,-0.58893801844341));
#25467=CARTESIAN_POINT('Ctrl Pts',(1.11361798302232,0.0790931367382169,
-0.590843253297796));
#25468=CARTESIAN_POINT('Ctrl Pts',(1.11591391090523,0.031554393716092,-0.594293921700568));
#25469=CARTESIAN_POINT('Ctrl Pts',(1.11634499309645,0.00996997580722143,
-0.595845493874729));
#25470=CARTESIAN_POINT('Ctrl Pts',(1.11601678473683,-0.0289296677419575,
-0.598609699396986));
#25471=CARTESIAN_POINT('Ctrl Pts',(1.11547563051356,-0.046248246002881,
-0.599828705409154));
#25472=CARTESIAN_POINT('Ctrl Pts',(1.11033593676314,-0.141017182893811,
-0.606432256818337));
#25473=CARTESIAN_POINT('Ctrl Pts',(1.09817291136362,-0.218056107844839,
-0.611567396396193));
#25474=CARTESIAN_POINT('Ctrl Pts',(1.07317172150137,-0.310324277526315,
-0.6181942374858));
#25475=CARTESIAN_POINT('Ctrl Pts',(1.06803662014465,-0.327538716249082,
-0.619453491293131));
#25476=CARTESIAN_POINT('Ctrl Pts',(1.05655675853671,-0.362777251585735,
-0.622081615716259));
#25477=CARTESIAN_POINT('Ctrl Pts',(1.05016601531874,-0.380759737117483,
-0.623449716211376));
#25478=CARTESIAN_POINT('Ctrl Pts',(1.02910612085745,-0.43545019073186,-0.627688432807875));
#25479=CARTESIAN_POINT('Ctrl Pts',(1.0129078019094,-0.471564190764137,-0.630597635660525));
#25480=CARTESIAN_POINT('Ctrl Pts',(0.972516933914018,-0.550243442192709,
-0.637142859056502));
#25481=CARTESIAN_POINT('Ctrl Pts',(0.947333095146665,-0.592313600440566,
-0.640787985650376));
#25482=CARTESIAN_POINT('Ctrl Pts',(0.902593264720848,-0.657223094117165,
-0.646586869962779));
#25483=CARTESIAN_POINT('Ctrl Pts',(0.884646895429411,-0.681191198099769,
-0.648770402959629));
#25484=CARTESIAN_POINT('Ctrl Pts',(0.855043330245326,-0.717653674610126,
-0.652146488437597));
#25485=CARTESIAN_POINT('Ctrl Pts',(0.844000257524308,-0.730650131208104,
-0.65336144092369));
#25486=CARTESIAN_POINT('Ctrl Pts',(0.819356492875607,-0.758366983808924,
-0.65597513354726));
#25487=CARTESIAN_POINT('Ctrl Pts',(0.805647187522388,-0.772990003389014,
-0.657367195031824));
#25488=CARTESIAN_POINT('Ctrl Pts',(0.753852694203413,-0.825373614858682,
-0.662434857157094));
#25489=CARTESIAN_POINT('Ctrl Pts',(0.713431303888153,-0.860827044343055,
-0.666028251045876));
#25490=CARTESIAN_POINT('Ctrl Pts',(0.655237067121373,-0.904744358568907,
-0.671000732143755));
#25491=CARTESIAN_POINT('Ctrl Pts',(0.639543591515078,-0.915948263340018,
-0.672323771917992));
#25492=CARTESIAN_POINT('Ctrl Pts',(0.60962513922318,-0.93611487995497,-0.674829781695365));
#25493=CARTESIAN_POINT('Ctrl Pts',(0.595511643540952,-0.945152039884758,
-0.676006410644711));
#25494=CARTESIAN_POINT('Ctrl Pts',(0.565743394377794,-0.963244362873431,
-0.678480318310755));
#25495=CARTESIAN_POINT('Ctrl Pts',(0.550086783152038,-0.972229073801511,
-0.679776386992321));
#25496=CARTESIAN_POINT('Ctrl Pts',(0.468749092850581,-1.01626630305245,
-0.686476857345634));
#25497=CARTESIAN_POINT('Ctrl Pts',(0.399670594426793,-1.04501992354791,
-0.692064172993986));
#25498=CARTESIAN_POINT('Ctrl Pts',(0.303111884063254,-1.07454968136455,
-0.699548089161246));
#25499=CARTESIAN_POINT('Ctrl Pts',(0.277464427442118,-1.08142410479284,
-0.701505893230627));
#25500=CARTESIAN_POINT('Ctrl Pts',(0.23124017549895,-1.09210618607379,-0.704968192290077));
#25501=CARTESIAN_POINT('Ctrl Pts',(0.210739027718316,-1.09625570016186,
-0.706480952610665));
#25502=CARTESIAN_POINT('Ctrl Pts',(0.175084973374962,-1.10245927389464,
-0.709066607154982));
#25503=CARTESIAN_POINT('Ctrl Pts',(0.159976788452227,-1.10477692980497,
-0.71014815638368));
#25504=CARTESIAN_POINT('Ctrl Pts',(0.117068880774548,-1.11047804379366,
-0.713178529878514));
#25505=CARTESIAN_POINT('Ctrl Pts',(0.0891711334790336,-1.11314318565162,
-0.715102267228391));
#25506=CARTESIAN_POINT('Ctrl Pts',(0.0152811507985157,-1.11743175062111,
-0.720142872910414));
#25507=CARTESIAN_POINT('Ctrl Pts',(-0.0308137122952009,-1.11728414138088,
-0.723231670271439));
#25508=CARTESIAN_POINT('Ctrl Pts',(-0.0952192246255691,-1.11300919976543,
-0.72763937450432));
#25509=CARTESIAN_POINT('Ctrl Pts',(-0.113685215640747,-1.11131065463956,
-0.728913865262833));
#25510=CARTESIAN_POINT('Ctrl Pts',(-0.148023356154526,-1.10725480142821,
-0.731318768731457));
#25511=CARTESIAN_POINT('Ctrl Pts',(-0.163868256657507,-1.10502207506357,
-0.732443232159436));
#25512=CARTESIAN_POINT('Ctrl Pts',(-0.196621678780309,-1.0996540002806,
-0.734802925696262));
#25513=CARTESIAN_POINT('Ctrl Pts',(-0.213475544539095,-1.09647587733155,
-0.736035774793721));
#25514=CARTESIAN_POINT('Ctrl Pts',(-0.265221128464893,-1.08544898262041,
-0.739873197203898));
#25515=CARTESIAN_POINT('Ctrl Pts',(-0.299825399606563,-1.07627648889838,
-0.742513719077342));
#25516=CARTESIAN_POINT('Ctrl Pts',(-0.379743256694071,-1.05093994097453,
-0.748743352318556));
#25517=CARTESIAN_POINT('Ctrl Pts',(-0.424645943648842,-1.03345300238751,
-0.752346226165065));
#25518=CARTESIAN_POINT('Ctrl Pts',(-0.487214914516867,-1.00441802980982,
-0.75744306487192));
#25519=CARTESIAN_POINT('Ctrl Pts',(-0.505928609859782,-0.995101362044645,
-0.758977791885026));
#25520=CARTESIAN_POINT('Ctrl Pts',(-0.539953440105651,-0.976982756699067,
-0.761779872162063));
#25521=CARTESIAN_POINT('Ctrl Pts',(-0.555343172350867,-0.968324757444224,
-0.763051856284975));
#25522=CARTESIAN_POINT('Ctrl Pts',(-0.583668790471788,-0.951514077086158,
-0.765397339556922));
#25523=CARTESIAN_POINT('Ctrl Pts',(-0.596656575410486,-0.943449667964898,
-0.766473781057835));
#25524=CARTESIAN_POINT('Ctrl Pts',(-0.639460923839602,-0.915663473653058,
-0.770032511721639));
#25525=CARTESIAN_POINT('Ctrl Pts',(-0.668533444987986,-0.894786599671619,
-0.772469947624589));
#25526=CARTESIAN_POINT('Ctrl Pts',(-0.72803295391035,-0.847603619460765,
-0.777616303612912));
#25527=CARTESIAN_POINT('Ctrl Pts',(-0.758179997893041,-0.820945642382338,
-0.780321629381393));
#25528=CARTESIAN_POINT('Ctrl Pts',(-0.799468538679245,-0.780171380634711,
-0.784291725795911));
#25529=CARTESIAN_POINT('Ctrl Pts',(-0.811856990307968,-0.767323281669991,
-0.785521109365758));
#25530=CARTESIAN_POINT('Ctrl Pts',(-0.834363157369079,-0.742790458236818,
-0.787841049600906));
#25531=CARTESIAN_POINT('Ctrl Pts',(-0.844549838235625,-0.731194694447102,
-0.788927233214396));
#25532=CARTESIAN_POINT('Ctrl Pts',(-0.865180088529773,-0.706655790853523,
-0.791209916824488));
#25533=CARTESIAN_POINT('Ctrl Pts',(-0.875559603626039,-0.693711840905156,
-0.792404513977711));
#25534=CARTESIAN_POINT('Ctrl Pts',(-0.907300753515491,-0.652220064845121,
-0.796199979080816));
#25535=CARTESIAN_POINT('Ctrl Pts',(-0.927568629724395,-0.622842741494524,
-0.798838788211285));
#25536=CARTESIAN_POINT('Ctrl Pts',(-0.970743721155919,-0.55337615200648,
-0.804929873546265));
#25537=CARTESIAN_POINT('Ctrl Pts',(-0.992675550999678,-0.512673074309552,
-0.808393283270505));
#25538=CARTESIAN_POINT('Ctrl Pts',(-1.02358913443108,-0.445901531677113,
-0.813837743434644));
#25539=CARTESIAN_POINT('Ctrl Pts',(-1.03421911519682,-0.420583836526569,
-0.815850913095372));
#25540=CARTESIAN_POINT('Ctrl Pts',(-1.04914064218594,-0.381127643436842,
-0.818895300375298));
#25541=CARTESIAN_POINT('Ctrl Pts',(-1.05408962214885,-0.367235793244649,
-0.819949856985987));
#25542=CARTESIAN_POINT('Ctrl Pts',(-1.06457803559718,-0.335889589960992,
-0.82228820497776));
#25543=CARTESIAN_POINT('Ctrl Pts',(-1.06997115590549,-0.318385421864146,
-0.823566603718397));
#25544=CARTESIAN_POINT('Ctrl Pts',(-1.08406985225794,-0.26837260345258,
-0.827160118541158));
#25545=CARTESIAN_POINT('Ctrl Pts',(-1.09176652687607,-0.235575068707072,
-0.829446643500241));
#25546=CARTESIAN_POINT('Ctrl Pts',(-1.10501995603339,-0.164990729751102,
-0.834309246183183));
#25547=CARTESIAN_POINT('Ctrl Pts',(-1.11015166295162,-0.1271245486515,-0.836883249233791));
#25548=CARTESIAN_POINT('Ctrl Pts',(-1.11475710446898,-0.0714110531937625,
-0.840713226297503));
#25549=CARTESIAN_POINT('Ctrl Pts',(-1.11578889944405,-0.0536954246865552,
-0.841937373023348));
#25550=CARTESIAN_POINT('Ctrl Pts',(-1.11689520847532,-0.0207016552272614,
-0.844240747418634));
#25551=CARTESIAN_POINT('Ctrl Pts',(-1.1170830270095,-0.00542492262766989,
-0.845316790009298));
#25552=CARTESIAN_POINT('Ctrl Pts',(-1.11679315931087,0.0259477352854286,
-0.847553090895658));
#25553=CARTESIAN_POINT('Ctrl Pts',(-1.11628279693837,0.0420138989074261,
-0.848711802297192));
#25554=CARTESIAN_POINT('Ctrl Pts',(-1.11350619398124,0.093428780111666,
-0.852457326341894));
#25555=CARTESIAN_POINT('Ctrl Pts',(-1.1098659867498,0.128697038343365,-0.855083646008531));
#25556=CARTESIAN_POINT('Ctrl Pts',(-1.09788947947481,0.207695338285677,
-0.861044323243453));
#25557=CARTESIAN_POINT('Ctrl Pts',(-1.08858835282085,0.251284036045455,
-0.864387894854055));
#25558=CARTESIAN_POINT('Ctrl Pts',(-1.07162315027663,0.312878848488355,
-0.86912033721398));
#25559=CARTESIAN_POINT('Ctrl Pts',(-1.06599299429459,0.331452666862934,
-0.870548394892119));
#25560=CARTESIAN_POINT('Ctrl Pts',(-1.05476115668701,0.36537170990575,-0.873150600962024));
#25561=CARTESIAN_POINT('Ctrl Pts',(-1.0492958810119,0.380763467942627,-0.874329224331263));
#25562=CARTESIAN_POINT('Ctrl Pts',(-1.03800209829953,0.410533289165098,
-0.876600004545797));
#25563=CARTESIAN_POINT('Ctrl Pts',(-1.03220529608311,0.424924244767954,
-0.877693579640065));
#25564=CARTESIAN_POINT('Ctrl Pts',(-1.0114859159707,0.473484785214209,-0.881381794545307));
#25565=CARTESIAN_POINT('Ctrl Pts',(-0.995172662031445,0.507068747093084,
-0.88392887766051));
#25566=CARTESIAN_POINT('Ctrl Pts',(-0.945776378317264,0.59713296989077,
-0.89089990504806));
#25567=CARTESIAN_POINT('Ctrl Pts',(-0.90932877506683,0.651764236978487,
-0.895290318042283));
#25568=CARTESIAN_POINT('Ctrl Pts',(-0.85887825736663,0.714279352173068,
-0.900913351112112));
#25569=CARTESIAN_POINT('Ctrl Pts',(-0.84926873031843,0.725694991316666,
-0.901967408221818));
#25570=CARTESIAN_POINT('Ctrl Pts',(-0.828644309581112,0.749175524787077,
-0.904201003827353));
#25571=CARTESIAN_POINT('Ctrl Pts',(-0.817598489920929,0.761185321982524,
-0.905380784671543));
#25572=CARTESIAN_POINT('Ctrl Pts',(-0.793001387353391,0.786747534130122,
-0.907969371515655));
#25573=CARTESIAN_POINT('Ctrl Pts',(-0.779350493374864,0.800201952292473,
-0.90938208413594));
#25574=CARTESIAN_POINT('Ctrl Pts',(-0.734309167703067,0.842336807487848,
-0.9139580448811));
#25575=CARTESIAN_POINT('Ctrl Pts',(-0.70157997556205,0.869583934989602,
-0.917156130140118));
#25576=CARTESIAN_POINT('Ctrl Pts',(-0.639540477712964,0.915572785812997,
-0.922923184444654));
#25577=CARTESIAN_POINT('Ctrl Pts',(-0.610699011937772,0.934962526109273,
-0.925500197814225));
#25578=CARTESIAN_POINT('Ctrl Pts',(-0.567867741709528,0.9610074883144,-0.929146335576841));
#25579=CARTESIAN_POINT('Ctrl Pts',(-0.554536053336679,0.968749290570932,
-0.93025697426775));
#25580=CARTESIAN_POINT('Ctrl Pts',(-0.526474100248925,0.984295490819199,
-0.932542356286181));
#25581=CARTESIAN_POINT('Ctrl Pts',(-0.51171875207078,0.992053651878127,
-0.933715811422599));
#25582=CARTESIAN_POINT('Ctrl Pts',(-0.452990224509344,1.02131160693359,
-0.938293251144693));
#25583=CARTESIAN_POINT('Ctrl Pts',(-0.407765306240264,1.04033046095139,
-0.94161551976887));
#25584=CARTESIAN_POINT('Ctrl Pts',(-0.313037828080522,1.07308588823884,
-0.948410367454849));
#25585=CARTESIAN_POINT('Ctrl Pts',(-0.263433120774754,1.08652867895733,
-0.951883688628962));
#25586=CARTESIAN_POINT('Ctrl Pts',(-0.196979328012632,1.09957757647535,
-0.95661022891241));
#25587=CARTESIAN_POINT('Ctrl Pts',(-0.180765877016589,1.10238007628764,
-0.957769039559126));
#25588=CARTESIAN_POINT('Ctrl Pts',(-0.149645727930048,1.10702287798097,
-0.960012463254124));
#25589=CARTESIAN_POINT('Ctrl Pts',(-0.134770806361007,1.10892162563533,
-0.961093677413286));
#25590=CARTESIAN_POINT('Ctrl Pts',(-0.0820732731622451,1.11453682573504,
-0.964950381477751));
#25591=CARTESIAN_POINT('Ctrl Pts',(-0.0440722367273357,1.11656706895916,
-0.967779000956304));
#25592=CARTESIAN_POINT('Ctrl Pts',(0.0540305524033847,1.11677795949199,
-0.975117906286598));
#25593=CARTESIAN_POINT('Ctrl Pts',(0.114151155725786,1.11203507507255,-0.97965010173671));
#25594=CARTESIAN_POINT('Ctrl Pts',(0.188467982153772,1.100231277558,-0.985115587025778));
#25595=CARTESIAN_POINT('Ctrl Pts',(0.203374403245894,1.09755874827963,-0.986204153414178));
#25596=CARTESIAN_POINT('Ctrl Pts',(0.236063821038359,1.0910256528619,-0.988575982945092));
#25597=CARTESIAN_POINT('Ctrl Pts',(0.253821207080709,1.08703416613913,-0.9898550669114));
#25598=CARTESIAN_POINT('Ctrl Pts',(0.292298236793962,1.07741543574307,-0.992617716620507));
#25599=CARTESIAN_POINT('Ctrl Pts',(0.312978265295055,1.07162275221265,-0.994096826484634));
#25600=CARTESIAN_POINT('Ctrl Pts',(0.380956088887678,1.05049225879604,-0.998970509474916));
#25601=CARTESIAN_POINT('Ctrl Pts',(0.427476292869596,1.03262248510317,-1.00232444355582));
#25602=CARTESIAN_POINT('Ctrl Pts',(0.501777055710514,0.998212465206567,
-1.00791521430462));
#25603=CARTESIAN_POINT('Ctrl Pts',(0.53037224227781,0.983431809674303,-1.01012838908167));
#25604=CARTESIAN_POINT('Ctrl Pts',(0.572130309905694,0.959439684514594,
-1.01350534028038));
#25605=CARTESIAN_POINT('Ctrl Pts',(0.585826681947766,0.951162253494843,
-1.01463753009962));
#25606=CARTESIAN_POINT('Ctrl Pts',(0.612866734630896,0.933981118440412,
-1.0169308333167));
#25607=CARTESIAN_POINT('Ctrl Pts',(0.626186752566185,0.925089263853542,
-1.01809082693388));
#25608=CARTESIAN_POINT('Ctrl Pts',(0.654913887564356,0.904976207517935,
-1.02065482724021));
#25609=CARTESIAN_POINT('Ctrl Pts',(0.670241222410078,0.893628769797773,
-1.02206364946472));
#25610=CARTESIAN_POINT('Ctrl Pts',(0.721352459819767,0.853686784337798,
-1.0268863553142));
#25611=CARTESIAN_POINT('Ctrl Pts',(0.755674530592387,0.823225962826674,
-1.03034125113025));
#25612=CARTESIAN_POINT('Ctrl Pts',(0.807305122531451,0.771469794764212,
-1.03578513225715));
#25613=CARTESIAN_POINT('Ctrl Pts',(0.825889378543328,0.751438631054798,
-1.0378027422642));
#25614=CARTESIAN_POINT('Ctrl Pts',(0.85390525146924,0.718978765547925,-1.04091515493341));
#25615=CARTESIAN_POINT('Ctrl Pts',(0.863838296471794,0.706982031588233,
-1.04203324901225));
#25616=CARTESIAN_POINT('Ctrl Pts',(0.885842337257275,0.679273374591332,
-1.04454926651593));
#25617=CARTESIAN_POINT('Ctrl Pts',(0.897760308848472,0.663437812855681,
-1.04594089912198));
#25618=CARTESIAN_POINT('Ctrl Pts',(0.940529854645035,0.603426561316026,
-1.05107021135596));
#25619=CARTESIAN_POINT('Ctrl Pts',(0.968711315983671,0.557325272017379,
-1.05472760903283));
#25620=CARTESIAN_POINT('Ctrl Pts',(1.01459496700254,0.468543805603866,-1.06153069346646));
#25621=CARTESIAN_POINT('Ctrl Pts',(1.03322667884151,0.426336847146873,-1.06467456745001));
#25622=CARTESIAN_POINT('Ctrl Pts',(1.05530418605042,0.366318476561309,-1.0691470158903));
#25623=CARTESIAN_POINT('Ctrl Pts',(1.06107083620922,0.349365124742118,-1.07041052359689));
#25624=CARTESIAN_POINT('Ctrl Pts',(1.07103108937878,0.317492082608692,-1.07279569358009));
#25625=CARTESIAN_POINT('Ctrl Pts',(1.07531873931894,0.302647697696071,-1.07391112223302));
#25626=CARTESIAN_POINT('Ctrl Pts',(1.08372674491576,0.270983199444743,-1.07630039051983));
#25627=CARTESIAN_POINT('Ctrl Pts',(1.08775815030352,0.254178484810853,-1.07757346606282));
#25628=CARTESIAN_POINT('Ctrl Pts',(1.09920672432866,0.200911767862958,-1.08161386784057));
#25629=CARTESIAN_POINT('Ctrl Pts',(1.10516405878848,0.164140051615529,-1.08441071192921));
#25630=CARTESIAN_POINT('Ctrl Pts',(1.11313632206713,0.0925116321749409,
-1.08980025738597));
#25631=CARTESIAN_POINT('Ctrl Pts',(1.11537610008911,0.0576750688941246,
-1.09239483580262));
#25632=CARTESIAN_POINT('Ctrl Pts',(1.11631613577469,0.00624209603872625,
-1.09613888125271));
#25633=CARTESIAN_POINT('Ctrl Pts',(1.11625709653239,-0.0103330825248156,
-1.09733154747569));
#25634=CARTESIAN_POINT('Ctrl Pts',(1.11532332434456,-0.0472093011195721,
-1.09996059458416));
#25635=CARTESIAN_POINT('Ctrl Pts',(1.11426722420198,-0.067507546287733,
-1.10139141621481));
#25636=CARTESIAN_POINT('Ctrl Pts',(1.10868779994077,-0.138334923954908,
-1.10634987545962));
#25637=CARTESIAN_POINT('Ctrl Pts',(1.10133962030423,-0.188658275579207,
-1.10981111643529));
#25638=CARTESIAN_POINT('Ctrl Pts',(1.07959814478269,-0.289583901889022,
-1.1168539594144));
#25639=CARTESIAN_POINT('Ctrl Pts',(1.0649653301397,-0.340143841151782,-1.12043711273469));
#25640=CARTESIAN_POINT('Ctrl Pts',(1.0402539432014,-0.407092951957314,-1.12543456230341));
#25641=CARTESIAN_POINT('Ctrl Pts',(1.03326497189092,-0.424618550531358,
-1.12676739376517));
#25642=CARTESIAN_POINT('Ctrl Pts',(1.01941815551277,-0.45685260978153,-1.12927609230871));
#25643=CARTESIAN_POINT('Ctrl Pts',(1.01269198621406,-0.471581615429797,
-1.1304460690027));
#25644=CARTESIAN_POINT('Ctrl Pts',(0.989163829256111,-0.520147742837765,
-1.13438713833658));
#25645=CARTESIAN_POINT('Ctrl Pts',(0.970928209393707,-0.553228690762047,
-1.13720375937833));
#25646=CARTESIAN_POINT('Ctrl Pts',(0.92597884305988,-0.625749700867753,
-1.14358686699613));
#25647=CARTESIAN_POINT('Ctrl Pts',(0.898294594044716,-0.664591024295858,
-1.14715621217329));
#25648=CARTESIAN_POINT('Ctrl Pts',(0.857069697743663,-0.715361386315322,
-1.15191194064786));
#25649=CARTESIAN_POINT('Ctrl Pts',(0.845526245963272,-0.728914240577514,
-1.1531915450963));
#25650=CARTESIAN_POINT('Ctrl Pts',(0.818491764529182,-0.759191099177518,
-1.15608212328668));
#25651=CARTESIAN_POINT('Ctrl Pts',(0.802800657412089,-0.775739281332732,
-1.15768545012032));
#25652=CARTESIAN_POINT('Ctrl Pts',(0.76681968081965,-0.81148398151618,-1.16122157447671));
#25653=CARTESIAN_POINT('Ctrl Pts',(0.746286813137865,-0.830441180245557,
-1.16314758176595));
#25654=CARTESIAN_POINT('Ctrl Pts',(0.676991009179002,-0.889859141557608,
-1.16941324396116));
#25655=CARTESIAN_POINT('Ctrl Pts',(0.625446039688801,-0.927101619168428,
-1.17371624456519));
#25656=CARTESIAN_POINT('Ctrl Pts',(0.550169183105251,-0.972217481367136,
-1.17981804356229));
#25657=CARTESIAN_POINT('Ctrl Pts',(0.528818209110273,-0.984071076769615,
-1.18153021990509));
#25658=CARTESIAN_POINT('Ctrl Pts',(0.491984019956504,-1.00292332829553,
-1.18447220874538));
#25659=CARTESIAN_POINT('Ctrl Pts',(0.476696605684069,-1.01029998662431,
-1.18568991475916));
#25660=CARTESIAN_POINT('Ctrl Pts',(0.434145987134609,-1.0295958956179,-1.18908007359259));
#25661=CARTESIAN_POINT('Ctrl Pts',(0.406553200265277,-1.04074219244302,
-1.1912802804877));
#25662=CARTESIAN_POINT('Ctrl Pts',(0.333153415825322,-1.0669721778709,-1.1970858745644));
#25663=CARTESIAN_POINT('Ctrl Pts',(0.286674562829502,-1.08019795380544,
-1.20071533118248));
#25664=CARTESIAN_POINT('Ctrl Pts',(0.21977038433892,-1.09468524172238,-1.20574155087924));
#25665=CARTESIAN_POINT('Ctrl Pts',(0.199882874314479,-1.09843535550142,
-1.20720964347452));
#25666=CARTESIAN_POINT('Ctrl Pts',(0.158677184619967,-1.10507314265271,
-1.21020500880998));
#25667=CARTESIAN_POINT('Ctrl Pts',(0.137346315536213,-1.10789183987108,
-1.2117309138464));
#25668=CARTESIAN_POINT('Ctrl Pts',(0.0578253119596095,-1.11612516676388,
-1.21735301767836));
#25669=CARTESIAN_POINT('Ctrl Pts',(-0.0007897928477788,-1.11768935041499,
-1.22136509379683));
#25670=CARTESIAN_POINT('Ctrl Pts',(-0.11387500185164,-1.11198216449286,
-1.22913593826288));
#25671=CARTESIAN_POINT('Ctrl Pts',(-0.168393309681907,-1.10525704406103,
-1.23289715332687));
#25672=CARTESIAN_POINT('Ctrl Pts',(-0.242946202835828,-1.09034635843923,
-1.23824110058869));
#25673=CARTESIAN_POINT('Ctrl Pts',(-0.263661929028808,-1.08557424900894,
-1.23974792877966));
#25674=CARTESIAN_POINT('Ctrl Pts',(-0.302633547942523,-1.07537644070583,
-1.24263828990327));
#25675=CARTESIAN_POINT('Ctrl Pts',(-0.320895999817841,-1.0700772135446,
-1.24401724454367));
#25676=CARTESIAN_POINT('Ctrl Pts',(-0.388834444137772,-1.04837547248558,
-1.24924765976264));
#25677=CARTESIAN_POINT('Ctrl Pts',(-0.437431167749803,-1.02884834375456,
-1.25318179381202));
#25678=CARTESIAN_POINT('Ctrl Pts',(-0.508504613606336,-0.994333314151419,
-1.25903686345293));
#25679=CARTESIAN_POINT('Ctrl Pts',(-0.532158147116165,-0.981778355513795,
-1.26100023317393));
#25680=CARTESIAN_POINT('Ctrl Pts',(-0.574563300398608,-0.957307601219113,
-1.26453681636663));
#25681=CARTESIAN_POINT('Ctrl Pts',(-0.593461718938977,-0.945649094933868,
-1.2661219664867));
#25682=CARTESIAN_POINT('Ctrl Pts',(-0.644375275958978,-0.912151809271095,
-1.27043545555292));
#25683=CARTESIAN_POINT('Ctrl Pts',(-0.675668764426734,-0.889200370193944,
-1.27313514232132));
#25684=CARTESIAN_POINT('Ctrl Pts',(-0.760437520387496,-0.820144561142635,
-1.28069894045784));
#25685=CARTESIAN_POINT('Ctrl Pts',(-0.811055261632599,-0.770478713171644,
-1.28552266871189));
#25686=CARTESIAN_POINT('Ctrl Pts',(-0.874484451983752,-0.695153715383073,
-1.29239831682034));
#25687=CARTESIAN_POINT('Ctrl Pts',(-0.891646638926817,-0.673141212799298,
-1.29436235324845));
#25688=CARTESIAN_POINT('Ctrl Pts',(-0.919703712778341,-0.634150658299314,
-1.29778966744056));
#25689=CARTESIAN_POINT('Ctrl Pts',(-0.931013634384034,-0.617474950131453,
-1.29924029044429));
#25690=CARTESIAN_POINT('Ctrl Pts',(-0.951725734380025,-0.5849959600492,
-1.30204658206248));
#25691=CARTESIAN_POINT('Ctrl Pts',(-0.961201202874254,-0.569253958823924,
-1.30339893752634));
#25692=CARTESIAN_POINT('Ctrl Pts',(-0.994270057819556,-0.511019147880041,
-1.30835525083632));
#25693=CARTESIAN_POINT('Ctrl Pts',(-1.01542620382818,-0.467142941382244,
-1.31200158069852));
#25694=CARTESIAN_POINT('Ctrl Pts',(-1.04266204202624,-0.399818094214572,
-1.31731455804578));
#25695=CARTESIAN_POINT('Ctrl Pts',(-1.05095349258127,-0.37726796591669,
-1.31905021897796));
#25696=CARTESIAN_POINT('Ctrl Pts',(-1.06783378208471,-0.326436173938074,
-1.32288298987987));
#25697=CARTESIAN_POINT('Ctrl Pts',(-1.07605213671493,-0.29802774751781,
-1.32497147091931));
#25698=CARTESIAN_POINT('Ctrl Pts',(-1.09205113087124,-0.233450144132,-1.32963463265107));
#25699=CARTESIAN_POINT('Ctrl Pts',(-1.09920426871889,-0.197116915666788,
-1.33220014807258));
#25700=CARTESIAN_POINT('Ctrl Pts',(-1.11569139976872,-0.0848645490057636,
-1.34004888630328));
#25701=CARTESIAN_POINT('Ctrl Pts',(-1.11920391951796,-0.00806009617995092,
-1.34531246542237));
#25702=CARTESIAN_POINT('Ctrl Pts',(-1.11335269071756,0.0920233385725479,
-1.35241704957437));
#25703=CARTESIAN_POINT('Ctrl Pts',(-1.11119224195733,0.11572547805626,-1.35411777718821));
#25704=CARTESIAN_POINT('Ctrl Pts',(-1.10354318058673,0.177071879490257,
-1.35858901706502));
#25705=CARTESIAN_POINT('Ctrl Pts',(-1.0968474758073,0.214367326080166,-1.3613874522399));
#25706=CARTESIAN_POINT('Ctrl Pts',(-1.07873998266251,0.291897496557865,
-1.36728850096717));
#25707=CARTESIAN_POINT('Ctrl Pts',(-1.06690821471463,0.332037830586118,
-1.3703797243111));
#25708=CARTESIAN_POINT('Ctrl Pts',(-1.04332152760018,0.398232326867899,
-1.3754649079695));
#25709=CARTESIAN_POINT('Ctrl Pts',(-1.03274322803085,0.424698782517065,
-1.37750185784614));
#25710=CARTESIAN_POINT('Ctrl Pts',(-0.995494040347185,0.508618254227233,
-1.38401007855805));
#25711=CARTESIAN_POINT('Ctrl Pts',(-0.964956834095852,0.564390205958779,
-1.38841147648662));
#25712=CARTESIAN_POINT('Ctrl Pts',(-0.892967481706339,0.673298566929881,
-1.39747097352407));
#25713=CARTESIAN_POINT('Ctrl Pts',(-0.850937651780783,0.72610268365452,
-1.4021329463705));
#25714=CARTESIAN_POINT('Ctrl Pts',(-0.785667057548767,0.794283450457149,
-1.40882615327226));
#25715=CARTESIAN_POINT('Ctrl Pts',(-0.766143934832389,0.81322073125236,
-1.41077052091126));
#25716=CARTESIAN_POINT('Ctrl Pts',(-0.720375161308584,0.854369873452665,
-1.41522533430838));
#25717=CARTESIAN_POINT('Ctrl Pts',(-0.693838948060834,0.876001260804895,
-1.41774575192641));
#25718=CARTESIAN_POINT('Ctrl Pts',(-0.633258156945879,0.920815597145715,
-1.42330892229183));
#25719=CARTESIAN_POINT('Ctrl Pts',(-0.59879921827957,0.943411854228772,
-1.4263360361838));
#25720=CARTESIAN_POINT('Ctrl Pts',(-0.533064199397785,0.981527990020711,
-1.43182303736665));
#25721=CARTESIAN_POINT('Ctrl Pts',(-0.50211333730462,0.997600684576518,
-1.43430816934474));
#25722=CARTESIAN_POINT('Ctrl Pts',(-0.43346420760776,1.02934490598123,-1.43965775086329));
#25723=CARTESIAN_POINT('Ctrl Pts',(-0.395507335393598,1.04448215382306,
-1.44251517581157));
#25724=CARTESIAN_POINT('Ctrl Pts',(-0.26711867659718,1.08788950411197,-1.45197329338261));
#25725=CARTESIAN_POINT('Ctrl Pts',(-0.173552851448838,1.1071011125986,-1.45853692012621));
#25726=CARTESIAN_POINT('Ctrl Pts',(-0.0491969920609825,1.11625444550779,
-1.46743850887193));
#25727=CARTESIAN_POINT('Ctrl Pts',(-0.0192027323245962,1.11722754308489,
-1.46959886421849));
#25728=CARTESIAN_POINT('Ctrl Pts',(0.0390259210125597,1.11665977811538,
-1.47384454681893));
#25729=CARTESIAN_POINT('Ctrl Pts',(0.0672398127568702,1.11526531437875,
-1.47592461460744));
#25730=CARTESIAN_POINT('Ctrl Pts',(0.13566487510423,1.1092240533465,-1.48096698326874));
#25731=CARTESIAN_POINT('Ctrl Pts',(0.175770475157463,1.10343054811916,-1.48390680342966));
#25732=CARTESIAN_POINT('Ctrl Pts',(0.267046634661586,1.08517574510875,-1.49058741766001));
#25733=CARTESIAN_POINT('Ctrl Pts',(0.317931688778372,1.07123280478388,-1.49431106263498));
#25734=CARTESIAN_POINT('Ctrl Pts',(0.446961994983713,1.02612044323732,-1.50391787545689));
#25735=CARTESIAN_POINT('Ctrl Pts',(0.523316979042064,0.989605242025754,
-1.50976888528809));
#25736=CARTESIAN_POINT('Ctrl Pts',(0.632908523567412,0.921159089521382,
-1.51888437332726));
#25737=CARTESIAN_POINT('Ctrl Pts',(0.669748303379762,0.894927711381821,
-1.52209312747034));
#25738=CARTESIAN_POINT('Ctrl Pts',(0.730610405353075,0.845580443854341,
-1.52773785069793));
#25739=CARTESIAN_POINT('Ctrl Pts',(0.7552881057523,0.823599046260279,-1.5301467049352));
#25740=CARTESIAN_POINT('Ctrl Pts',(0.817218965948864,0.763098843103266,
-1.53647429966056));
#25741=CARTESIAN_POINT('Ctrl Pts',(0.852662889830548,0.722959726302608,
-1.54034188256599));
#25742=CARTESIAN_POINT('Ctrl Pts',(0.938211054001444,0.610963635981032,
-1.55041907671587));
#25743=CARTESIAN_POINT('Ctrl Pts',(0.983263737595165,0.535174401068512,
-1.55657154136733));
#25744=CARTESIAN_POINT('Ctrl Pts',(1.05355565231594,0.378547858674659,-1.56863732896307));
#25745=CARTESIAN_POINT('Ctrl Pts',(1.07952855842687,0.297931382092672,-1.5745601387804));
#25746=CARTESIAN_POINT('Ctrl Pts',(1.1050362391125,0.169640335255523,-1.58393561109276));
#25747=CARTESIAN_POINT('Ctrl Pts',(1.11111365921164,0.123684939102018,-1.58730302707212));
#25748=CARTESIAN_POINT('Ctrl Pts',(1.11964636245312,-0.00367233478476775,
-1.59655127403001));
#25749=CARTESIAN_POINT('Ctrl Pts',(1.11605101611499,-0.085101664783812,
-1.60233845571577));
#25750=CARTESIAN_POINT('Ctrl Pts',(1.0816505606552,-0.312274176175625,-1.61862620449722));
#25751=CARTESIAN_POINT('Ctrl Pts',(1.03056423362021,-0.45524871230428,-1.62905386459966));
#25752=CARTESIAN_POINT('Ctrl Pts',(0.922586007371914,-0.632513575792815,
-1.64395355031118));
#25753=CARTESIAN_POINT('Ctrl Pts',(0.888040527122837,-0.679871542158833,
-1.64818318901711));
#25754=CARTESIAN_POINT('Ctrl Pts',(0.764236840703511,-0.824202940541874,
-1.66181556537727));
#25755=CARTESIAN_POINT('Ctrl Pts',(0.660519067741824,-0.909040197336868,
-1.67115934543248));
#25756=CARTESIAN_POINT('Ctrl Pts',(0.463560083860833,-1.02011807088014,
-1.68719358718629));
#25757=CARTESIAN_POINT('Ctrl Pts',(0.375334948218811,-1.05637112684073,
-1.69392081615549));
#25758=CARTESIAN_POINT('Ctrl Pts',(0.191017799332561,-1.10461528968122,
-1.70755628210277));
#25759=CARTESIAN_POINT('Ctrl Pts',(0.0954959843605988,-1.1164612562587,
-1.71438524122992));
#25760=CARTESIAN_POINT('Ctrl Pts',(4.85215486032485E-6,-1.11628565924263,
-1.72119948076935));
#25761=CARTESIAN_POINT('',(3.48982020092455E-10,-1.11698717731251,-1.77886751164369));
#25762=CARTESIAN_POINT('',(0.,-1.116987298108,-1.721132486541));
#25763=CARTESIAN_POINT('Ctrl Pts',(-4.51646176117242E-5,1.11628556616826,
-0.028845753490975));
#25764=CARTESIAN_POINT('Ctrl Pts',(0.0945737663334262,1.11646371878452,
-0.0355870386379063));
#25765=CARTESIAN_POINT('Ctrl Pts',(0.189224370129108,1.10483896102052,-0.0423343546232623));
#25766=CARTESIAN_POINT('Ctrl Pts',(0.372906704517377,1.05724696582637,-0.0558777394065449));
#25767=CARTESIAN_POINT('Ctrl Pts',(0.461252181102166,1.02117700224735,-0.062629461743586));
#25768=CARTESIAN_POINT('Ctrl Pts',(0.668471432388766,0.904915646636026,
-0.0795557664982609));
#25769=CARTESIAN_POINT('Ctrl Pts',(0.780383055419209,0.811029500761427,
-0.0897649811840648));
#25770=CARTESIAN_POINT('Ctrl Pts',(0.977352549963107,0.567498199932401,
-0.112102790001303));
#25771=CARTESIAN_POINT('Ctrl Pts',(1.03703915589554,0.43114576827777,-0.122493806927422));
#25772=CARTESIAN_POINT('Ctrl Pts',(1.11066616674449,0.178042375581358,-0.141264319305712));
#25773=CARTESIAN_POINT('Ctrl Pts',(1.1250370353998,0.0352369170927906,-0.151306365748182));
#25774=CARTESIAN_POINT('Ctrl Pts',(1.09418460733438,-0.296790717289766,
-0.175096927046621));
#25775=CARTESIAN_POINT('Ctrl Pts',(1.02997735713433,-0.440477084842064,
-0.186018843166476));
#25776=CARTESIAN_POINT('Ctrl Pts',(0.925588908242817,-0.636392952388509,
-0.201824931705356));
#25777=CARTESIAN_POINT('Ctrl Pts',(0.840538191683154,-0.751460714065254,
-0.211837015280091));
#25778=CARTESIAN_POINT('Ctrl Pts',(0.611182247799738,-0.946513834085736,
-0.233319769585066));
#25779=CARTESIAN_POINT('Ctrl Pts',(0.478234529751117,-1.0191711099922,-0.243900801774971));
#25780=CARTESIAN_POINT('Ctrl Pts',(0.222597234321242,-1.1004636264182,-0.263002748092197));
#25781=CARTESIAN_POINT('Ctrl Pts',(0.0794663775051929,-1.12675755955542,
-0.273170746756787));
#25782=CARTESIAN_POINT('Ctrl Pts',(-0.232981315456763,-1.10176800386665,
-0.295527565272568));
#25783=CARTESIAN_POINT('Ctrl Pts',(-0.377700605109014,-1.06037143957915,
-0.306036970274604));
#25784=CARTESIAN_POINT('Ctrl Pts',(-0.604852724324526,-0.944731736167623,
-0.324194405506215));
#25785=CARTESIAN_POINT('Ctrl Pts',(-0.731331226988448,-0.863974006299954,
-0.33465639462854));
#25786=CARTESIAN_POINT('Ctrl Pts',(-0.943397907937856,-0.613934547621999,
-0.358026630171605));
#25787=CARTESIAN_POINT('Ctrl Pts',(-1.01607631574406,-0.484189787750187,
-0.368412151890716));
#25788=CARTESIAN_POINT('Ctrl Pts',(-1.11857306467121,-0.173002860562976,
-0.391764370126267));
#25789=CARTESIAN_POINT('Ctrl Pts',(-1.12165266273671,-0.0230529286473884,
-0.402222387376179));
#25790=CARTESIAN_POINT('Ctrl Pts',(-1.10179845703878,0.228016486144736,
-0.420164306092339));
#25791=CARTESIAN_POINT('Ctrl Pts',(-1.06324590215937,0.369253565391365,
-0.430395833792596));
#25792=CARTESIAN_POINT('Ctrl Pts',(-0.924464855646202,0.649976757040026,
-0.452728617062329));
#25793=CARTESIAN_POINT('Ctrl Pts',(-0.825915661788618,0.761161572818576,
-0.46310258159148));
#25794=CARTESIAN_POINT('Ctrl Pts',(-0.62621431634986,0.934430304671199,
-0.481930408255844));
#25795=CARTESIAN_POINT('Ctrl Pts',(-0.502214996937546,1.00732385711169,
-0.491992988167886));
#25796=CARTESIAN_POINT('Ctrl Pts',(-0.191201997533733,1.11682300306852,
-0.51551693664123));
#25797=CARTESIAN_POINT('Ctrl Pts',(-0.0349012702549832,1.12007370080308,
-0.526380158581428));
#25798=CARTESIAN_POINT('Ctrl Pts',(0.203851405860733,1.1061171885703,-0.543408695580735));
#25799=CARTESIAN_POINT('Ctrl Pts',(0.341786112597022,1.07261170247852,-0.553349115596787));
#25800=CARTESIAN_POINT('Ctrl Pts',(0.603413551668518,0.95156305246285,-0.573918159961364));
#25801=CARTESIAN_POINT('Ctrl Pts',(0.725113385898939,0.861211673415832,
-0.584504519828558));
#25802=CARTESIAN_POINT('Ctrl Pts',(0.905273423514477,0.663857977873337,
-0.603532452081928));
#25803=CARTESIAN_POINT('Ctrl Pts',(0.989304020610892,0.545163021076612,
-0.613692540952363));
#25804=CARTESIAN_POINT('Ctrl Pts',(1.09791444748826,0.250846118613206,-0.636070285825294));
#25805=CARTESIAN_POINT('Ctrl Pts',(1.12102369397598,0.101931202388124,-0.646591923275123));
#25806=CARTESIAN_POINT('Ctrl Pts',(1.11127472608704,-0.152382998725974,
-0.664720299224974));
#25807=CARTESIAN_POINT('Ctrl Pts',(1.09120934524513,-0.300938815206498,
-0.67517036237632));
#25808=CARTESIAN_POINT('Ctrl Pts',(0.953355092950195,-0.598483057720638,
-0.698547434541527));
#25809=CARTESIAN_POINT('Ctrl Pts',(0.865889506205134,-0.71909663240587,
-0.708951545171134));
#25810=CARTESIAN_POINT('Ctrl Pts',(0.630908211369362,-0.938430669099252,
-0.731860596310233));
#25811=CARTESIAN_POINT('Ctrl Pts',(0.499473987912849,-1.00559671816685,
-0.742165965145054));
#25812=CARTESIAN_POINT('Ctrl Pts',(0.254954649474663,-1.09592824110064,
-0.760737340530769));
#25813=CARTESIAN_POINT('Ctrl Pts',(0.110233508147554,-1.12012616746575,
-0.770990446786831));
#25814=CARTESIAN_POINT('Ctrl Pts',(-0.202625788977264,-1.11169037854405,
-0.793308777819729));
#25815=CARTESIAN_POINT('Ctrl Pts',(-0.344594062564993,-1.06910154094398,
-0.803660097358051));
#25816=CARTESIAN_POINT('Ctrl Pts',(-0.586363065095523,-0.959974916638414,
-0.822550244130425));
#25817=CARTESIAN_POINT('Ctrl Pts',(-0.704733656287598,-0.877644037487908,
-0.832635757158428));
#25818=CARTESIAN_POINT('Ctrl Pts',(-0.924445762809,-0.651144082671884,-0.855147894869199));
#25819=CARTESIAN_POINT('Ctrl Pts',(-0.99587830302718,-0.517818669122217,
-0.865692152173815));
#25820=CARTESIAN_POINT('Ctrl Pts',(-1.08982166380632,-0.277939862987315,
-0.884035045773487));
#25821=CARTESIAN_POINT('Ctrl Pts',(-1.1169872981078,-0.139044412854726,
-0.89394629670385));
#25822=CARTESIAN_POINT('Ctrl Pts',(-1.1169872981078,0.139044412854725,-0.91378873021515));
#25823=CARTESIAN_POINT('Ctrl Pts',(-1.08982166380632,0.277939862987314,
-0.9236999811454));
#25824=CARTESIAN_POINT('Ctrl Pts',(-0.995878303027182,0.517818669122212,
-0.942042874744956));
#25825=CARTESIAN_POINT('Ctrl Pts',(-0.924445762809003,0.651144082671879,
-0.952587132049651));
#25826=CARTESIAN_POINT('Ctrl Pts',(-0.704733656287602,0.877644037487905,
-0.975099269760432));
#25827=CARTESIAN_POINT('Ctrl Pts',(-0.586363065095528,0.959974916638411,
-0.985184782788548));
#25828=CARTESIAN_POINT('Ctrl Pts',(-0.344594062565002,1.06910154094397,
-1.00407492956102));
#25829=CARTESIAN_POINT('Ctrl Pts',(-0.202625788977273,1.11169037854405,
-1.01442624909947));
#25830=CARTESIAN_POINT('Ctrl Pts',(0.110233508147546,1.12012616746575,-1.0367445801323));
#25831=CARTESIAN_POINT('Ctrl Pts',(0.254954649474654,1.09592824110065,-1.04699768638824));
#25832=CARTESIAN_POINT('Ctrl Pts',(0.499473987912827,1.00559671816686,-1.06556906177382));
#25833=CARTESIAN_POINT('Ctrl Pts',(0.63090821136934,0.938430669099267,-1.07587443060856));
#25834=CARTESIAN_POINT('Ctrl Pts',(0.865889506205115,0.719096632405891,
-1.0987834817475));
#25835=CARTESIAN_POINT('Ctrl Pts',(0.953355092950176,0.598483057720668,
-1.10918759237701));
#25836=CARTESIAN_POINT('Ctrl Pts',(1.09120934524512,0.300938815206533,-1.13256466454209));
#25837=CARTESIAN_POINT('Ctrl Pts',(1.11127472608703,0.15238299872601,-1.14301472769363));
#25838=CARTESIAN_POINT('Ctrl Pts',(1.12102369397598,-0.101931202388078,
-1.16114310364356));
#25839=CARTESIAN_POINT('Ctrl Pts',(1.09791444748827,-0.250846118613163,
-1.17166474109357));
#25840=CARTESIAN_POINT('Ctrl Pts',(0.98930402061091,-0.54516302107658,-1.19404248596663));
#25841=CARTESIAN_POINT('Ctrl Pts',(0.905273423514496,-0.663857977873313,
-1.20420257483709));
#25842=CARTESIAN_POINT('Ctrl Pts',(0.725113385898957,-0.861211673415817,
-1.2232305070904));
#25843=CARTESIAN_POINT('Ctrl Pts',(0.603413551668539,-0.951563052462835,
-1.23381686695743));
#25844=CARTESIAN_POINT('Ctrl Pts',(0.341786112597045,-1.07261170247852,
-1.25438591132205));
#25845=CARTESIAN_POINT('Ctrl Pts',(0.203851405860754,-1.10611718857029,
-1.26432633133823));
#25846=CARTESIAN_POINT('Ctrl Pts',(-0.0349012702549558,-1.12007370080308,
-1.28135486833774));
#25847=CARTESIAN_POINT('Ctrl Pts',(-0.191201997533714,-1.11682300306852,
-1.29221809027823));
#25848=CARTESIAN_POINT('Ctrl Pts',(-0.502214996937538,-1.0073238571117,
-1.31574203875159));
#25849=CARTESIAN_POINT('Ctrl Pts',(-0.626214316349852,-0.934430304671204,
-1.32580461866347));
#25850=CARTESIAN_POINT('Ctrl Pts',(-0.825915661788611,-0.761161572818582,
-1.34463244532763));
#25851=CARTESIAN_POINT('Ctrl Pts',(-0.924464855646192,-0.649976757040037,
-1.35500640985656));
#25852=CARTESIAN_POINT('Ctrl Pts',(-1.06324590215937,-0.369253565391388,
-1.3773391931262));
#25853=CARTESIAN_POINT('Ctrl Pts',(-1.10179845703877,-0.228016486144762,
-1.38757072082651));
#25854=CARTESIAN_POINT('Ctrl Pts',(-1.1216526627367,0.0230529286473262,
-1.40551263954272));
#25855=CARTESIAN_POINT('Ctrl Pts',(-1.11857306467122,0.173002860562925,
-1.41597065679271));
#25856=CARTESIAN_POINT('Ctrl Pts',(-1.01607631574407,0.484189787750164,
-1.43932287502835));
#25857=CARTESIAN_POINT('Ctrl Pts',(-0.943397907937868,0.61393454762198,
-1.4497083967475));
#25858=CARTESIAN_POINT('Ctrl Pts',(-0.731331226988447,0.86397400629996,
-1.47307863229063));
#25859=CARTESIAN_POINT('Ctrl Pts',(-0.604852724324511,0.944731736167629,
-1.48354062141298));
#25860=CARTESIAN_POINT('Ctrl Pts',(-0.377700605109023,1.06037143957915,
-1.50169805664461));
#25861=CARTESIAN_POINT('Ctrl Pts',(-0.232981315456773,1.10176800386664,
-1.51220746164666));
#25862=CARTESIAN_POINT('Ctrl Pts',(0.0794663775051852,1.12675755955542,
-1.53456428016245));
#25863=CARTESIAN_POINT('Ctrl Pts',(0.222597234321235,1.1004636264182,-1.54473227882704));
#25864=CARTESIAN_POINT('Ctrl Pts',(0.478234529751102,1.0191711099922,-1.56383422514426));
#25865=CARTESIAN_POINT('Ctrl Pts',(0.611182247799714,0.946513834085742,
-1.57441525733418));
#25866=CARTESIAN_POINT('Ctrl Pts',(0.840538191683133,0.751460714065254,
-1.59589801163903));
#25867=CARTESIAN_POINT('Ctrl Pts',(0.925588908242788,0.636392952388505,
-1.60591009521362));
#25868=CARTESIAN_POINT('Ctrl Pts',(1.02997735713438,0.440477084841939,-1.62171618375237));
#25869=CARTESIAN_POINT('Ctrl Pts',(1.09418460733438,0.296790717289617,-1.632638099872));
#25870=CARTESIAN_POINT('Ctrl Pts',(1.1250370353998,-0.0352369170928104,
-1.65642866117049));
#25871=CARTESIAN_POINT('Ctrl Pts',(1.1106661667445,-0.17804237558137,-1.66647070761317));
#25872=CARTESIAN_POINT('Ctrl Pts',(1.03703915589556,-0.431145768277768,
-1.68524121999164));
#25873=CARTESIAN_POINT('Ctrl Pts',(0.977352549963126,-0.567498199932388,
-1.69563223691796));
#25874=CARTESIAN_POINT('Ctrl Pts',(0.780383055419231,-0.811029500761411,
-1.71797004573513));
#25875=CARTESIAN_POINT('Ctrl Pts',(0.668471432388786,-0.904915646636013,
-1.72817926042076));
#25876=CARTESIAN_POINT('Ctrl Pts',(0.461203748610871,-1.02120417552908,
-1.74510952128988));
#25877=CARTESIAN_POINT('Ctrl Pts',(0.372801878430357,-1.05728988862616,
-1.75186529968031));
#25878=CARTESIAN_POINT('Ctrl Pts',(0.189124507262833,-1.1048491526056,-1.76540775381491));
#25879=CARTESIAN_POINT('Ctrl Pts',(0.094547706959705,-1.1164597472411,-1.77214984360044));
#25880=CARTESIAN_POINT('Ctrl Pts',(2.02707199885784E-6,-1.11628565404413,
-1.77888591117587));
#25881=CARTESIAN_POINT('Ctrl Pts',(-0.4696881186261,0.9981380597272,0.01413543027923));
#25882=CARTESIAN_POINT('Ctrl Pts',(-0.2318942596183,1.110035356068,-0.004822903054108));
#25883=CARTESIAN_POINT('Ctrl Pts',(0.3258579542137,1.155927922117,-0.04273956972077));
#25884=CARTESIAN_POINT('Ctrl Pts',(1.003936318643,0.6594544137959,-0.09961456972077));
#25885=CARTESIAN_POINT('Ctrl Pts',(1.190400720751,-0.1598981886148,-0.1564895697208));
#25886=CARTESIAN_POINT('Ctrl Pts',(0.7943069665412,-0.9009591520544,-0.2133645697208));
#25887=CARTESIAN_POINT('Ctrl Pts',(0.009432467987834,-1.201066414053,-0.2702395697208));
#25888=CARTESIAN_POINT('Ctrl Pts',(-0.7800537946193,-0.9133258114035,-0.3271145697208));
#25889=CARTESIAN_POINT('Ctrl Pts',(-1.187754649245,-0.1785709428966,-0.3839895697208));
#25890=CARTESIAN_POINT('Ctrl Pts',(-1.014124826746,0.6435832038027,-0.4408645697208));
#25891=CARTESIAN_POINT('Ctrl Pts',(-0.3441455177085,1.150744276231,-0.4977395697208));
#25892=CARTESIAN_POINT('Ctrl Pts',(0.4942711510281,1.094689252768,-0.5546145697208));
#25893=CARTESIAN_POINT('Ctrl Pts',(1.090773532456,0.5028534860695,-0.6114895697208));
#25894=CARTESIAN_POINT('Ctrl Pts',(1.153411671532,-0.3350970673819,-0.6683645697208));
#25895=CARTESIAN_POINT('Ctrl Pts',(0.6515281822355,-1.009038926982,-0.7252395697208));
#25896=CARTESIAN_POINT('Ctrl Pts',(-0.169236898936,-1.189120431432,-0.7821145697208));
#25897=CARTESIAN_POINT('Ctrl Pts',(-0.9071712857378,-0.7872031419892,-0.8389895697208));
#25898=CARTESIAN_POINT('Ctrl Pts',(-1.201103046544,0.,-0.8958645697208));
#25899=CARTESIAN_POINT('Ctrl Pts',(-0.9071712857378,0.7872031419892,-0.9527395697208));
#25900=CARTESIAN_POINT('Ctrl Pts',(-0.169236898936,1.189120431432,-1.009614569721));
#25901=CARTESIAN_POINT('Ctrl Pts',(0.6515281822355,1.009038926982,-1.066489569721));
#25902=CARTESIAN_POINT('Ctrl Pts',(1.153411671532,0.3350970673819,-1.123364569721));
#25903=CARTESIAN_POINT('Ctrl Pts',(1.090773532456,-0.5028534860695,-1.180239569721));
#25904=CARTESIAN_POINT('Ctrl Pts',(0.4942711510281,-1.094689252768,-1.237114569721));
#25905=CARTESIAN_POINT('Ctrl Pts',(-0.3441455177085,-1.150744276231,-1.293989569721));
#25906=CARTESIAN_POINT('Ctrl Pts',(-1.014124826746,-0.6435832038027,-1.350864569721));
#25907=CARTESIAN_POINT('Ctrl Pts',(-1.187754649245,0.1785709428966,-1.407739569721));
#25908=CARTESIAN_POINT('Ctrl Pts',(-0.7800537946193,0.9133258114035,-1.464614569721));
#25909=CARTESIAN_POINT('Ctrl Pts',(0.009432467987832,1.201066414053,-1.521489569721));
#25910=CARTESIAN_POINT('Ctrl Pts',(0.7943069665412,0.9009591520544,-1.578364569721));
#25911=CARTESIAN_POINT('Ctrl Pts',(1.190400720751,0.1598981886148,-1.635239569721));
#25912=CARTESIAN_POINT('Ctrl Pts',(1.003936318643,-0.6594544137959,-1.692114569721));
#25913=CARTESIAN_POINT('Ctrl Pts',(0.3258579542138,-1.155927922117,-1.748989569721));
#25914=CARTESIAN_POINT('Ctrl Pts',(-0.2318942596183,-1.110035356068,-1.786906236387));
#25915=CARTESIAN_POINT('Ctrl Pts',(-0.4696881186261,-0.9981380597272,-1.805864569721));
#25916=CARTESIAN_POINT('Ctrl Pts',(-0.5279823721497,1.122019654338,-0.06491069439342));
#25917=CARTESIAN_POINT('Ctrl Pts',(-0.2606752788197,1.247804824574,-0.08386902772675));
#25918=CARTESIAN_POINT('Ctrl Pts',(0.3663010598456,1.299393240218,-0.1217856943934));
#25919=CARTESIAN_POINT('Ctrl Pts',(1.128537550737,0.7413010717389,-0.1786606943934));
#25920=CARTESIAN_POINT('Ctrl Pts',(1.33814455045,-0.1797435821333,-0.2355356943934));
#25921=CARTESIAN_POINT('Ctrl Pts',(0.892890536887,-1.012779611507,-0.2924106943934));
#25922=CARTESIAN_POINT('Ctrl Pts',(0.01060315691615,-1.350133991585,-0.3492856943934));
#25923=CARTESIAN_POINT('Ctrl Pts',(-0.8768683655278,-1.026681130153,-0.4061606943934));
#25924=CARTESIAN_POINT('Ctrl Pts',(-1.335170067905,-0.2007338620856,-0.4630356943934));
#25925=CARTESIAN_POINT('Ctrl Pts',(-1.139990581936,0.723460043259,-0.5199106943934));
#25926=CARTESIAN_POINT('Ctrl Pts',(-0.3868583419482,1.293566238123,-0.5767856943934));
#25927=CARTESIAN_POINT('Ctrl Pts',(0.555616470709,1.230554075189,-0.6336606943934));
#25928=CARTESIAN_POINT('Ctrl Pts',(1.226152364316,0.5652639823961,-0.6905356943934));
#25929=CARTESIAN_POINT('Ctrl Pts',(1.296564691016,-0.3766868641562,-0.7474106943934));
#25930=CARTESIAN_POINT('Ctrl Pts',(0.7323910942975,-1.134273457497,-0.8042856943934));
#25931=CARTESIAN_POINT('Ctrl Pts',(-0.190241344867,-1.336705360987,-0.8611606943934));
#25932=CARTESIAN_POINT('Ctrl Pts',(-1.019762749782,-0.8849050375959,-0.9180356943934));
#25933=CARTESIAN_POINT('Ctrl Pts',(-1.350175170634,0.,-0.9749106943934));
#25934=CARTESIAN_POINT('Ctrl Pts',(-1.019762749782,0.8849050375959,-1.031785694393));
#25935=CARTESIAN_POINT('Ctrl Pts',(-0.190241344867,1.336705360987,-1.088660694393));
#25936=CARTESIAN_POINT('Ctrl Pts',(0.7323910942975,1.134273457497,-1.145535694393));
#25937=CARTESIAN_POINT('Ctrl Pts',(1.296564691016,0.3766868641562,-1.202410694393));
#25938=CARTESIAN_POINT('Ctrl Pts',(1.226152364316,-0.5652639823961,-1.259285694393));
#25939=CARTESIAN_POINT('Ctrl Pts',(0.555616470709,-1.230554075189,-1.316160694393));
#25940=CARTESIAN_POINT('Ctrl Pts',(-0.3868583419482,-1.293566238123,-1.373035694393));
#25941=CARTESIAN_POINT('Ctrl Pts',(-1.139990581936,-0.723460043259,-1.429910694393));
#25942=CARTESIAN_POINT('Ctrl Pts',(-1.335170067905,0.2007338620856,-1.486785694393));
#25943=CARTESIAN_POINT('Ctrl Pts',(-0.8768683655278,1.026681130153,-1.543660694393));
#25944=CARTESIAN_POINT('Ctrl Pts',(0.01060315691615,1.350133991585,-1.600535694393));
#25945=CARTESIAN_POINT('Ctrl Pts',(0.892890536887,1.012779611507,-1.657410694393));
#25946=CARTESIAN_POINT('Ctrl Pts',(1.33814455045,0.1797435821333,-1.714285694393));
#25947=CARTESIAN_POINT('Ctrl Pts',(1.128537550737,-0.7413010717389,-1.771160694393));
#25948=CARTESIAN_POINT('Ctrl Pts',(0.3663010598456,-1.299393240218,-1.828035694393));
#25949=CARTESIAN_POINT('Ctrl Pts',(-0.2606752788197,-1.247804824574,-1.86595236106));
#25950=CARTESIAN_POINT('Ctrl Pts',(-0.5279823721497,-1.122019654338,-1.884910694393));
#25951=CARTESIAN_POINT('Ctrl Pts',(-0.5862766256734,1.24590124895,-0.1439568190661));
#25952=CARTESIAN_POINT('Ctrl Pts',(-0.2894562980212,1.38557429308,-0.1629151523994));
#25953=CARTESIAN_POINT('Ctrl Pts',(0.4067441654775,1.442858558319,-0.2008318190661));
#25954=CARTESIAN_POINT('Ctrl Pts',(1.253138782831,0.823147729682,-0.2577068190661));
#25955=CARTESIAN_POINT('Ctrl Pts',(1.48588838015,-0.1995889756518,-0.3145818190661));
#25956=CARTESIAN_POINT('Ctrl Pts',(0.9914741072328,-1.12460007096,-0.3714568190661));
#25957=CARTESIAN_POINT('Ctrl Pts',(0.01177384584446,-1.499201569118,-0.4283318190661));
#25958=CARTESIAN_POINT('Ctrl Pts',(-0.9736829364363,-1.140036448902,-0.4852068190661));
#25959=CARTESIAN_POINT('Ctrl Pts',(-1.482585486565,-0.2228967812747,-0.5420818190661));
#25960=CARTESIAN_POINT('Ctrl Pts',(-1.265856337127,0.8033368827153,-0.5989568190661));
#25961=CARTESIAN_POINT('Ctrl Pts',(-0.4295711661878,1.436388200015,-0.6558318190661));
#25962=CARTESIAN_POINT('Ctrl Pts',(0.61696179039,1.36641889761,-0.7127068190661));
#25963=CARTESIAN_POINT('Ctrl Pts',(1.361531196175,0.6276744787227,-0.7695818190661));
#25964=CARTESIAN_POINT('Ctrl Pts',(1.439717710501,-0.4182766609306,-0.8264568190661));
#25965=CARTESIAN_POINT('Ctrl Pts',(0.8132540063595,-1.259507988013,-0.8833318190661));
#25966=CARTESIAN_POINT('Ctrl Pts',(-0.211245790798,-1.484290290542,-0.9402068190661));
#25967=CARTESIAN_POINT('Ctrl Pts',(-1.132354213826,-0.9826069332027,-0.9970818190661));
#25968=CARTESIAN_POINT('Ctrl Pts',(-1.499247294724,0.,-1.053956819066));
#25969=CARTESIAN_POINT('Ctrl Pts',(-1.132354213826,0.9826069332027,-1.110831819066));
#25970=CARTESIAN_POINT('Ctrl Pts',(-0.211245790798,1.484290290542,-1.167706819066));
#25971=CARTESIAN_POINT('Ctrl Pts',(0.8132540063595,1.259507988012,-1.224581819066));
#25972=CARTESIAN_POINT('Ctrl Pts',(1.439717710501,0.4182766609306,-1.281456819066));
#25973=CARTESIAN_POINT('Ctrl Pts',(1.361531196175,-0.6276744787227,-1.338331819066));
#25974=CARTESIAN_POINT('Ctrl Pts',(0.61696179039,-1.36641889761,-1.395206819066));
#25975=CARTESIAN_POINT('Ctrl Pts',(-0.4295711661878,-1.436388200015,-1.452081819066));
#25976=CARTESIAN_POINT('Ctrl Pts',(-1.265856337127,-0.8033368827153,-1.508956819066));
#25977=CARTESIAN_POINT('Ctrl Pts',(-1.482585486565,0.2228967812747,-1.565831819066));
#25978=CARTESIAN_POINT('Ctrl Pts',(-0.9736829364363,1.140036448902,-1.622706819066));
#25979=CARTESIAN_POINT('Ctrl Pts',(0.01177384584446,1.499201569118,-1.679581819066));
#25980=CARTESIAN_POINT('Ctrl Pts',(0.9914741072328,1.12460007096,-1.736456819066));
#25981=CARTESIAN_POINT('Ctrl Pts',(1.48588838015,0.1995889756517,-1.793331819066));
#25982=CARTESIAN_POINT('Ctrl Pts',(1.253138782831,-0.823147729682,-1.850206819066));
#25983=CARTESIAN_POINT('Ctrl Pts',(0.4067441654775,-1.442858558319,-1.907081819066));
#25984=CARTESIAN_POINT('Ctrl Pts',(-0.2894562980212,-1.38557429308,-1.944998485733));
#25985=CARTESIAN_POINT('Ctrl Pts',(-0.5862766256734,-1.24590124895,-1.963956819066));
#25986=CARTESIAN_POINT('Ctrl Pts',(-0.644570879197,1.369782843561,-0.2230029437387));
#25987=CARTESIAN_POINT('Ctrl Pts',(-0.3182373172226,1.523343761587,-0.241961277072));
#25988=CARTESIAN_POINT('Ctrl Pts',(0.4471872711094,1.586323876419,-0.2798779437387));
#25989=CARTESIAN_POINT('Ctrl Pts',(1.377740014924,0.904994387625,-0.3367529437387));
#25990=CARTESIAN_POINT('Ctrl Pts',(1.633632209849,-0.2194343691702,-0.3936279437387));
#25991=CARTESIAN_POINT('Ctrl Pts',(1.090057677579,-1.236420530413,-0.4505029437387));
#25992=CARTESIAN_POINT('Ctrl Pts',(0.01294453477278,-1.648269146651,-0.5073779437387));
#25993=CARTESIAN_POINT('Ctrl Pts',(-1.070497507345,-1.253391767652,-0.5642529437387));
#25994=CARTESIAN_POINT('Ctrl Pts',(-1.630000905225,-0.2450597004638,-0.6211279437387));
#25995=CARTESIAN_POINT('Ctrl Pts',(-1.391722092318,0.8832137221716,-0.6780029437387));
#25996=CARTESIAN_POINT('Ctrl Pts',(-0.4722839904274,1.579210161907,-0.7348779437387));
#25997=CARTESIAN_POINT('Ctrl Pts',(0.6783071100709,1.502283720031,-0.7917529437387));
#25998=CARTESIAN_POINT('Ctrl Pts',(1.496910028035,0.6900849750494,-0.8486279437387));
#25999=CARTESIAN_POINT('Ctrl Pts',(1.582870729986,-0.4598664577049,-0.9055029437387));
#26000=CARTESIAN_POINT('Ctrl Pts',(0.8941169184215,-1.384742518528,-0.9623779437387));
#26001=CARTESIAN_POINT('Ctrl Pts',(-0.232250236729,-1.631875220096,-1.019252943739));
#26002=CARTESIAN_POINT('Ctrl Pts',(-1.24494567787,-1.080308828809,-1.076127943739));
#26003=CARTESIAN_POINT('Ctrl Pts',(-1.648319418813,0.,-1.133002943739));
#26004=CARTESIAN_POINT('Ctrl Pts',(-1.24494567787,1.080308828809,-1.189877943739));
#26005=CARTESIAN_POINT('Ctrl Pts',(-0.232250236729,1.631875220096,-1.246752943739));
#26006=CARTESIAN_POINT('Ctrl Pts',(0.8941169184216,1.384742518528,-1.303627943739));
#26007=CARTESIAN_POINT('Ctrl Pts',(1.582870729986,0.4598664577049,-1.360502943739));
#26008=CARTESIAN_POINT('Ctrl Pts',(1.496910028035,-0.6900849750494,-1.417377943739));
#26009=CARTESIAN_POINT('Ctrl Pts',(0.6783071100709,-1.502283720031,-1.474252943739));
#26010=CARTESIAN_POINT('Ctrl Pts',(-0.4722839904274,-1.579210161907,-1.531127943739));
#26011=CARTESIAN_POINT('Ctrl Pts',(-1.391722092318,-0.8832137221716,-1.588002943739));
#26012=CARTESIAN_POINT('Ctrl Pts',(-1.630000905225,0.2450597004637,-1.644877943739));
#26013=CARTESIAN_POINT('Ctrl Pts',(-1.070497507345,1.253391767652,-1.701752943739));
#26014=CARTESIAN_POINT('Ctrl Pts',(0.01294453477277,1.648269146651,-1.758627943739));
#26015=CARTESIAN_POINT('Ctrl Pts',(1.090057677579,1.236420530413,-1.815502943739));
#26016=CARTESIAN_POINT('Ctrl Pts',(1.633632209849,0.2194343691702,-1.872377943739));
#26017=CARTESIAN_POINT('Ctrl Pts',(1.377740014924,-0.904994387625,-1.929252943739));
#26018=CARTESIAN_POINT('Ctrl Pts',(0.4471872711094,-1.586323876419,-1.986127943739));
#26019=CARTESIAN_POINT('Ctrl Pts',(-0.3182373172226,-1.523343761587,-2.024044610405));
#26020=CARTESIAN_POINT('Ctrl Pts',(-0.644570879197,-1.369782843561,-2.043002943739));
#26021=CARTESIAN_POINT('',(2.6147125314471E-5,1.4994193789824,-0.249671053225285));
#26022=CARTESIAN_POINT('',(0.,1.5,-0.25));
#26023=CARTESIAN_POINT('',(1.98293436217802E-9,-1.49923261688451,-1.99955700104142));
#26024=CARTESIAN_POINT('',(0.,-1.116987298108,-1.778867513459));
#26025=CARTESIAN_POINT('',(-1.55320824700497E-8,-1.49924686572649,-1.50043442831647));
#26026=CARTESIAN_POINT('Ctrl Pts',(2.23097736337663E-5,-1.49898153286063,
-1.99997329818231));
#26027=CARTESIAN_POINT('Ctrl Pts',(0.134297962277318,-1.49921292007654,
-1.99284084598502));
#26028=CARTESIAN_POINT('Ctrl Pts',(0.268638523155257,-1.48177177551889,
-1.98571955970265));
#26029=CARTESIAN_POINT('Ctrl Pts',(0.528263194565878,-1.41043852051632,
-1.97148351049348));
#26030=CARTESIAN_POINT('Ctrl Pts',(0.652764590084534,-1.35640660493856,
-1.96435339623912));
#26031=CARTESIAN_POINT('Ctrl Pts',(0.931735103478781,-1.18914032301524,
-1.94707782151409));
#26032=CARTESIAN_POINT('Ctrl Pts',(1.07750845761536,-1.05993255468443,-1.93689193230597));
#26033=CARTESIAN_POINT('Ctrl Pts',(1.25254449437154,-0.831135567222865,
-1.92160665898308));
#26034=CARTESIAN_POINT('Ctrl Pts',(1.30304053657959,-0.749217456505738,
-1.91653952634601));
#26035=CARTESIAN_POINT('Ctrl Pts',(1.43181227758846,-0.485623244975981,
-1.90097008905635));
#26036=CARTESIAN_POINT('Ctrl Pts',(1.48316629283892,-0.291367104629342,
-1.89048350490497));
#26037=CARTESIAN_POINT('Ctrl Pts',(1.50934594974658,0.102298044287199,-1.8695359424923));
#26038=CARTESIAN_POINT('Ctrl Pts',(1.48352325672049,0.297075466163154,-1.85935213742399));
#26039=CARTESIAN_POINT('Ctrl Pts',(1.35557807886251,0.667978310212381,-1.83851893537112));
#26040=CARTESIAN_POINT('Ctrl Pts',(1.25672313739978,0.83970672062861,-1.82816969083531));
#26041=CARTESIAN_POINT('Ctrl Pts',(1.06762979706196,1.05767316039942,-1.81285467637234));
#26042=CARTESIAN_POINT('Ctrl Pts',(0.999123065546441,1.12299746696215,-1.80786874916872));
#26043=CARTESIAN_POINT('Ctrl Pts',(0.767476069975274,1.30345302823293,-1.79230752936234));
#26044=CARTESIAN_POINT('Ctrl Pts',(0.585984240279098,1.39346679007975,-1.78173766448593));
#26045=CARTESIAN_POINT('Ctrl Pts',(0.300277913889601,1.47207216422033,-1.7659960136364));
#26046=CARTESIAN_POINT('Ctrl Pts',(0.203413602327542,1.48897911420525,-1.76079851833577));
#26047=CARTESIAN_POINT('Ctrl Pts',(0.0102967612380773,1.50310836043465,
-1.75053281932962));
#26048=CARTESIAN_POINT('Ctrl Pts',(-0.0847305214639188,1.50057827069591,
-1.7455288363176));
#26049=CARTESIAN_POINT('Ctrl Pts',(-0.371065612297978,1.46518487578872,
-1.7302202765876));
#26050=CARTESIAN_POINT('Ctrl Pts',(-0.55852855100465,1.40403962788438,-1.71992087466587));
#26051=CARTESIAN_POINT('Ctrl Pts',(-0.901532722071179,1.21492385002722,
-1.69911972638573));
#26052=CARTESIAN_POINT('Ctrl Pts',(-1.05210324466703,1.08744435980206,-1.68889367702815));
#26053=CARTESIAN_POINT('Ctrl Pts',(-1.29645230872772,0.777009626499769,
-1.66791552392223));
#26054=CARTESIAN_POINT('Ctrl Pts',(-1.38796566499361,0.59897654274782,-1.65746396444275));
#26055=CARTESIAN_POINT('Ctrl Pts',(-1.49653067286123,0.222284704147848,
-1.63665964848054));
#26056=CARTESIAN_POINT('Ctrl Pts',(-1.51209522503029,0.030383734062011,
-1.62667625208365));
#26057=CARTESIAN_POINT('Ctrl Pts',(-1.46756788059896,-0.362285500545997,
-1.60568821925797));
#26058=CARTESIAN_POINT('Ctrl Pts',(-1.40686745038182,-0.555204034967444,
-1.59513614417251));
#26059=CARTESIAN_POINT('Ctrl Pts',(-1.26475548289951,-0.812299601436654,
-1.57955746641289));
#26060=CARTESIAN_POINT('Ctrl Pts',(-1.21076632254199,-0.890422548519847,
-1.57455459690986));
#26061=CARTESIAN_POINT('Ctrl Pts',(-1.0247982663024,-1.11092223632562,-1.5592371921963));
#26062=CARTESIAN_POINT('Ctrl Pts',(-0.871086221419003,-1.23469578181935,
-1.54892247495095));
#26063=CARTESIAN_POINT('Ctrl Pts',(-0.593557655491734,-1.38241748281778,
-1.53223369317102));
#26064=CARTESIAN_POINT('Ctrl Pts',(-0.479696532132474,-1.4266223627924,
-1.52581914810394));
#26065=CARTESIAN_POINT('Ctrl Pts',(-0.242997175564243,-1.48494069752041,
-1.51292148769707));
#26066=CARTESIAN_POINT('Ctrl Pts',(-0.12147955209144,-1.49919084530293,
-1.50647826589496));
#26067=CARTESIAN_POINT('Ctrl Pts',(-2.21303979701729E-5,-1.49898153255151,
-1.50002669228961));
#26068=CARTESIAN_POINT('',(-5.94856812453578E-6,-1.49980089084043,-0.499887533576674));
#26069=CARTESIAN_POINT('Ctrl Pts',(-1.99648916368068E-5,-1.49907115383004,
-1.50007835931766));
#26070=CARTESIAN_POINT('Ctrl Pts',(0.100010792179548,-1.49907329786687,
-1.49486616364447));
#26071=CARTESIAN_POINT('Ctrl Pts',(0.200069985078629,-1.48925441345302,
-1.48963801729206));
#26072=CARTESIAN_POINT('Ctrl Pts',(0.390249520322464,-1.45111632655054,
-1.47928869001663));
#26073=CARTESIAN_POINT('Ctrl Pts',(0.479780074262229,-1.42412384089412,
-1.47417772966106));
#26074=CARTESIAN_POINT('Ctrl Pts',(0.743202348689664,-1.31644836894232,
-1.45869240472173));
#26075=CARTESIAN_POINT('Ctrl Pts',(0.890131060916161,-1.21634961998574,
-1.44967981979634));
#26076=CARTESIAN_POINT('Ctrl Pts',(1.09461260844504,-1.03108060982117,-1.43533626589644));
#26077=CARTESIAN_POINT('Ctrl Pts',(1.1729008973174,-0.941745915552239,-1.42915580900288));
#26078=CARTESIAN_POINT('Ctrl Pts',(1.30586262347788,-0.74705652125546,-1.41637434299397));
#26079=CARTESIAN_POINT('Ctrl Pts',(1.36019807409692,-0.642744360951115,
-1.40991938178315));
#26080=CARTESIAN_POINT('Ctrl Pts',(1.43684888869537,-0.439512380455255,
-1.39841603094486));
#26081=CARTESIAN_POINT('Ctrl Pts',(1.46258240871579,-0.343438435407343,
-1.39329338565573));
#26082=CARTESIAN_POINT('Ctrl Pts',(1.4955073700359,-0.145370938819839,-1.38288605729537));
#26083=CARTESIAN_POINT('Ctrl Pts',(1.50215165440464,-0.0432317669545728,
-1.37759510159625));
#26084=CARTESIAN_POINT('Ctrl Pts',(1.49493265746611,0.150815175439314,-1.36722522754921));
#26085=CARTESIAN_POINT('Ctrl Pts',(1.48294425990366,0.241996318482833,-1.36217498793555));
#26086=CARTESIAN_POINT('Ctrl Pts',(1.4171223673639,0.531784006300281,-1.34595372867182));
#26087=CARTESIAN_POINT('Ctrl Pts',(1.33544689557698,0.699314133729542,-1.33659896396809));
#26088=CARTESIAN_POINT('Ctrl Pts',(1.19973229083852,0.903152679566719,-1.32390070890711));
#26089=CARTESIAN_POINT('Ctrl Pts',(1.14617866632872,0.970503721518277,-1.31941772892764));
#26090=CARTESIAN_POINT('Ctrl Pts',(1.02308385799108,1.10045192315476,-1.309800909446));
#26091=CARTESIAN_POINT('Ctrl Pts',(0.952612668514966,1.16201288551934,-1.30463751792554));
#26092=CARTESIAN_POINT('Ctrl Pts',(0.749672622361954,1.30821426838173,-1.2910095866553));
#26093=CARTESIAN_POINT('Ctrl Pts',(0.608352109295587,1.37900069556785,-1.28295864515549));
#26094=CARTESIAN_POINT('Ctrl Pts',(0.377206086272509,1.45358015351625,-1.27041671486279));
#26095=CARTESIAN_POINT('Ctrl Pts',(0.292097969799569,1.47319097101559,-1.26590263694807));
#26096=CARTESIAN_POINT('Ctrl Pts',(0.0898567471207522,1.50150376362953,
-1.25501677461679));
#26097=CARTESIAN_POINT('Ctrl Pts',(-0.0272253993977831,1.5039278197908,
-1.24853630947231));
#26098=CARTESIAN_POINT('Ctrl Pts',(-0.298527879387531,1.4777809042739,-1.23372098560702));
#26099=CARTESIAN_POINT('Ctrl Pts',(-0.45044657350189,1.4382619968281,-1.2257758523679));
#26100=CARTESIAN_POINT('Ctrl Pts',(-0.691046340416202,1.33481966129264,
-1.21226172515724));
#26101=CARTESIAN_POINT('Ctrl Pts',(-0.78505272569885,1.28205564623737,-1.20666418776859));
#26102=CARTESIAN_POINT('Ctrl Pts',(-0.953191872890371,1.16185980252796,
-1.1954464713411));
#26103=CARTESIAN_POINT('Ctrl Pts',(-1.02802544796662,1.09622974031063,-1.18994188269062));
#26104=CARTESIAN_POINT('Ctrl Pts',(-1.19354290531248,0.919019881447236,
-1.17681353188812));
#26105=CARTESIAN_POINT('Ctrl Pts',(-1.27570185142782,0.800404022341491,
-1.16951178509106));
#26106=CARTESIAN_POINT('Ctrl Pts',(-1.38768122665806,0.577628143130332,
-1.15666830613508));
#26107=CARTESIAN_POINT('Ctrl Pts',(-1.42556288709254,0.477113380022469,
-1.15109714816553));
#26108=CARTESIAN_POINT('Ctrl Pts',(-1.47781991767828,0.273941629700634,
-1.1397165799079));
#26109=CARTESIAN_POINT('Ctrl Pts',(-1.49313607998845,0.172070011743343,
-1.13401960730222));
#26110=CARTESIAN_POINT('Ctrl Pts',(-1.50371664120506,-0.0551323601073528,
-1.12170116965879));
#26111=CARTESIAN_POINT('Ctrl Pts',(-1.49366873901588,-0.180040504057676,
-1.11529369189568));
#26112=CARTESIAN_POINT('Ctrl Pts',(-1.44320719446622,-0.425509966378713,
-1.10242124470283));
#26113=CARTESIAN_POINT('Ctrl Pts',(-1.40223811657279,-0.546093269237912,
-1.09587535154167));
#26114=CARTESIAN_POINT('Ctrl Pts',(-1.26881799908278,-0.818122243168699,
-1.07941603801019));
#26115=CARTESIAN_POINT('Ctrl Pts',(-1.15460642284242,-0.981022106197246,
-1.06857417798349));
#26116=CARTESIAN_POINT('Ctrl Pts',(-0.897625310307818,-1.20753212352388,
-1.05094200853052));
#26117=CARTESIAN_POINT('Ctrl Pts',(-0.763406902307776,-1.30530337522424,
-1.04266849888574));
#26118=CARTESIAN_POINT('Ctrl Pts',(-0.432379286030744,-1.44495334384168,
-1.02310454786419));
#26119=CARTESIAN_POINT('Ctrl Pts',(-0.24768634626944,-1.494071802094,-1.0126836955935));
#26120=CARTESIAN_POINT('Ctrl Pts',(0.123993311035133,-1.50277099843374,
-0.99354665852439));
#26121=CARTESIAN_POINT('Ctrl Pts',(0.282789316550348,-1.48127209667292,
-0.985466284213652));
#26122=CARTESIAN_POINT('Ctrl Pts',(0.592840947756912,-1.38675471981538,
-0.967848554952269));
#26123=CARTESIAN_POINT('Ctrl Pts',(0.770188299195702,-1.30499820912315,
-0.957173992091056));
#26124=CARTESIAN_POINT('Ctrl Pts',(1.0091683764049,-1.11261880737999,-0.941380104211402));
#26125=CARTESIAN_POINT('Ctrl Pts',(1.073317430635,-1.05086531321477,-0.936872292770045));
#26126=CARTESIAN_POINT('Ctrl Pts',(1.20700755932124,-0.897034516416044,
-0.926243466813761));
#26127=CARTESIAN_POINT('Ctrl Pts',(1.2720596868803,-0.801725608748136,-0.919992081713298));
#26128=CARTESIAN_POINT('Ctrl Pts',(1.38574003033754,-0.586690589800353,
-0.906675857250465));
#26129=CARTESIAN_POINT('Ctrl Pts',(1.43150828147209,-0.464980700073504,
-0.899643953226378));
#26130=CARTESIAN_POINT('Ctrl Pts',(1.49753073591719,-0.180369835395416,
-0.88448612623695));
#26131=CARTESIAN_POINT('Ctrl Pts',(1.51285058584363,0.00247071549351316,
-0.875399835205175));
#26132=CARTESIAN_POINT('Ctrl Pts',(1.46230301349907,0.37267475367652,-0.855108229566284));
#26133=CARTESIAN_POINT('Ctrl Pts',(1.40593455773014,0.56796265523729,-0.844074579384696));
#26134=CARTESIAN_POINT('Ctrl Pts',(1.25251289572464,0.828285671734061,-0.828546501939329));
#26135=CARTESIAN_POINT('Ctrl Pts',(1.2078958083307,0.892061281596229,-0.824591589989435));
#26136=CARTESIAN_POINT('Ctrl Pts',(1.100827212269,1.02212890624593,-0.815794818911729));
#26137=CARTESIAN_POINT('Ctrl Pts',(1.03673876444052,1.08680447019536,-0.810902511090885));
#26138=CARTESIAN_POINT('Ctrl Pts',(0.860982719771297,1.23511568589174,-0.798382479495188));
#26139=CARTESIAN_POINT('Ctrl Pts',(0.718891117909026,1.3301263352465,-0.7890640585549));
#26140=CARTESIAN_POINT('Ctrl Pts',(0.422477786378846,1.44432400663123,-0.772644215476221));
#26141=CARTESIAN_POINT('Ctrl Pts',(0.301546629055091,1.47430348317788,-0.766383304558125));
#26142=CARTESIAN_POINT('Ctrl Pts',(0.0782712966722918,1.50050526795073,
-0.754410942138888));
#26143=CARTESIAN_POINT('Ctrl Pts',(-0.0218966802260001,1.50224799260922,
-0.748964773344174));
#26144=CARTESIAN_POINT('Ctrl Pts',(-0.248676328306329,1.48397607588603,
-0.736574336211773));
#26145=CARTESIAN_POINT('Ctrl Pts',(-0.375095119546514,1.45763411426832,
-0.729656514606377));
#26146=CARTESIAN_POINT('Ctrl Pts',(-0.612077379531005,1.37463449545206,
-0.716662996105306));
#26147=CARTESIAN_POINT('Ctrl Pts',(-0.721807835821291,1.32025327114755,
-0.710491973297748));
#26148=CARTESIAN_POINT('Ctrl Pts',(-0.915055210225513,1.19249631921147,
-0.698160760775035));
#26149=CARTESIAN_POINT('Ctrl Pts',(-0.999168138085294,1.12275051159727,
-0.692229347781927));
#26150=CARTESIAN_POINT('Ctrl Pts',(-1.1444484769929,0.973558823158012,-0.680918157030638));
#26151=CARTESIAN_POINT('Ctrl Pts',(-1.20700328585692,0.895307349521417,
-0.67553121744527));
#26152=CARTESIAN_POINT('Ctrl Pts',(-1.30668967310925,0.740930549865537,
-0.665897403655337));
#26153=CARTESIAN_POINT('Ctrl Pts',(-1.3461972124217,0.666466136868907,-0.661616642075847));
#26154=CARTESIAN_POINT('Ctrl Pts',(-1.45276490927942,0.416369341677812,
-0.647558516382313));
#26155=CARTESIAN_POINT('Ctrl Pts',(-1.4864222724122,0.246339841458581,-0.638220784166622));
#26156=CARTESIAN_POINT('Ctrl Pts',(-1.50250622978574,-0.00547396038538936,
-0.624547403106134));
#26157=CARTESIAN_POINT('Ctrl Pts',(-1.49910504162675,-0.105679094128752,
-0.619168655697039));
#26158=CARTESIAN_POINT('Ctrl Pts',(-1.47323337206388,-0.296077263212728,
-0.609090188545362));
#26159=CARTESIAN_POINT('Ctrl Pts',(-1.45224759160403,-0.386023362816676,
-0.604409926631516));
#26160=CARTESIAN_POINT('Ctrl Pts',(-1.38664469068925,-0.582199052059527,
-0.593640518279727));
#26161=CARTESIAN_POINT('Ctrl Pts',(-1.33755993494745,-0.686611593605869,
-0.587483783524372));
#26162=CARTESIAN_POINT('Ctrl Pts',(-1.19157954730198,-0.924069523552559,
-0.572418827905029));
#26163=CARTESIAN_POINT('Ctrl Pts',(-1.06921617363583,-1.07274929497444,
-0.562131028343388));
#26164=CARTESIAN_POINT('Ctrl Pts',(-0.838007112048112,-1.24636184039802,
-0.547178757121285));
#26165=CARTESIAN_POINT('Ctrl Pts',(-0.772275043899146,-1.2879809690239,
-0.543168246187858));
#26166=CARTESIAN_POINT('Ctrl Pts',(-0.595357994137584,-1.38133873895422,
-0.532596315569934));
#26167=CARTESIAN_POINT('Ctrl Pts',(-0.48049307141643,-1.42505352361137,
-0.52599765545279));
#26168=CARTESIAN_POINT('Ctrl Pts',(-0.243880376027954,-1.48416071365803,
-0.512837224887416));
#26169=CARTESIAN_POINT('Ctrl Pts',(-0.121966173250744,-1.49959078914017,
-0.506272370752933));
#26170=CARTESIAN_POINT('Ctrl Pts',(-5.94856812308198E-6,-1.49980089084043,
-0.499887533576674));
#26171=CARTESIAN_POINT('Ctrl Pts',(-5.45381040766187E-5,1.49913119745383,
-0.2500210497538));
#26172=CARTESIAN_POINT('Ctrl Pts',(0.0780741250135448,1.49929196137212,
-0.25417399022211));
#26173=CARTESIAN_POINT('Ctrl Pts',(0.156227279223828,1.49345098065259,-0.258324060294719));
#26174=CARTESIAN_POINT('Ctrl Pts',(0.310596746515901,1.46954678065932,-0.266598905901088));
#26175=CARTESIAN_POINT('Ctrl Pts',(0.386430580339945,1.45155040788365,-0.270688784714035));
#26176=CARTESIAN_POINT('Ctrl Pts',(0.510597996972894,1.41116401327425,-0.277603709312788));
#26177=CARTESIAN_POINT('Ctrl Pts',(0.559335006167078,1.39237630444979,-0.280375865718772));
#26178=CARTESIAN_POINT('Ctrl Pts',(0.784703042495158,1.29174833012765,-0.293517915139593));
#26179=CARTESIAN_POINT('Ctrl Pts',(0.947356094247462,1.17771675062754,-0.303973591508499));
#26180=CARTESIAN_POINT('Ctrl Pts',(1.14601025373637,0.97177688005302,-0.319123070038468));
#26181=CARTESIAN_POINT('Ctrl Pts',(1.20336533402626,0.900260866186981,-0.323904926989636));
#26182=CARTESIAN_POINT('Ctrl Pts',(1.3074220891629,0.74150612948606,-0.333871860552341));
#26183=CARTESIAN_POINT('Ctrl Pts',(1.35281468784255,0.654104018334678,-0.339082925501949));
#26184=CARTESIAN_POINT('Ctrl Pts',(1.46110290740528,0.385005677589548,-0.354573723739613));
#26185=CARTESIAN_POINT('Ctrl Pts',(1.49917179657801,0.192899123978207,-0.364932563984502));
#26186=CARTESIAN_POINT('Ctrl Pts',(1.50005395314928,-0.0935609344680583,
-0.380019105219707));
#26187=CARTESIAN_POINT('Ctrl Pts',(1.49128205669311,-0.187011148649471,
-0.384858146033504));
#26188=CARTESIAN_POINT('Ctrl Pts',(1.43858978421221,-0.46077828414352,-0.399586610860885));
#26189=CARTESIAN_POINT('Ctrl Pts',(1.36981503131428,-0.6354752183641,-0.409586106317029));
#26190=CARTESIAN_POINT('Ctrl Pts',(1.19399261033596,-0.919357485746789,
-0.427422853750231));
#26191=CARTESIAN_POINT('Ctrl Pts',(1.07023831968133,-1.07945897176414,-0.437570713370438));
#26192=CARTESIAN_POINT('Ctrl Pts',(0.745231599973944,-1.30969751346691,
-0.458761834351435));
#26193=CARTESIAN_POINT('Ctrl Pts',(0.60647008903889,-1.37919810936771,-0.467088487340002));
#26194=CARTESIAN_POINT('Ctrl Pts',(0.386357124185273,-1.4508074407617,-0.479477250885268));
#26195=CARTESIAN_POINT('Ctrl Pts',(0.310096596107869,-1.46927193141189,
-0.483634056530725));
#26196=CARTESIAN_POINT('Ctrl Pts',(0.155734301255375,-1.49385305411899,
-0.491814027433449));
#26197=CARTESIAN_POINT('Ctrl Pts',(0.0779900951438741,-1.49993525515011,
-0.495804300368557));
#26198=CARTESIAN_POINT('Ctrl Pts',(-5.94856812385146E-6,-1.49980089084043,
-0.499887533576674));
#26199=CARTESIAN_POINT('Origin',(0.,0.,-0.1394337567297));
#26200=CARTESIAN_POINT('Ctrl Pts',(0.744968168489605,0.832275826917867,
-0.0288675134594948));
#26201=CARTESIAN_POINT('Ctrl Pts',(0.820536075581119,0.772694075545469,
-0.0323343597996823));
#26202=CARTESIAN_POINT('Ctrl Pts',(0.888319065033549,0.703527584149935,
-0.0358520130386424));
#26203=CARTESIAN_POINT('Ctrl Pts',(1.00420116625598,0.549722060754537,-0.0426018521374664));
#26204=CARTESIAN_POINT('Ctrl Pts',(1.05194671393374,0.46548854388906,-0.0458014910649413));
#26205=CARTESIAN_POINT('Ctrl Pts',(1.14548142269179,0.238999221444348,-0.054093189900224));
#26206=CARTESIAN_POINT('Ctrl Pts',(1.17559157541332,0.0910515767618189,
-0.0593081637429571));
#26207=CARTESIAN_POINT('Ctrl Pts',(1.17898019787369,-0.232090382779026,
-0.0704113096782213));
#26208=CARTESIAN_POINT('Ctrl Pts',(1.14154010388872,-0.385690419769286,
-0.0752717872232544));
#26209=CARTESIAN_POINT('Ctrl Pts',(1.03572750735375,-0.649696928154135,
-0.0845969547332541));
#26210=CARTESIAN_POINT('Ctrl Pts',(0.951156135418845,-0.787109400527422,
-0.0900526791622705));
#26211=CARTESIAN_POINT('Ctrl Pts',(0.721634288848172,-1.02225749613246,
-0.100562262399528));
#26212=CARTESIAN_POINT('Ctrl Pts',(0.588532898986576,-1.11363889948885,
-0.105377071715436));
#26213=CARTESIAN_POINT('Ctrl Pts',(0.315871721161606,-1.23373464302002,
-0.114890369640727));
#26214=CARTESIAN_POINT('Ctrl Pts',(0.151790440261885,-1.28133896397508,
-0.120398971070755));
#26215=CARTESIAN_POINT('Ctrl Pts',(-0.207688164228471,-1.28803319903162,
-0.131225510153154));
#26216=CARTESIAN_POINT('Ctrl Pts',(-0.372096471593029,-1.25929311503737,
-0.136137657132471));
#26217=CARTESIAN_POINT('Ctrl Pts',(-0.606449248409185,-1.17134130497118,
-0.143909249049979));
#26218=CARTESIAN_POINT('Ctrl Pts',(-0.683635266369702,-1.13344733995681,
-0.146588319384348));
#26219=CARTESIAN_POINT('Ctrl Pts',(-0.898762753693144,-0.999992061462493,
-0.154209401247211));
#26220=CARTESIAN_POINT('Ctrl Pts',(-1.023045689868,-0.884666880895479,-0.158861114127343));
#26221=CARTESIAN_POINT('Ctrl Pts',(-1.21499816253587,-0.62701520519118,
-0.168345093070664));
#26222=CARTESIAN_POINT('Ctrl Pts',(-1.30322421937978,-0.465133468706287,
-0.173954548293179));
#26223=CARTESIAN_POINT('Ctrl Pts',(-1.396098871979,-0.0890189253362162,
-0.184883028428706));
#26224=CARTESIAN_POINT('Ctrl Pts',(-1.40428952685201,0.094383696364421,
-0.189840736254647));
#26225=CARTESIAN_POINT('Ctrl Pts',(-1.36457053643431,0.36492990957595,-0.197751935705949));
#26226=CARTESIAN_POINT('Ctrl Pts',(-1.34218706524158,0.454984701466365,
-0.200460993435208));
#26227=CARTESIAN_POINT('Ctrl Pts',(-1.24640900146056,0.72334716682606,-0.208556259828602));
#26228=CARTESIAN_POINT('Ctrl Pts',(-1.14970150719883,0.875992371981236,
-0.213147597428451));
#26229=CARTESIAN_POINT('Ctrl Pts',(-0.927851456015851,1.13067058341069,
-0.222414304614733));
#26230=CARTESIAN_POINT('Ctrl Pts',(-0.777605907604323,1.25562501836106,
-0.228009361355914));
#26231=CARTESIAN_POINT('Ctrl Pts',(-0.499086218409759,1.39290411763667,
-0.236270142180347));
#26232=CARTESIAN_POINT('Ctrl Pts',(-0.404620071502844,1.42784380035548,
-0.238844364349628));
#26233=CARTESIAN_POINT('Ctrl Pts',(-0.206951338718649,1.479122751139,-0.244181282610545));
#26234=CARTESIAN_POINT('Ctrl Pts',(-0.103809416887393,1.49470151933882,
-0.246943115301072));
#26235=CARTESIAN_POINT('Ctrl Pts',(-5.49227227915165E-5,1.49958368796161,
-0.249759642713153));
#26236=CARTESIAN_POINT('Ctrl Pts',(0.4476762729852,1.446154421709,0.2341132162814));
#26237=CARTESIAN_POINT('Ctrl Pts',(0.780837923908,1.343019815924,0.2157803457397));
#26238=CARTESIAN_POINT('Ctrl Pts',(1.371452992187,0.8976671939028,0.1791146046562));
#26239=CARTESIAN_POINT('Ctrl Pts',(1.629094976531,-0.1827030763265,0.1241159930311));
#26240=CARTESIAN_POINT('Ctrl Pts',(1.138753746462,-1.179126191151,0.06911738140596));
#26241=CARTESIAN_POINT('Ctrl Pts',(0.1258625640595,-1.634413387851,0.01411876978083));
#26242=CARTESIAN_POINT('Ctrl Pts',(-0.9448155158217,-1.339577634668,-0.0408798418443));
#26243=CARTESIAN_POINT('Ctrl Pts',(-1.581863387021,-0.4299428555337,-0.09587845346944));
#26244=CARTESIAN_POINT('Ctrl Pts',(-1.492914631311,0.6770152357909,-0.1508770650946));
#26245=CARTESIAN_POINT('Ctrl Pts',(-0.7187903802255,1.47325619137,-0.2058756767197));
#26246=CARTESIAN_POINT('Ctrl Pts',(0.385223516623,1.593344378308,-0.2608742883448));
#26247=CARTESIAN_POINT('Ctrl Pts',(1.312438620817,0.9821651256391,-0.31587289997));
#26248=CARTESIAN_POINT('Ctrl Pts',(1.637308341563,-0.07978005883413,-0.3708715115951));
#26249=CARTESIAN_POINT('Ctrl Pts',(1.210733317465,-1.105110084454,-0.4258701232202));
#26250=CARTESIAN_POINT('Ctrl Pts',(0.2284906959225,-1.623248430244,-0.4808687348454));
#26251=CARTESIAN_POINT('Ctrl Pts',(-0.858618021139,-1.396394843238,-0.5358673464705));
#26252=CARTESIAN_POINT('Ctrl Pts',(-1.551662904744,-0.5286640658313,-0.5908659580956));
#26253=CARTESIAN_POINT('Ctrl Pts',(-1.532570123523,0.5816977573753,-0.6458645697208));
#26254=CARTESIAN_POINT('Ctrl Pts',(-0.8101023337328,1.425088654555,-0.7008631813459));
#26255=CARTESIAN_POINT('Ctrl Pts',(0.2841629530904,1.614433300121,-0.755861792971));
#26256=CARTESIAN_POINT('Ctrl Pts',(1.24801129092,1.062831728049,-0.8108604045962));
#26257=CARTESIAN_POINT('Ctrl Pts',(1.639083258684,0.02344218173783,-0.8658590162213));
#26258=CARTESIAN_POINT('Ctrl Pts',(1.27789587838,-1.026706183462,-0.9208576278464));
#26259=CARTESIAN_POINT('Ctrl Pts',(0.3302165605045,-1.605646440099,-0.9758562394716));
#26260=CARTESIAN_POINT('Ctrl Pts',(-0.7690160758597,-1.447673216135,-1.030854851097));
#26261=CARTESIAN_POINT('Ctrl Pts',(-1.515307776415,-0.6252885404762,-1.085853462722));
#26262=CARTESIAN_POINT('Ctrl Pts',(-1.566147153266,0.4840731558256,-1.140852074347));
#26263=CARTESIAN_POINT('Ctrl Pts',(-0.8982008953502,1.371268677471,-1.195850685972));
#26264=CARTESIAN_POINT('Ctrl Pts',(0.1819742926137,1.629119380239,-1.250849297597));
#26265=CARTESIAN_POINT('Ctrl Pts',(1.178637797514,1.139281110916,-1.305847909222));
#26266=CARTESIAN_POINT('Ctrl Pts',(1.634342898764,0.1265778772082,-1.360846520848));
#26267=CARTESIAN_POINT('Ctrl Pts',(1.340042942684,-0.9442540804366,-1.415845132473));
#26268=CARTESIAN_POINT('Ctrl Pts',(0.4304348753708,-1.581586393104,-1.470843744098));
#26269=CARTESIAN_POINT('Ctrl Pts',(-0.3069388631827,-1.522891533776,-1.507509485181));
#26270=CARTESIAN_POINT('Ctrl Pts',(-0.624627630162,-1.37899129093,-1.525842355723));
#26271=CARTESIAN_POINT('Ctrl Pts',(0.4071889425826,1.315365868868,0.1550670916087));
#26272=CARTESIAN_POINT('Ctrl Pts',(0.7102198346237,1.22155863894,0.136734221067));
#26273=CARTESIAN_POINT('Ctrl Pts',(1.247420351243,0.8164831989845,0.1000684799836));
#26274=CARTESIAN_POINT('Ctrl Pts',(1.481761489027,-0.1661796189463,0.04506986835845));
#26275=CARTESIAN_POINT('Ctrl Pts',(1.03576615931,-1.072487366249,-0.00992874326668));
#26276=CARTESIAN_POINT('Ctrl Pts',(0.1144796976359,-1.486598909306,-0.06492735489181));
#26277=CARTESIAN_POINT('Ctrl Pts',(-0.859367480563,-1.218427764623,-0.1199259665169));
#26278=CARTESIAN_POINT('Ctrl Pts',(-1.438801470482,-0.3910593151348,-0.1749245781421));
#26279=CARTESIAN_POINT('Ctrl Pts',(-1.357897138564,0.6157867517431,-0.2299231897672));
#26280=CARTESIAN_POINT('Ctrl Pts',(-0.653783799867,1.340016585461,-0.2849218013923));
#26281=CARTESIAN_POINT('Ctrl Pts',(0.3503843421178,1.449244134041,-0.3399204130175));
#26282=CARTESIAN_POINT('Ctrl Pts',(1.193743172162,0.8933392343618,-0.3949190246426));
#26283=CARTESIAN_POINT('Ctrl Pts',(1.489232046713,-0.07256484150752,-0.4499176362677));
#26284=CARTESIAN_POINT('Ctrl Pts',(1.101235980189,-1.005165191637,-0.5049162478929));
#26285=CARTESIAN_POINT('Ctrl Pts',(0.2078262585646,-1.476443697703,-0.559914859518));
#26286=CARTESIAN_POINT('Ctrl Pts',(-0.7809655887694,-1.270106489796,-0.6149134711432));
#26287=CARTESIAN_POINT('Ctrl Pts',(-1.411332285301,-0.4808522920186,-0.6699120827683));
#26288=CARTESIAN_POINT('Ctrl Pts',(-1.393966233389,0.5290896771207,-0.7249106943934));
#26289=CARTESIAN_POINT('Ctrl Pts',(-0.7368376046753,1.296205265616,-0.7799093060186));
#26290=CARTESIAN_POINT('Ctrl Pts',(0.2584635804317,1.468425797871,-0.8349079176437));
#26291=CARTESIAN_POINT('Ctrl Pts',(1.135142576336,0.9667104414579,-0.8899065292688));
#26292=CARTESIAN_POINT('Ctrl Pts',(1.490846442359,0.02132209761756,-0.944905140894));
#26293=CARTESIAN_POINT('Ctrl Pts',(1.162324435866,-0.9338520498285,-0.9999037525191));
#26294=CARTESIAN_POINT('Ctrl Pts',(0.3003521522337,-1.460433611426,-1.054902364144));
#26295=CARTESIAN_POINT('Ctrl Pts',(-0.6994671409997,-1.316747305262,-1.109900975769));
#26296=CARTESIAN_POINT('Ctrl Pts',(-1.378265073222,-0.5687381596254,-1.164899587394));
#26297=CARTESIAN_POINT('Ctrl Pts',(-1.424506594944,0.4402941329432,-1.21989819902));
#26298=CARTESIAN_POINT('Ctrl Pts',(-0.816968633083,1.247252705739,-1.274896810645));
#26299=CARTESIAN_POINT('Ctrl Pts',(0.1655167455995,1.481783685691,-1.32989542227));
#26300=CARTESIAN_POINT('Ctrl Pts',(1.072043142374,1.036245829525,-1.384894033895));
#26301=CARTESIAN_POINT('Ctrl Pts',(1.486534795172,0.1151303186811,-1.43989264552));
#26302=CARTESIAN_POINT('Ctrl Pts',(1.218850990713,-0.8588568207524,-1.494891257145));
#26303=CARTESIAN_POINT('Ctrl Pts',(0.3915068372603,-1.438549527579,-1.54988986877));
#26304=CARTESIAN_POINT('Ctrl Pts',(-0.2791796632497,-1.385162964236,-1.586555609854));
#26305=CARTESIAN_POINT('Ctrl Pts',(-0.5681370212845,-1.254276894864,-1.604888480396));
#26306=CARTESIAN_POINT('Ctrl Pts',(0.3667016121801,1.184577316028,0.07602096693608));
#26307=CARTESIAN_POINT('Ctrl Pts',(0.6396017453395,1.100097461957,0.05768809639437));
#26308=CARTESIAN_POINT('Ctrl Pts',(1.1233877103,0.7352992040661,0.02102235531094));
#26309=CARTESIAN_POINT('Ctrl Pts',(1.334428001522,-0.1496561615661,-0.03397625631419));
#26310=CARTESIAN_POINT('Ctrl Pts',(0.9327785721571,-0.9658485413479,-0.08897486793932));
#26311=CARTESIAN_POINT('Ctrl Pts',(0.1030968312124,-1.338784430761,-0.1439734795645));
#26312=CARTESIAN_POINT('Ctrl Pts',(-0.7739194453042,-1.097277894577,-0.1989720911896));
#26313=CARTESIAN_POINT('Ctrl Pts',(-1.295739553944,-0.352175774736,-0.2539707028147));
#26314=CARTESIAN_POINT('Ctrl Pts',(-1.222879645817,0.5545582676954,-0.3089693144399));
#26315=CARTESIAN_POINT('Ctrl Pts',(-0.5887772195086,1.206776979551,-0.363967926065));
#26316=CARTESIAN_POINT('Ctrl Pts',(0.3155451676127,1.305143889774,-0.4189665376901));
#26317=CARTESIAN_POINT('Ctrl Pts',(1.075047723507,0.8045133430845,-0.4739651493153));
#26318=CARTESIAN_POINT('Ctrl Pts',(1.341155751864,-0.06534962418092,-0.5289637609404));
#26319=CARTESIAN_POINT('Ctrl Pts',(0.9917386429129,-0.9052202988191,-0.5839623725655));
#26320=CARTESIAN_POINT('Ctrl Pts',(0.1871618212067,-1.329638965161,-0.6389609841907));
#26321=CARTESIAN_POINT('Ctrl Pts',(-0.7033131563998,-1.143818136353,-0.6939595958158));
#26322=CARTESIAN_POINT('Ctrl Pts',(-1.271001665859,-0.433040518206,-0.7489582074409));
#26323=CARTESIAN_POINT('Ctrl Pts',(-1.255362343256,0.4764815968661,-0.8039568190661));
#26324=CARTESIAN_POINT('Ctrl Pts',(-0.6635728756178,1.167321876677,-0.8589554306912));
#26325=CARTESIAN_POINT('Ctrl Pts',(0.2327642077729,1.322418295622,-0.9139540423163));
#26326=CARTESIAN_POINT('Ctrl Pts',(1.022273861752,0.8705891548663,-0.9689526539415));
#26327=CARTESIAN_POINT('Ctrl Pts',(1.342609626034,0.01920201349729,-1.023951265567));
#26328=CARTESIAN_POINT('Ctrl Pts',(1.046752993353,-0.8409979161953,-1.078949877192));
#26329=CARTESIAN_POINT('Ctrl Pts',(0.270487743963,-1.315220782753,-1.133948488817));
#26330=CARTESIAN_POINT('Ctrl Pts',(-0.6299182061397,-1.18582139439,-1.188947100442));
#26331=CARTESIAN_POINT('Ctrl Pts',(-1.241222370029,-0.5121877787746,-1.243945712067));
#26332=CARTESIAN_POINT('Ctrl Pts',(-1.282866036621,0.3965151100608,-1.298944323692));
#26333=CARTESIAN_POINT('Ctrl Pts',(-0.7357363708159,1.123236734008,-1.353942935317));
#26334=CARTESIAN_POINT('Ctrl Pts',(0.1490591985852,1.334447991143,-1.408941546943));
#26335=CARTESIAN_POINT('Ctrl Pts',(0.9654484872351,0.933210548134,-1.463940158568));
#26336=CARTESIAN_POINT('Ctrl Pts',(1.338726691579,0.103682760154,-1.518938770193));
#26337=CARTESIAN_POINT('Ctrl Pts',(1.097659038743,-0.7734595610681,-1.573937381818));
#26338=CARTESIAN_POINT('Ctrl Pts',(0.3525787991498,-1.295512662054,-1.628935993443));
#26339=CARTESIAN_POINT('Ctrl Pts',(-0.2514204633167,-1.247434394696,-1.665601734526));
#26340=CARTESIAN_POINT('Ctrl Pts',(-0.5116464124071,-1.129562498799,-1.683934605068));
#26341=CARTESIAN_POINT('Ctrl Pts',(0.3262142817775,1.053788763187,-0.003025157736566));
#26342=CARTESIAN_POINT('Ctrl Pts',(0.5689836560552,0.9786362849728,-0.02135802827828));
#26343=CARTESIAN_POINT('Ctrl Pts',(0.9993550693557,0.6541152091478,-0.0580237693617));
#26344=CARTESIAN_POINT('Ctrl Pts',(1.187094514017,-0.1331327041859,-0.1130223809868));
#26345=CARTESIAN_POINT('Ctrl Pts',(0.8297909850046,-0.8592097164464,-0.168020992612));
#26346=CARTESIAN_POINT('Ctrl Pts',(0.09171396478879,-1.190969952216,-0.2230196042371));
#26347=CARTESIAN_POINT('Ctrl Pts',(-0.6884714100455,-0.9761280245314,-0.2780182158622));
#26348=CARTESIAN_POINT('Ctrl Pts',(-1.152677637406,-0.3132922343372,-0.3330168274874));
#26349=CARTESIAN_POINT('Ctrl Pts',(-1.08786215307,0.4933297836476,-0.3880154391125));
#26350=CARTESIAN_POINT('Ctrl Pts',(-0.5237706391502,1.073537373642,-0.4430140507376));
#26351=CARTESIAN_POINT('Ctrl Pts',(0.2807059931075,1.161043645508,-0.4980126623628));
#26352=CARTESIAN_POINT('Ctrl Pts',(0.9563522748523,0.7156874518072,-0.5530112739879));
#26353=CARTESIAN_POINT('Ctrl Pts',(1.193079457014,-0.05813440685431,-0.608009885613));
#26354=CARTESIAN_POINT('Ctrl Pts',(0.8822413056368,-0.8052754060015,-0.6630084972382));
#26355=CARTESIAN_POINT('Ctrl Pts',(0.1664973838488,-1.18283423262,-0.7180071088633));
#26356=CARTESIAN_POINT('Ctrl Pts',(-0.6256607240303,-1.017529782911,-0.7730057204884));
#26357=CARTESIAN_POINT('Ctrl Pts',(-1.130671046416,-0.3852287443933,-0.8280043321136));
#26358=CARTESIAN_POINT('Ctrl Pts',(-1.116758453123,0.4238735166115,-0.8830029437387));
#26359=CARTESIAN_POINT('Ctrl Pts',(-0.5903081465603,1.038438487738,-0.9380015553638));
#26360=CARTESIAN_POINT('Ctrl Pts',(0.2070648351141,1.176410793373,-0.993000166989));
#26361=CARTESIAN_POINT('Ctrl Pts',(0.909405147168,0.7744678682747,-1.047998778614));
#26362=CARTESIAN_POINT('Ctrl Pts',(1.194372809709,0.01708192937703,-1.102997390239));
#26363=CARTESIAN_POINT('Ctrl Pts',(0.9311815508389,-0.7481437825621,-1.157996001864));
#26364=CARTESIAN_POINT('Ctrl Pts',(0.2406233356923,-1.17000795408,-1.21299461349));
#26365=CARTESIAN_POINT('Ctrl Pts',(-0.5603692712797,-1.054895483517,-1.267993225115));
#26366=CARTESIAN_POINT('Ctrl Pts',(-1.104179666836,-0.4556373979237,-1.32299183674));
#26367=CARTESIAN_POINT('Ctrl Pts',(-1.141225478299,0.3527360871784,-1.377990448365));
#26368=CARTESIAN_POINT('Ctrl Pts',(-0.6545041085487,0.9992207622761,-1.43298905999));
#26369=CARTESIAN_POINT('Ctrl Pts',(0.1326016515709,1.187112296595,-1.487987671615));
#26370=CARTESIAN_POINT('Ctrl Pts',(0.8588538320959,0.8301752667432,-1.54298628324));
#26371=CARTESIAN_POINT('Ctrl Pts',(1.190918587986,0.09223520162696,-1.597984894865));
#26372=CARTESIAN_POINT('Ctrl Pts',(0.9764670867718,-0.6880623013838,-1.652983506491));
#26373=CARTESIAN_POINT('Ctrl Pts',(0.3136507610394,-1.152475796529,-1.707982118116));
#26374=CARTESIAN_POINT('Ctrl Pts',(-0.2236612633837,-1.109705825156,-1.744647859199));
#26375=CARTESIAN_POINT('Ctrl Pts',(-0.4551558035296,-1.004848102734,-1.762980729741));
#26376=CARTESIAN_POINT('',(0.,-1.5,-1.5));
#26377=CARTESIAN_POINT('Ctrl Pts',(0.644570879197,-1.369782843561,-1.456997056261));
#26378=CARTESIAN_POINT('Ctrl Pts',(0.3182373172226,-1.523343761587,-1.475955389595));
#26379=CARTESIAN_POINT('Ctrl Pts',(-0.4471872711094,-1.586323876419,-1.513872056261));
#26380=CARTESIAN_POINT('Ctrl Pts',(-1.377740014924,-0.904994387625,-1.570747056261));
#26381=CARTESIAN_POINT('Ctrl Pts',(-1.633632209849,0.2194343691702,-1.627622056261));
#26382=CARTESIAN_POINT('Ctrl Pts',(-1.090057677579,1.236420530413,-1.684497056261));
#26383=CARTESIAN_POINT('Ctrl Pts',(-0.01294453477278,1.648269146651,-1.741372056261));
#26384=CARTESIAN_POINT('Ctrl Pts',(1.070497507345,1.253391767652,-1.798247056261));
#26385=CARTESIAN_POINT('Ctrl Pts',(1.630000905225,0.2450597004638,-1.855122056261));
#26386=CARTESIAN_POINT('Ctrl Pts',(1.391722092318,-0.8832137221716,-1.911997056261));
#26387=CARTESIAN_POINT('Ctrl Pts',(0.4722839904274,-1.579210161907,-1.968872056261));
#26388=CARTESIAN_POINT('Ctrl Pts',(-0.6783071100709,-1.502283720031,-2.025747056261));
#26389=CARTESIAN_POINT('Ctrl Pts',(-1.496910028035,-0.6900849750494,-2.082622056261));
#26390=CARTESIAN_POINT('Ctrl Pts',(-1.582870729986,0.4598664577049,-2.139497056261));
#26391=CARTESIAN_POINT('Ctrl Pts',(-0.8941169184215,1.384742518528,-2.196372056261));
#26392=CARTESIAN_POINT('Ctrl Pts',(0.232250236729,1.631875220096,-2.253247056261));
#26393=CARTESIAN_POINT('Ctrl Pts',(1.24494567787,1.080308828809,-2.310122056261));
#26394=CARTESIAN_POINT('Ctrl Pts',(1.648319418813,0.,-2.366997056261));
#26395=CARTESIAN_POINT('Ctrl Pts',(1.24494567787,-1.080308828809,-2.423872056261));
#26396=CARTESIAN_POINT('Ctrl Pts',(0.232250236729,-1.631875220096,-2.480747056261));
#26397=CARTESIAN_POINT('Ctrl Pts',(-0.8941169184215,-1.384742518528,-2.537622056261));
#26398=CARTESIAN_POINT('Ctrl Pts',(-1.582870729986,-0.4598664577049,-2.594497056261));
#26399=CARTESIAN_POINT('Ctrl Pts',(-1.496910028035,0.6900849750494,-2.651372056261));
#26400=CARTESIAN_POINT('Ctrl Pts',(-0.6783071100709,1.502283720031,-2.708247056261));
#26401=CARTESIAN_POINT('Ctrl Pts',(0.4722839904274,1.579210161907,-2.765122056261));
#26402=CARTESIAN_POINT('Ctrl Pts',(1.391722092317,0.8832137221716,-2.821997056261));
#26403=CARTESIAN_POINT('Ctrl Pts',(1.630000905225,-0.2450597004637,-2.878872056261));
#26404=CARTESIAN_POINT('Ctrl Pts',(1.070497507345,-1.253391767652,-2.935747056261));
#26405=CARTESIAN_POINT('Ctrl Pts',(-0.01294453477277,-1.648269146651,-2.992622056261));
#26406=CARTESIAN_POINT('Ctrl Pts',(-1.090057677579,-1.236420530413,-3.049497056261));
#26407=CARTESIAN_POINT('Ctrl Pts',(-1.633632209849,-0.2194343691702,-3.106372056261));
#26408=CARTESIAN_POINT('Ctrl Pts',(-1.377740014924,0.904994387625,-3.163247056261));
#26409=CARTESIAN_POINT('Ctrl Pts',(-0.4471872711094,1.586323876419,-3.220122056261));
#26410=CARTESIAN_POINT('Ctrl Pts',(0.3182373172226,1.523343761587,-3.258038722928));
#26411=CARTESIAN_POINT('Ctrl Pts',(0.644570879197,1.369782843561,-3.276997056261));
#26412=CARTESIAN_POINT('Ctrl Pts',(0.5862766256734,-1.24590124895,-1.536043180934));
#26413=CARTESIAN_POINT('Ctrl Pts',(0.2894562980212,-1.38557429308,-1.555001514267));
#26414=CARTESIAN_POINT('Ctrl Pts',(-0.4067441654775,-1.442858558319,-1.592918180934));
#26415=CARTESIAN_POINT('Ctrl Pts',(-1.253138782831,-0.823147729682,-1.649793180934));
#26416=CARTESIAN_POINT('Ctrl Pts',(-1.48588838015,0.1995889756518,-1.706668180934));
#26417=CARTESIAN_POINT('Ctrl Pts',(-0.9914741072328,1.12460007096,-1.763543180934));
#26418=CARTESIAN_POINT('Ctrl Pts',(-0.01177384584446,1.499201569118,-1.820418180934));
#26419=CARTESIAN_POINT('Ctrl Pts',(0.9736829364363,1.140036448902,-1.877293180934));
#26420=CARTESIAN_POINT('Ctrl Pts',(1.482585486565,0.2228967812747,-1.934168180934));
#26421=CARTESIAN_POINT('Ctrl Pts',(1.265856337127,-0.8033368827153,-1.991043180934));
#26422=CARTESIAN_POINT('Ctrl Pts',(0.4295711661878,-1.436388200015,-2.047918180934));
#26423=CARTESIAN_POINT('Ctrl Pts',(-0.61696179039,-1.36641889761,-2.104793180934));
#26424=CARTESIAN_POINT('Ctrl Pts',(-1.361531196175,-0.6276744787227,-2.161668180934));
#26425=CARTESIAN_POINT('Ctrl Pts',(-1.439717710501,0.4182766609306,-2.218543180934));
#26426=CARTESIAN_POINT('Ctrl Pts',(-0.8132540063595,1.259507988013,-2.275418180934));
#26427=CARTESIAN_POINT('Ctrl Pts',(0.211245790798,1.484290290542,-2.332293180934));
#26428=CARTESIAN_POINT('Ctrl Pts',(1.132354213826,0.9826069332027,-2.389168180934));
#26429=CARTESIAN_POINT('Ctrl Pts',(1.499247294724,0.,-2.446043180934));
#26430=CARTESIAN_POINT('Ctrl Pts',(1.132354213826,-0.9826069332027,-2.502918180934));
#26431=CARTESIAN_POINT('Ctrl Pts',(0.211245790798,-1.484290290542,-2.559793180934));
#26432=CARTESIAN_POINT('Ctrl Pts',(-0.8132540063595,-1.259507988013,-2.616668180934));
#26433=CARTESIAN_POINT('Ctrl Pts',(-1.439717710501,-0.4182766609306,-2.673543180934));
#26434=CARTESIAN_POINT('Ctrl Pts',(-1.361531196175,0.6276744787227,-2.730418180934));
#26435=CARTESIAN_POINT('Ctrl Pts',(-0.61696179039,1.36641889761,-2.787293180934));
#26436=CARTESIAN_POINT('Ctrl Pts',(0.4295711661878,1.436388200015,-2.844168180934));
#26437=CARTESIAN_POINT('Ctrl Pts',(1.265856337127,0.8033368827153,-2.901043180934));
#26438=CARTESIAN_POINT('Ctrl Pts',(1.482585486565,-0.2228967812747,-2.957918180934));
#26439=CARTESIAN_POINT('Ctrl Pts',(0.9736829364363,-1.140036448902,-3.014793180934));
#26440=CARTESIAN_POINT('Ctrl Pts',(-0.01177384584446,-1.499201569118,-3.071668180934));
#26441=CARTESIAN_POINT('Ctrl Pts',(-0.9914741072328,-1.12460007096,-3.128543180934));
#26442=CARTESIAN_POINT('Ctrl Pts',(-1.48588838015,-0.1995889756517,-3.185418180934));
#26443=CARTESIAN_POINT('Ctrl Pts',(-1.253138782831,0.823147729682,-3.242293180934));
#26444=CARTESIAN_POINT('Ctrl Pts',(-0.4067441654775,1.442858558319,-3.299168180934));
#26445=CARTESIAN_POINT('Ctrl Pts',(0.2894562980212,1.38557429308,-3.337084847601));
#26446=CARTESIAN_POINT('Ctrl Pts',(0.5862766256734,1.24590124895,-3.356043180934));
#26447=CARTESIAN_POINT('Ctrl Pts',(0.5279823721497,-1.122019654338,-1.615089305607));
#26448=CARTESIAN_POINT('Ctrl Pts',(0.2606752788197,-1.247804824574,-1.63404763894));
#26449=CARTESIAN_POINT('Ctrl Pts',(-0.3663010598456,-1.299393240218,-1.671964305607));
#26450=CARTESIAN_POINT('Ctrl Pts',(-1.128537550737,-0.7413010717389,-1.728839305607));
#26451=CARTESIAN_POINT('Ctrl Pts',(-1.33814455045,0.1797435821333,-1.785714305607));
#26452=CARTESIAN_POINT('Ctrl Pts',(-0.892890536887,1.012779611507,-1.842589305607));
#26453=CARTESIAN_POINT('Ctrl Pts',(-0.01060315691615,1.350133991585,-1.899464305607));
#26454=CARTESIAN_POINT('Ctrl Pts',(0.8768683655278,1.026681130153,-1.956339305607));
#26455=CARTESIAN_POINT('Ctrl Pts',(1.335170067905,0.2007338620856,-2.013214305607));
#26456=CARTESIAN_POINT('Ctrl Pts',(1.139990581936,-0.723460043259,-2.070089305607));
#26457=CARTESIAN_POINT('Ctrl Pts',(0.3868583419482,-1.293566238123,-2.126964305607));
#26458=CARTESIAN_POINT('Ctrl Pts',(-0.555616470709,-1.230554075189,-2.183839305607));
#26459=CARTESIAN_POINT('Ctrl Pts',(-1.226152364316,-0.5652639823961,-2.240714305607));
#26460=CARTESIAN_POINT('Ctrl Pts',(-1.296564691016,0.3766868641562,-2.297589305607));
#26461=CARTESIAN_POINT('Ctrl Pts',(-0.7323910942975,1.134273457497,-2.354464305607));
#26462=CARTESIAN_POINT('Ctrl Pts',(0.190241344867,1.336705360987,-2.411339305607));
#26463=CARTESIAN_POINT('Ctrl Pts',(1.019762749782,0.8849050375959,-2.468214305607));
#26464=CARTESIAN_POINT('Ctrl Pts',(1.350175170634,0.,-2.525089305607));
#26465=CARTESIAN_POINT('Ctrl Pts',(1.019762749782,-0.8849050375959,-2.581964305607));
#26466=CARTESIAN_POINT('Ctrl Pts',(0.190241344867,-1.336705360987,-2.638839305607));
#26467=CARTESIAN_POINT('Ctrl Pts',(-0.7323910942975,-1.134273457497,-2.695714305607));
#26468=CARTESIAN_POINT('Ctrl Pts',(-1.296564691016,-0.3766868641562,-2.752589305607));
#26469=CARTESIAN_POINT('Ctrl Pts',(-1.226152364316,0.5652639823961,-2.809464305607));
#26470=CARTESIAN_POINT('Ctrl Pts',(-0.555616470709,1.230554075189,-2.866339305607));
#26471=CARTESIAN_POINT('Ctrl Pts',(0.3868583419482,1.293566238123,-2.923214305607));
#26472=CARTESIAN_POINT('Ctrl Pts',(1.139990581936,0.723460043259,-2.980089305607));
#26473=CARTESIAN_POINT('Ctrl Pts',(1.335170067905,-0.2007338620856,-3.036964305607));
#26474=CARTESIAN_POINT('Ctrl Pts',(0.8768683655278,-1.026681130153,-3.093839305607));
#26475=CARTESIAN_POINT('Ctrl Pts',(-0.01060315691615,-1.350133991585,-3.150714305607));
#26476=CARTESIAN_POINT('Ctrl Pts',(-0.892890536887,-1.012779611507,-3.207589305607));
#26477=CARTESIAN_POINT('Ctrl Pts',(-1.33814455045,-0.1797435821333,-3.264464305607));
#26478=CARTESIAN_POINT('Ctrl Pts',(-1.128537550737,0.7413010717389,-3.321339305607));
#26479=CARTESIAN_POINT('Ctrl Pts',(-0.3663010598456,1.299393240218,-3.378214305607));
#26480=CARTESIAN_POINT('Ctrl Pts',(0.2606752788197,1.247804824574,-3.416130972273));
#26481=CARTESIAN_POINT('Ctrl Pts',(0.5279823721497,1.122019654338,-3.435089305607));
#26482=CARTESIAN_POINT('Ctrl Pts',(0.4696881186261,-0.9981380597272,-1.694135430279));
#26483=CARTESIAN_POINT('Ctrl Pts',(0.2318942596183,-1.110035356068,-1.713093763613));
#26484=CARTESIAN_POINT('Ctrl Pts',(-0.3258579542137,-1.155927922117,-1.751010430279));
#26485=CARTESIAN_POINT('Ctrl Pts',(-1.003936318643,-0.6594544137959,-1.807885430279));
#26486=CARTESIAN_POINT('Ctrl Pts',(-1.190400720751,0.1598981886148,-1.864760430279));
#26487=CARTESIAN_POINT('Ctrl Pts',(-0.7943069665412,0.9009591520544,-1.921635430279));
#26488=CARTESIAN_POINT('Ctrl Pts',(-0.009432467987834,1.201066414053,-1.978510430279));
#26489=CARTESIAN_POINT('Ctrl Pts',(0.7800537946193,0.9133258114035,-2.035385430279));
#26490=CARTESIAN_POINT('Ctrl Pts',(1.187754649245,0.1785709428966,-2.092260430279));
#26491=CARTESIAN_POINT('Ctrl Pts',(1.014124826746,-0.6435832038027,-2.149135430279));
#26492=CARTESIAN_POINT('Ctrl Pts',(0.3441455177085,-1.150744276231,-2.206010430279));
#26493=CARTESIAN_POINT('Ctrl Pts',(-0.4942711510281,-1.094689252768,-2.262885430279));
#26494=CARTESIAN_POINT('Ctrl Pts',(-1.090773532456,-0.5028534860695,-2.319760430279));
#26495=CARTESIAN_POINT('Ctrl Pts',(-1.153411671532,0.3350970673819,-2.376635430279));
#26496=CARTESIAN_POINT('Ctrl Pts',(-0.6515281822355,1.009038926982,-2.433510430279));
#26497=CARTESIAN_POINT('Ctrl Pts',(0.169236898936,1.189120431432,-2.490385430279));
#26498=CARTESIAN_POINT('Ctrl Pts',(0.9071712857378,0.7872031419892,-2.547260430279));
#26499=CARTESIAN_POINT('Ctrl Pts',(1.201103046544,0.,-2.604135430279));
#26500=CARTESIAN_POINT('Ctrl Pts',(0.9071712857378,-0.7872031419892,-2.661010430279));
#26501=CARTESIAN_POINT('Ctrl Pts',(0.169236898936,-1.189120431432,-2.717885430279));
#26502=CARTESIAN_POINT('Ctrl Pts',(-0.6515281822355,-1.009038926982,-2.774760430279));
#26503=CARTESIAN_POINT('Ctrl Pts',(-1.153411671532,-0.3350970673819,-2.831635430279));
#26504=CARTESIAN_POINT('Ctrl Pts',(-1.090773532456,0.5028534860695,-2.888510430279));
#26505=CARTESIAN_POINT('Ctrl Pts',(-0.4942711510281,1.094689252768,-2.945385430279));
#26506=CARTESIAN_POINT('Ctrl Pts',(0.3441455177085,1.150744276231,-3.002260430279));
#26507=CARTESIAN_POINT('Ctrl Pts',(1.014124826746,0.6435832038027,-3.059135430279));
#26508=CARTESIAN_POINT('Ctrl Pts',(1.187754649245,-0.1785709428966,-3.116010430279));
#26509=CARTESIAN_POINT('Ctrl Pts',(0.7800537946193,-0.9133258114035,-3.172885430279));
#26510=CARTESIAN_POINT('Ctrl Pts',(-0.009432467987832,-1.201066414053,-3.229760430279));
#26511=CARTESIAN_POINT('Ctrl Pts',(-0.7943069665412,-0.9009591520544,-3.286635430279));
#26512=CARTESIAN_POINT('Ctrl Pts',(-1.190400720751,-0.1598981886148,-3.343510430279));
#26513=CARTESIAN_POINT('Ctrl Pts',(-1.003936318643,0.6594544137959,-3.400385430279));
#26514=CARTESIAN_POINT('Ctrl Pts',(-0.3258579542138,1.155927922117,-3.457260430279));
#26515=CARTESIAN_POINT('Ctrl Pts',(0.2318942596183,1.110035356068,-3.495177096946));
#26516=CARTESIAN_POINT('Ctrl Pts',(0.4696881186261,0.9981380597272,-3.514135430279));
#26517=CARTESIAN_POINT('',(1.98293436067666E-9,1.49923261688425,-3.25044299895813));
#26518=CARTESIAN_POINT('Ctrl Pts',(2.06854461059408E-5,-1.49901358627223,
-1.99995486355702));
#26519=CARTESIAN_POINT('Ctrl Pts',(-0.0953214838110155,-1.49902491199573,
-2.00491761318046));
#26520=CARTESIAN_POINT('Ctrl Pts',(-0.190691030216163,-1.49011947635382,
-2.0098913899261));
#26521=CARTESIAN_POINT('Ctrl Pts',(-0.37249893387041,-1.45546670386657,
-2.0197305237836));
#26522=CARTESIAN_POINT('Ctrl Pts',(-0.458525227544424,-1.43085386099099,
-2.02459116547238));
#26523=CARTESIAN_POINT('Ctrl Pts',(-0.722446426617393,-1.32838383657233,
-2.04004693335259));
#26524=CARTESIAN_POINT('Ctrl Pts',(-0.86645493380528,-1.23164641754706,
-2.04893369151967));
#26525=CARTESIAN_POINT('Ctrl Pts',(-1.06600265467772,-1.06039735381172,
-2.0626050331301));
#26526=CARTESIAN_POINT('Ctrl Pts',(-1.1468383556571,-0.972980331374049,
-2.06875630933358));
#26527=CARTESIAN_POINT('Ctrl Pts',(-1.29967423550166,-0.762168700625944,
-2.08268102999226));
#26528=CARTESIAN_POINT('Ctrl Pts',(-1.36539620478645,-0.636646697395617,
-2.09046986466724));
#26529=CARTESIAN_POINT('Ctrl Pts',(-1.44568091735312,-0.409137312958668,
-2.10325803431831));
#26530=CARTESIAN_POINT('Ctrl Pts',(-1.46940771045106,-0.31232155032306,
-2.10841762364369));
#26531=CARTESIAN_POINT('Ctrl Pts',(-1.50054215939577,-0.0968012311816991,
-2.11974762234642));
#26532=CARTESIAN_POINT('Ctrl Pts',(-1.50386336583337,0.0225864242432771,
-2.1259279009948));
#26533=CARTESIAN_POINT('Ctrl Pts',(-1.48028992278847,0.279075253883525,
-2.13972651028424));
#26534=CARTESIAN_POINT('Ctrl Pts',(-1.44824876150154,0.4138678742304,-2.14734526453954));
#26535=CARTESIAN_POINT('Ctrl Pts',(-1.36138274914138,0.635627037820876,
-2.15997498794209));
#26536=CARTESIAN_POINT('Ctrl Pts',(-1.31601337842939,0.724432162573865,
-2.16513698024779));
#26537=CARTESIAN_POINT('Ctrl Pts',(-1.19858130700141,0.907957044093622,
-2.17647071223724));
#26538=CARTESIAN_POINT('Ctrl Pts',(-1.12297157880735,1.00051622230357,-2.18265174258831));
#26539=CARTESIAN_POINT('Ctrl Pts',(-0.935510734630244,1.18096930350524,
-2.19658311814016));
#26540=CARTESIAN_POINT('Ctrl Pts',(-0.820853703812189,1.26317291479198,
-2.2043395207105));
#26541=CARTESIAN_POINT('Ctrl Pts',(-0.607361198665937,1.3742110709498,-2.21709317469487));
#26542=CARTESIAN_POINT('Ctrl Pts',(-0.51481950301746,1.41125178892119,-2.22225152016787));
#26543=CARTESIAN_POINT('Ctrl Pts',(-0.306211258634909,1.47211310867909,
-2.23355595013963));
#26544=CARTESIAN_POINT('Ctrl Pts',(-0.188926596877854,1.49208312971459,
-2.23971190758978));
#26545=CARTESIAN_POINT('Ctrl Pts',(0.0670817760636266,1.50479893204463,
-2.25344188021204));
#26546=CARTESIAN_POINT('Ctrl Pts',(0.204264061836362,1.49224160547224,-2.26101759022915));
#26547=CARTESIAN_POINT('Ctrl Pts',(0.435383240177761,1.43800305381027,-2.27361014831976));
#26548=CARTESIAN_POINT('Ctrl Pts',(0.529759724211701,1.40572556203723,-2.27877412817635));
#26549=CARTESIAN_POINT('Ctrl Pts',(0.728440094304206,1.31545684930317,-2.29012620086494));
#26550=CARTESIAN_POINT('Ctrl Pts',(0.831081185798915,1.25358147405109,-2.29632332229973));
#26551=CARTESIAN_POINT('Ctrl Pts',(1.03747315158837,1.09264013452201,-2.31033406844491));
#26552=CARTESIAN_POINT('Ctrl Pts',(1.13578892642221,0.989806391524517,-2.31815505599114));
#26553=CARTESIAN_POINT('Ctrl Pts',(1.27616339680962,0.792923500200331,-2.33096631701669));
#26554=CARTESIAN_POINT('Ctrl Pts',(1.32572981587352,0.706468967378648,-2.33612261921326));
#26555=CARTESIAN_POINT('Ctrl Pts',(1.41494914035029,0.508669815652517,-2.34741077045875));
#26556=CARTESIAN_POINT('Ctrl Pts',(1.45101571447836,0.395608673694945,-2.35355276851213));
#26557=CARTESIAN_POINT('Ctrl Pts',(1.49905455000177,0.145868247220176,-2.36717831536221));
#26558=CARTESIAN_POINT('Ctrl Pts',(1.50597375104993,0.00999053376861738,
-2.37466154019217));
#26559=CARTESIAN_POINT('Ctrl Pts',(1.48555860957949,-0.224860674032068,
-2.38717178661232));
#26560=CARTESIAN_POINT('Ctrl Pts',(1.46712396673904,-0.322920215350939,
-2.39233879547481));
#26561=CARTESIAN_POINT('Ctrl Pts',(1.40609716643204,-0.532947437374544,
-2.40371621536761));
#26562=CARTESIAN_POINT('Ctrl Pts',(1.35932684529135,-0.643798827201405,
-2.40993516379191));
#26563=CARTESIAN_POINT('Ctrl Pts',(1.22813604202715,-0.873215485968569,
-2.42407803827426));
#26564=CARTESIAN_POINT('Ctrl Pts',(1.13881445511511,-0.986617888171145,
-2.43201228151042));
#26565=CARTESIAN_POINT('Ctrl Pts',(0.961751173064136,-1.15426033407159,
-2.44492489192123));
#26566=CARTESIAN_POINT('Ctrl Pts',(0.883016083173381,-1.21528568040111,
-2.45007785607501));
#26567=CARTESIAN_POINT('Ctrl Pts',(0.699907663242089,-1.33073761999768,
-2.46133910588146));
#26568=CARTESIAN_POINT('Ctrl Pts',(0.593394360759729,-1.38193694102506,
-2.46745797747925));
#26569=CARTESIAN_POINT('Ctrl Pts',(0.356452332247631,-1.46302840729839,
-2.48088037938892));
#26570=CARTESIAN_POINT('Ctrl Pts',(0.226267156171132,-1.48861703792701,
-2.48817998771775));
#26571=CARTESIAN_POINT('Ctrl Pts',(-0.00575573259439318,-1.5024942239878,
-2.50052727259265));
#26572=CARTESIAN_POINT('Ctrl Pts',(-0.105522727995198,-1.49854594605227,
-2.50570057131398));
#26573=CARTESIAN_POINT('Ctrl Pts',(-0.323231911345657,-1.46862568093801,
-2.51713232860667));
#26574=CARTESIAN_POINT('Ctrl Pts',(-0.440651133511134,-1.43814338966285,
-2.52339821195141));
#26575=CARTESIAN_POINT('Ctrl Pts',(-0.691202779825589,-1.33949753157959,
-2.53779882845232));
#26576=CARTESIAN_POINT('Ctrl Pts',(-0.819432220536387,-1.26490268988018,
-2.54594988333623));
#26577=CARTESIAN_POINT('Ctrl Pts',(-1.01263927792284,-1.10985318182195,
-2.55905699989568));
#26578=CARTESIAN_POINT('Ctrl Pts',(-1.08376671442087,-1.0402156578075,-2.56420386152162));
#26579=CARTESIAN_POINT('Ctrl Pts',(-1.22248539198468,-0.875270661351363,
-2.57541672165905));
#26580=CARTESIAN_POINT('Ctrl Pts',(-1.28731113077471,-0.777524084483589,
-2.58149402763003));
#26581=CARTESIAN_POINT('Ctrl Pts',(-1.39385162402236,-0.566766273385554,
-2.59415987802189));
#26582=CARTESIAN_POINT('Ctrl Pts',(-1.43435322287458,-0.454479793904059,
-2.60073445227219));
#26583=CARTESIAN_POINT('Ctrl Pts',(-1.5015812723815,-0.160350362470448,
-2.61683902084733));
#26584=CARTESIAN_POINT('Ctrl Pts',(-1.50960418346396,0.0246008456484675,
-2.62616861592989));
#26585=CARTESIAN_POINT('Ctrl Pts',(-1.45976216021801,0.392156499871173,
-2.64565249615838));
#26586=CARTESIAN_POINT('Ctrl Pts',(-1.399761565596,0.571423312151105,-2.65599198974553));
#26587=CARTESIAN_POINT('Ctrl Pts',(-1.23961818549049,0.853752427289747,
-2.67322630593744));
#26588=CARTESIAN_POINT('Ctrl Pts',(-1.15716102202243,0.962143722011475,
-2.68020040010219));
#26589=CARTESIAN_POINT('Ctrl Pts',(-0.992056672740698,1.12835719182904,
-2.6924177652927));
#26590=CARTESIAN_POINT('Ctrl Pts',(-0.915130850074121,1.19202945755895,
-2.69763968365057));
#26591=CARTESIAN_POINT('Ctrl Pts',(-0.75101558780099,1.30203114848037,-2.70828226418718));
#26592=CARTESIAN_POINT('Ctrl Pts',(-0.664441333703433,1.34825382201765,
-2.71368412404045));
#26593=CARTESIAN_POINT('Ctrl Pts',(-0.46986663112808,1.42827884858882,-2.72497345546366));
#26594=CARTESIAN_POINT('Ctrl Pts',(-0.361429859064508,1.45911306464794,
-2.73082613074596));
#26595=CARTESIAN_POINT('Ctrl Pts',(-0.0868762359938478,1.50558560899306,
-2.74531699283014));
#26596=CARTESIAN_POINT('Ctrl Pts',(0.108524317627118,1.51122808336332,-2.75529891943664));
#26597=CARTESIAN_POINT('Ctrl Pts',(0.523722674688482,1.42104336270279,-2.77848372599165));
#26598=CARTESIAN_POINT('Ctrl Pts',(0.694234730116656,1.33806699529441,-2.78820584741986));
#26599=CARTESIAN_POINT('Ctrl Pts',(0.910861496243455,1.19466783524342,-2.80172096811971));
#26600=CARTESIAN_POINT('Ctrl Pts',(0.988671361944147,1.13146867146216,-2.80691876599564));
#26601=CARTESIAN_POINT('Ctrl Pts',(1.15071022630635,0.970526548957071,-2.81906886004611));
#26602=CARTESIAN_POINT('Ctrl Pts',(1.22919775430357,0.869129945757312,-2.8261266012726));
#26603=CARTESIAN_POINT('Ctrl Pts',(1.35102651289315,0.660088788782457,-2.83909822282311));
#26604=CARTESIAN_POINT('Ctrl Pts',(1.39685081727246,0.555601837988471,-2.84501522777272));
#26605=CARTESIAN_POINT('Ctrl Pts',(1.46023242591464,0.352631180147119,-2.85607893598742));
#26606=CARTESIAN_POINT('Ctrl Pts',(1.48061440505275,0.254942345668339,-2.86123656160737));
#26607=CARTESIAN_POINT('Ctrl Pts',(1.5071026689533,0.00828580751352354,
-2.87435255893675));
#26608=CARTESIAN_POINT('Ctrl Pts',(1.50081675130931,-0.140074127300878,
-2.88250645615547));
#26609=CARTESIAN_POINT('Ctrl Pts',(1.44962171173141,-0.400100283558441,
-2.89669155693413));
#26610=CARTESIAN_POINT('Ctrl Pts',(1.41383856372191,-0.511332352467065,
-2.90273927950043));
#26611=CARTESIAN_POINT('Ctrl Pts',(1.32508034510813,-0.707735304781241,
-2.91395129249664));
#26612=CARTESIAN_POINT('Ctrl Pts',(1.275257993154,-0.794428647626848,-2.91912511463628));
#26613=CARTESIAN_POINT('Ctrl Pts',(1.13603749864269,-0.989120951294424,
-2.93180966008441));
#26614=CARTESIAN_POINT('Ctrl Pts',(1.03978372917173,-1.09007739184633,-2.93947685530409));
#26615=CARTESIAN_POINT('Ctrl Pts',(0.83999292081546,-1.24722356599987,-2.9530967536497));
#26616=CARTESIAN_POINT('Ctrl Pts',(0.742007099482862,-1.30747183339931,
-2.95905803429899));
#26617=CARTESIAN_POINT('Ctrl Pts',(0.548714342580016,-1.39841818028193,
-2.97017198315474));
#26618=CARTESIAN_POINT('Ctrl Pts',(0.454659915573889,-1.43197845453193,
-2.97533518699447));
#26619=CARTESIAN_POINT('Ctrl Pts',(0.216974120279951,-1.49111903235992,
-2.98829538417047));
#26620=CARTESIAN_POINT('Ctrl Pts',(0.0724161569396505,-1.50527557455147,
-2.99627396486514));
#26621=CARTESIAN_POINT('Ctrl Pts',(-0.188277504892063,-1.49194501788374,
-3.01025172537403));
#26622=CARTESIAN_POINT('Ctrl Pts',(-0.30276292806724,-1.47261448509982,
-3.01626424532904));
#26623=CARTESIAN_POINT('Ctrl Pts',(-0.509166190941301,-1.41331142809819,
-3.02743639057836));
#26624=CARTESIAN_POINT('Ctrl Pts',(-0.602092049119227,-1.37653010346475,
-3.03260599265011));
#26625=CARTESIAN_POINT('Ctrl Pts',(-0.816798907961732,-1.26585681258326,
-3.04539924148289));
#26626=CARTESIAN_POINT('Ctrl Pts',(-0.932266966021383,-1.18361839848064,
-3.05318933375495));
#26627=CARTESIAN_POINT('Ctrl Pts',(-1.1176717611952,-1.00598881418804,-3.06694380600407));
#26628=CARTESIAN_POINT('Ctrl Pts',(-1.1911992232032,-0.917143963823157,
-3.07291881283867));
#26629=CARTESIAN_POINT('Ctrl Pts',(-1.30836409219534,-0.738141596012679,
-3.08404861925295));
#26630=CARTESIAN_POINT('Ctrl Pts',(-1.35471182572544,-0.649655711805248,
-3.08921376341646));
#26631=CARTESIAN_POINT('Ctrl Pts',(-1.44584034292854,-0.42384252583581,
-3.10210234042886));
#26632=CARTESIAN_POINT('Ctrl Pts',(-1.47984174077635,-0.284133317596366,
-3.11000165399304));
#26633=CARTESIAN_POINT('Ctrl Pts',(-1.50356071468369,-0.0257340761398541,
-3.12390253859812));
#26634=CARTESIAN_POINT('Ctrl Pts',(-1.500706949238,0.0902601036655123,-3.12991376788401));
#26635=CARTESIAN_POINT('Ctrl Pts',(-1.4713835756108,0.302890057303145,-3.14108242947861));
#26636=CARTESIAN_POINT('Ctrl Pts',(-1.44820663630739,0.400068083833837,
-3.14625016146593));
#26637=CARTESIAN_POINT('Ctrl Pts',(-1.36846871474809,0.630511787657366,
-3.15916112595278));
#26638=CARTESIAN_POINT('Ctrl Pts',(-1.30213290035678,0.758432227761769,
-3.16707761328715));
#26639=CARTESIAN_POINT('Ctrl Pts',(-1.15014464600899,0.968689653569568,
-3.18095602028395));
#26640=CARTESIAN_POINT('Ctrl Pts',(-1.07203283432336,1.05396027144467,-3.18693871001679));
#26641=CARTESIAN_POINT('Ctrl Pts',(-0.872606659870649,1.22786655368525,
-3.2006960890497));
#26642=CARTESIAN_POINT('Ctrl Pts',(-0.726903650726398,1.32597814557258,
-3.20968126963886));
#26643=CARTESIAN_POINT('Ctrl Pts',(-0.462343408398025,1.42967442692924,
-3.22519006837585));
#26644=CARTESIAN_POINT('Ctrl Pts',(-0.375674252658106,1.45470533198749,
-3.23009449424634));
#26645=CARTESIAN_POINT('Ctrl Pts',(-0.192359458101488,1.48996300799368,
-3.24002156504885));
#26646=CARTESIAN_POINT('Ctrl Pts',(-0.0961554125704673,1.49902501105836,
-3.24503897916825));
#26647=CARTESIAN_POINT('Ctrl Pts',(2.06854460825176E-5,1.49901358627223,
-3.25004513644298));
#26648=CARTESIAN_POINT('',(-3.24550813896681E-10,1.11698717744401,-3.47113249718027));
#26649=CARTESIAN_POINT('',(0.,1.5,-3.25));
#26650=CARTESIAN_POINT('Ctrl Pts',(-2.52570946139784E-6,-1.11628565496219,
-1.7211141243504));
#26651=CARTESIAN_POINT('Ctrl Pts',(-0.0945479806554323,-1.1164597063096,
-1.72785017591353));
#26652=CARTESIAN_POINT('Ctrl Pts',(-0.189124550454961,-1.10484912539831,
-1.73459224965733));
#26653=CARTESIAN_POINT('Ctrl Pts',(-0.372801771216836,-1.05728993252109,
-1.74813469212525));
#26654=CARTESIAN_POINT('Ctrl Pts',(-0.46120369907326,-1.02120420332243,
-1.75489047466375));
#26655=CARTESIAN_POINT('Ctrl Pts',(-0.668471432388855,-0.904915646636004,
-1.77182073957925));
#26656=CARTESIAN_POINT('Ctrl Pts',(-0.780383055419264,-0.811029500761429,
-1.78202995426488));
#26657=CARTESIAN_POINT('Ctrl Pts',(-0.977352549963127,-0.567498199932436,
-1.80436776308206));
#26658=CARTESIAN_POINT('Ctrl Pts',(-1.03703915589555,-0.431145768277802,
-1.8147587800084));
#26659=CARTESIAN_POINT('Ctrl Pts',(-1.11066616674449,-0.178042375581388,
-1.83352929238689));
#26660=CARTESIAN_POINT('Ctrl Pts',(-1.1250370353998,-0.0352369170927978,
-1.84357133882956));
#26661=CARTESIAN_POINT('Ctrl Pts',(-1.09418460733438,0.296790717289756,
-1.86736190012804));
#26662=CARTESIAN_POINT('Ctrl Pts',(-1.02997735713434,0.440477084842055,
-1.87828381624767));
#26663=CARTESIAN_POINT('Ctrl Pts',(-0.925588908242799,0.636392952388536,
-1.89408990478641));
#26664=CARTESIAN_POINT('Ctrl Pts',(-0.840538191683134,0.751460714065274,
-1.90410198836101));
#26665=CARTESIAN_POINT('Ctrl Pts',(-0.61118224779972,0.946513834085747,
-1.92558474266587));
#26666=CARTESIAN_POINT('Ctrl Pts',(-0.4782345297511,1.0191711099922,-1.93616577485579));
#26667=CARTESIAN_POINT('Ctrl Pts',(-0.222597234321223,1.1004636264182,-1.955267721173));
#26668=CARTESIAN_POINT('Ctrl Pts',(-0.0794663775051731,1.12675755955542,
-1.96543571983759));
#26669=CARTESIAN_POINT('Ctrl Pts',(0.232981315456785,1.10176800386664,-1.98779253835339));
#26670=CARTESIAN_POINT('Ctrl Pts',(0.377700605109035,1.06037143957914,-1.99830194335543));
#26671=CARTESIAN_POINT('Ctrl Pts',(0.60485272432455,0.944731736167608,-2.01645937858707));
#26672=CARTESIAN_POINT('Ctrl Pts',(0.731331226988472,0.863974006299934,
-2.02692136770941));
#26673=CARTESIAN_POINT('Ctrl Pts',(0.943397907937875,0.61393454762197,-2.05029160325254));
#26674=CARTESIAN_POINT('Ctrl Pts',(1.01607631574408,0.484189787750154,-2.06067712497169));
#26675=CARTESIAN_POINT('Ctrl Pts',(1.11857306467123,0.173002860562897,-2.08402934320733));
#26676=CARTESIAN_POINT('Ctrl Pts',(1.1216526627367,0.0230529286472913,-2.09448736045733));
#26677=CARTESIAN_POINT('Ctrl Pts',(1.10179845703877,-0.228016486144775,
-2.11242927917354));
#26678=CARTESIAN_POINT('Ctrl Pts',(1.06324590215936,-0.369253565391399,
-2.12266080687385));
#26679=CARTESIAN_POINT('Ctrl Pts',(0.924464855646186,-0.649976757040046,
-2.14499359014349));
#26680=CARTESIAN_POINT('Ctrl Pts',(0.825915661788604,-0.761161572818591,
-2.15536755467241));
#26681=CARTESIAN_POINT('Ctrl Pts',(0.626214316349842,-0.934430304671211,
-2.17419538133658));
#26682=CARTESIAN_POINT('Ctrl Pts',(0.502214996937528,-1.0073238571117,-2.18425796124846));
#26683=CARTESIAN_POINT('Ctrl Pts',(0.19120199753371,-1.11682300306852,-2.20778190972181));
#26684=CARTESIAN_POINT('Ctrl Pts',(0.0349012702549543,-1.12007370080308,
-2.21864513166231));
#26685=CARTESIAN_POINT('Ctrl Pts',(-0.203851405860762,-1.10611718857029,
-2.23567366866181));
#26686=CARTESIAN_POINT('Ctrl Pts',(-0.341786112597053,-1.07261170247851,
-2.245614088678));
#26687=CARTESIAN_POINT('Ctrl Pts',(-0.603413551668547,-0.95156305246283,
-2.26618313304261));
#26688=CARTESIAN_POINT('Ctrl Pts',(-0.725113385898963,-0.861211673415812,
-2.27676949290965));
#26689=CARTESIAN_POINT('Ctrl Pts',(-0.905273423514502,-0.663857977873306,
-2.29579742516296));
#26690=CARTESIAN_POINT('Ctrl Pts',(-0.989304020610915,-0.545163021076572,
-2.30595751403342));
#26691=CARTESIAN_POINT('Ctrl Pts',(-1.09791444748827,-0.250846118613153,
-2.32833525890648));
#26692=CARTESIAN_POINT('Ctrl Pts',(-1.12102369397598,-0.101931202388067,
-2.33885689635648));
#26693=CARTESIAN_POINT('Ctrl Pts',(-1.11127472608703,0.152382998726041,
-2.35698527230642));
#26694=CARTESIAN_POINT('Ctrl Pts',(-1.09120934524511,0.300938815206558,
-2.36743533545796));
#26695=CARTESIAN_POINT('Ctrl Pts',(-0.953355092950169,0.598483057720678,
-2.39081240762303));
#26696=CARTESIAN_POINT('Ctrl Pts',(-0.865889506205107,0.719096632405901,
-2.40121651825254));
#26697=CARTESIAN_POINT('Ctrl Pts',(-0.630908211369321,0.938430669099282,
-2.42412556939149));
#26698=CARTESIAN_POINT('Ctrl Pts',(-0.499473987912807,1.00559671816687,
-2.43443093822623));
#26699=CARTESIAN_POINT('Ctrl Pts',(-0.254954649474644,1.09592824110065,
-2.45300231361181));
#26700=CARTESIAN_POINT('Ctrl Pts',(-0.110233508147538,1.12012616746575,
-2.46325541986775));
#26701=CARTESIAN_POINT('Ctrl Pts',(0.202625788977277,1.11169037854405,-2.48557375090056));
#26702=CARTESIAN_POINT('Ctrl Pts',(0.344594062565005,1.06910154094397,-2.49592507043897));
#26703=CARTESIAN_POINT('Ctrl Pts',(0.586363065095529,0.95997491663841,-2.5148152172114));
#26704=CARTESIAN_POINT('Ctrl Pts',(0.704733656287602,0.877644037487904,
-2.52490073023948));
#26705=CARTESIAN_POINT('Ctrl Pts',(0.924445762809004,0.651144082671878,
-2.54741286795022));
#26706=CARTESIAN_POINT('Ctrl Pts',(0.995878303027182,0.517818669122211,
-2.55795712525469));
#26707=CARTESIAN_POINT('Ctrl Pts',(1.08982166380632,0.277939862987314,-2.57630001885425));
#26708=CARTESIAN_POINT('Ctrl Pts',(1.1169872981078,0.139044412854724,-2.58621126978535));
#26709=CARTESIAN_POINT('Ctrl Pts',(1.1169872981078,-0.139044412854727,-2.60605370329665));
#26710=CARTESIAN_POINT('Ctrl Pts',(1.08982166380632,-0.277939862987316,
-2.61596495422619));
#26711=CARTESIAN_POINT('Ctrl Pts',(0.99587830302718,-0.517818669122218,
-2.63430784782586));
#26712=CARTESIAN_POINT('Ctrl Pts',(0.924445762808999,-0.651144082671885,
-2.64485210513048));
#26713=CARTESIAN_POINT('Ctrl Pts',(0.704733656287598,-0.877644037487907,
-2.66736424284125));
#26714=CARTESIAN_POINT('Ctrl Pts',(0.586363065095524,-0.959974916638413,
-2.67744975586925));
#26715=CARTESIAN_POINT('Ctrl Pts',(0.344594062564994,-1.06910154094398,
-2.69633990264163));
#26716=CARTESIAN_POINT('Ctrl Pts',(0.202625788977266,-1.11169037854405,
-2.70669122217995));
#26717=CARTESIAN_POINT('Ctrl Pts',(-0.110233508147553,-1.12012616746575,
-2.72900955321284));
#26718=CARTESIAN_POINT('Ctrl Pts',(-0.254954649474663,-1.09592824110064,
-2.73926265946891));
#26719=CARTESIAN_POINT('Ctrl Pts',(-0.499473987912819,-1.00559671816686,
-2.75783403485462));
#26720=CARTESIAN_POINT('Ctrl Pts',(-0.63090821136934,-0.938430669099273,
-2.76813940368944));
#26721=CARTESIAN_POINT('Ctrl Pts',(-0.865889506205136,-0.719096632405868,
-2.79104845482854));
#26722=CARTESIAN_POINT('Ctrl Pts',(-0.953355092950196,-0.598483057720636,
-2.80145256545815));
#26723=CARTESIAN_POINT('Ctrl Pts',(-1.09120934524513,-0.300938815206489,
-2.82482963762336));
#26724=CARTESIAN_POINT('Ctrl Pts',(-1.11127472608704,-0.152382998725963,
-2.83527970077493));
#26725=CARTESIAN_POINT('Ctrl Pts',(-1.12102369397598,0.101931202388125,
-2.85340807672478));
#26726=CARTESIAN_POINT('Ctrl Pts',(-1.09791444748826,0.250846118613208,
-2.86392971417461));
#26727=CARTESIAN_POINT('Ctrl Pts',(-0.989304020610891,0.545163021076614,
-2.88630745904754));
#26728=CARTESIAN_POINT('Ctrl Pts',(-0.905273423514476,0.663857977873339,
-2.89646754791798));
#26729=CARTESIAN_POINT('Ctrl Pts',(-0.725113385898938,0.861211673415833,
-2.91549548017135));
#26730=CARTESIAN_POINT('Ctrl Pts',(-0.603413551668517,0.951563052462851,
-2.92608184003854));
#26731=CARTESIAN_POINT('Ctrl Pts',(-0.341786112597021,1.07261170247852,
-2.94665088440312));
#26732=CARTESIAN_POINT('Ctrl Pts',(-0.203851405860732,1.1061171885703,-2.95659130441917));
#26733=CARTESIAN_POINT('Ctrl Pts',(0.0349012702549755,1.12007370080307,
-2.97361984141848));
#26734=CARTESIAN_POINT('Ctrl Pts',(0.191201997533727,1.11682300306852,-2.98448306335867));
#26735=CARTESIAN_POINT('Ctrl Pts',(0.502214996937547,1.00732385711169,-3.00800701183202));
#26736=CARTESIAN_POINT('Ctrl Pts',(0.626214316349863,0.934430304671194,
-3.01806959174406));
#26737=CARTESIAN_POINT('Ctrl Pts',(0.825915661788622,0.761161572818569,
-3.03689741840843));
#26738=CARTESIAN_POINT('Ctrl Pts',(0.924464855646206,0.649976757040018,
-3.04727138293758));
#26739=CARTESIAN_POINT('Ctrl Pts',(1.06324590215938,0.369253565391358,-3.06960416620731));
#26740=CARTESIAN_POINT('Ctrl Pts',(1.10179845703878,0.22801648614473,-3.07983569390757));
#26741=CARTESIAN_POINT('Ctrl Pts',(1.12165266273671,-0.023052928647412,
-3.09777761262373));
#26742=CARTESIAN_POINT('Ctrl Pts',(1.11857306467121,-0.173002860562994,
-3.10823562987364));
#26743=CARTESIAN_POINT('Ctrl Pts',(1.01607631574406,-0.484189787750188,
-3.13158784810919));
#26744=CARTESIAN_POINT('Ctrl Pts',(0.943397907937855,-0.613934547622001,
-3.1419733698283));
#26745=CARTESIAN_POINT('Ctrl Pts',(0.731331226988425,-0.863974006299982,
-3.16534360537137));
#26746=CARTESIAN_POINT('Ctrl Pts',(0.604852724324483,-0.944731736167644,
-3.17580559449369));
#26747=CARTESIAN_POINT('Ctrl Pts',(0.37770060510901,-1.06037143957915,-3.1939630297253));
#26748=CARTESIAN_POINT('Ctrl Pts',(0.232981315456759,-1.10176800386665,
-3.20447243472734));
#26749=CARTESIAN_POINT('Ctrl Pts',(-0.0794663775051969,-1.12675755955542,
-3.22682925324312));
#26750=CARTESIAN_POINT('Ctrl Pts',(-0.222597234321245,-1.1004636264182,
-3.23699725190771));
#26751=CARTESIAN_POINT('Ctrl Pts',(-0.47823452975112,-1.0191711099922,-3.25609919822493));
#26752=CARTESIAN_POINT('Ctrl Pts',(-0.611182247799739,-0.946513834085735,
-3.26668023041484));
#26753=CARTESIAN_POINT('Ctrl Pts',(-0.840538191683138,-0.751460714065267,
-3.28816298471981));
#26754=CARTESIAN_POINT('Ctrl Pts',(-0.925588908242806,-0.636392952388529,
-3.29817506829455));
#26755=CARTESIAN_POINT('Ctrl Pts',(-1.02997735713432,-0.440477084842082,
-3.31398115683343));
#26756=CARTESIAN_POINT('Ctrl Pts',(-1.09418460733438,-0.296790717289784,
-3.32490307295328));
#26757=CARTESIAN_POINT('Ctrl Pts',(-1.1250370353998,0.0352369170927936,
-3.34869363425172));
#26758=CARTESIAN_POINT('Ctrl Pts',(-1.11066616674449,0.178042375581363,
-3.35873568069418));
#26759=CARTESIAN_POINT('Ctrl Pts',(-1.03703915589554,0.431145768277777,
-3.37750619307247));
#26760=CARTESIAN_POINT('Ctrl Pts',(-0.977352549963106,0.567498199932408,
-3.38789720999858));
#26761=CARTESIAN_POINT('Ctrl Pts',(-0.780383055419209,0.811029500761431,
-3.41023501881582));
#26762=CARTESIAN_POINT('Ctrl Pts',(-0.668471432388769,0.904915646636028,
-3.42044423350163));
#26763=CARTESIAN_POINT('Ctrl Pts',(-0.461203748610638,1.02120417552921,
-3.43737449437096));
#26764=CARTESIAN_POINT('Ctrl Pts',(-0.372801878429867,1.05728988862637,
-3.4441302727615));
#26765=CARTESIAN_POINT('Ctrl Pts',(-0.18912446213411,1.10484916429063,-3.45767273022351));
#26766=CARTESIAN_POINT('Ctrl Pts',(-0.0945476136912702,1.11645975869105,
-3.46441482333082));
#26767=CARTESIAN_POINT('Ctrl Pts',(-1.88721575744071E-6,1.11628565378659,
-3.47115089422152));
#26768=CARTESIAN_POINT('Ctrl Pts',(0.4755900604755,-1.010680324589,-1.670126599063));
#26769=CARTESIAN_POINT('Ctrl Pts',(0.2348081643589,-1.123983684464,-1.689084932396));
#26770=CARTESIAN_POINT('Ctrl Pts',(-0.329952574922,-1.170452920957,-1.727001599063));
#26771=CARTESIAN_POINT('Ctrl Pts',(-1.016551442463,-0.6677408946504,-1.783876599063));
#26772=CARTESIAN_POINT('Ctrl Pts',(-1.205358893105,0.1619074151071,-1.840751599063));
#26773=CARTESIAN_POINT('Ctrl Pts',(-0.8042879589087,0.9122802996697,-1.897626599063));
#26774=CARTESIAN_POINT('Ctrl Pts',(-0.009550993186477,1.216158607898,-1.954501599063));
#26775=CARTESIAN_POINT('Ctrl Pts',(0.7898556864549,0.9248023542725,-2.011376599063));
#26776=CARTESIAN_POINT('Ctrl Pts',(1.202679571961,0.180814804896,-2.068251599063));
#26777=CARTESIAN_POINT('Ctrl Pts',(1.026867975908,-0.6516702524068,-2.125126599063));
#26778=CARTESIAN_POINT('Ctrl Pts',(0.348469933747,-1.165204139133,-2.182001599063));
#26779=CARTESIAN_POINT('Ctrl Pts',(-0.5004819949382,-1.108444747226,-2.238876599063));
#26780=CARTESIAN_POINT('Ctrl Pts',(-1.104479823299,-0.5091721726955,-2.295751599063));
#26781=CARTESIAN_POINT('Ctrl Pts',(-1.167905052019,0.3393077836576,-2.352626599063));
#26782=CARTESIAN_POINT('Ctrl Pts',(-0.6597150647482,1.02171816845,-2.409501599063));
#26783=CARTESIAN_POINT('Ctrl Pts',(0.1713634724997,1.204062516105,-2.466376599063));
#26784=CARTESIAN_POINT('Ctrl Pts',(0.9185704929214,0.7970948701029,-2.523251599063));
#26785=CARTESIAN_POINT('Ctrl Pts',(1.216195700701,0.,-2.580126599063));
#26786=CARTESIAN_POINT('Ctrl Pts',(0.9185704929214,-0.7970948701029,-2.637001599063));
#26787=CARTESIAN_POINT('Ctrl Pts',(0.1713634724997,-1.204062516105,-2.693876599063));
#26788=CARTESIAN_POINT('Ctrl Pts',(-0.6597150647482,-1.02171816845,-2.750751599063));
#26789=CARTESIAN_POINT('Ctrl Pts',(-1.167905052019,-0.3393077836576,-2.807626599063));
#26790=CARTESIAN_POINT('Ctrl Pts',(-1.104479823299,0.5091721726955,-2.864501599063));
#26791=CARTESIAN_POINT('Ctrl Pts',(-0.5004819949382,1.108444747226,-2.921376599063));
#26792=CARTESIAN_POINT('Ctrl Pts',(0.348469933747,1.165204139133,-2.978251599063));
#26793=CARTESIAN_POINT('Ctrl Pts',(1.026867975908,0.6516702524068,-3.035126599063));
#26794=CARTESIAN_POINT('Ctrl Pts',(1.202679571961,-0.180814804896,-3.092001599063));
#26795=CARTESIAN_POINT('Ctrl Pts',(0.7898556864549,-0.9248023542725,-3.148876599063));
#26796=CARTESIAN_POINT('Ctrl Pts',(-0.009550993186476,-1.216158607898,-3.205751599063));
#26797=CARTESIAN_POINT('Ctrl Pts',(-0.8042879589087,-0.9122802996697,-3.262626599063));
#26798=CARTESIAN_POINT('Ctrl Pts',(-1.205358893105,-0.1619074151071,-3.319501599063));
#26799=CARTESIAN_POINT('Ctrl Pts',(-1.016551442463,0.6677408946503,-3.376376599063));
#26800=CARTESIAN_POINT('Ctrl Pts',(-0.329952574922,1.170452920957,-3.433251599063));
#26801=CARTESIAN_POINT('Ctrl Pts',(0.2348081643589,1.123983684464,-3.47116826573));
#26802=CARTESIAN_POINT('Ctrl Pts',(0.4755900604755,1.010680324589,-3.490126599063));
#26803=CARTESIAN_POINT('Ctrl Pts',(0.4755900604755,-1.010680324589,-1.700042199688));
#26804=CARTESIAN_POINT('Ctrl Pts',(0.2348081643589,-1.123983684464,-1.719000533021));
#26805=CARTESIAN_POINT('Ctrl Pts',(-0.329952574922,-1.170452920957,-1.756917199688));
#26806=CARTESIAN_POINT('Ctrl Pts',(-1.016551442463,-0.6677408946504,-1.813792199688));
#26807=CARTESIAN_POINT('Ctrl Pts',(-1.205358893105,0.1619074151071,-1.870667199688));
#26808=CARTESIAN_POINT('Ctrl Pts',(-0.8042879589087,0.9122802996697,-1.927542199688));
#26809=CARTESIAN_POINT('Ctrl Pts',(-0.009550993186477,1.216158607898,-1.984417199688));
#26810=CARTESIAN_POINT('Ctrl Pts',(0.7898556864549,0.9248023542725,-2.041292199688));
#26811=CARTESIAN_POINT('Ctrl Pts',(1.202679571961,0.180814804896,-2.098167199688));
#26812=CARTESIAN_POINT('Ctrl Pts',(1.026867975908,-0.6516702524068,-2.155042199688));
#26813=CARTESIAN_POINT('Ctrl Pts',(0.348469933747,-1.165204139133,-2.211917199688));
#26814=CARTESIAN_POINT('Ctrl Pts',(-0.5004819949382,-1.108444747226,-2.268792199688));
#26815=CARTESIAN_POINT('Ctrl Pts',(-1.104479823299,-0.5091721726955,-2.325667199688));
#26816=CARTESIAN_POINT('Ctrl Pts',(-1.167905052019,0.3393077836576,-2.382542199688));
#26817=CARTESIAN_POINT('Ctrl Pts',(-0.6597150647482,1.02171816845,-2.439417199688));
#26818=CARTESIAN_POINT('Ctrl Pts',(0.1713634724997,1.204062516105,-2.496292199688));
#26819=CARTESIAN_POINT('Ctrl Pts',(0.9185704929214,0.7970948701029,-2.553167199688));
#26820=CARTESIAN_POINT('Ctrl Pts',(1.216195700701,0.,-2.610042199688));
#26821=CARTESIAN_POINT('Ctrl Pts',(0.9185704929214,-0.7970948701029,-2.666917199688));
#26822=CARTESIAN_POINT('Ctrl Pts',(0.1713634724997,-1.204062516105,-2.723792199688));
#26823=CARTESIAN_POINT('Ctrl Pts',(-0.6597150647482,-1.02171816845,-2.780667199688));
#26824=CARTESIAN_POINT('Ctrl Pts',(-1.167905052019,-0.3393077836576,-2.837542199688));
#26825=CARTESIAN_POINT('Ctrl Pts',(-1.104479823299,0.5091721726955,-2.894417199688));
#26826=CARTESIAN_POINT('Ctrl Pts',(-0.5004819949382,1.108444747226,-2.951292199688));
#26827=CARTESIAN_POINT('Ctrl Pts',(0.348469933747,1.165204139133,-3.008167199688));
#26828=CARTESIAN_POINT('Ctrl Pts',(1.026867975908,0.6516702524068,-3.065042199688));
#26829=CARTESIAN_POINT('Ctrl Pts',(1.202679571961,-0.180814804896,-3.121917199688));
#26830=CARTESIAN_POINT('Ctrl Pts',(0.7898556864549,-0.9248023542725,-3.178792199688));
#26831=CARTESIAN_POINT('Ctrl Pts',(-0.009550993186476,-1.216158607898,-3.235667199688));
#26832=CARTESIAN_POINT('Ctrl Pts',(-0.8042879589087,-0.9122802996697,-3.292542199688));
#26833=CARTESIAN_POINT('Ctrl Pts',(-1.205358893105,-0.1619074151071,-3.349417199688));
#26834=CARTESIAN_POINT('Ctrl Pts',(-1.016551442463,0.6677408946503,-3.406292199688));
#26835=CARTESIAN_POINT('Ctrl Pts',(-0.329952574922,1.170452920957,-3.463167199688));
#26836=CARTESIAN_POINT('Ctrl Pts',(0.2348081643589,1.123983684464,-3.501083866354));
#26837=CARTESIAN_POINT('Ctrl Pts',(0.4755900604755,1.010680324589,-3.520042199688));
#26838=CARTESIAN_POINT('Ctrl Pts',(0.4755900604755,-1.010680324589,-1.729957800312));
#26839=CARTESIAN_POINT('Ctrl Pts',(0.2348081643589,-1.123983684464,-1.748916133646));
#26840=CARTESIAN_POINT('Ctrl Pts',(-0.329952574922,-1.170452920957,-1.786832800312));
#26841=CARTESIAN_POINT('Ctrl Pts',(-1.016551442463,-0.6677408946504,-1.843707800312));
#26842=CARTESIAN_POINT('Ctrl Pts',(-1.205358893105,0.1619074151071,-1.900582800312));
#26843=CARTESIAN_POINT('Ctrl Pts',(-0.8042879589087,0.9122802996697,-1.957457800312));
#26844=CARTESIAN_POINT('Ctrl Pts',(-0.009550993186478,1.216158607898,-2.014332800312));
#26845=CARTESIAN_POINT('Ctrl Pts',(0.7898556864549,0.9248023542725,-2.071207800312));
#26846=CARTESIAN_POINT('Ctrl Pts',(1.202679571961,0.180814804896,-2.128082800312));
#26847=CARTESIAN_POINT('Ctrl Pts',(1.026867975908,-0.6516702524068,-2.184957800312));
#26848=CARTESIAN_POINT('Ctrl Pts',(0.348469933747,-1.165204139133,-2.241832800312));
#26849=CARTESIAN_POINT('Ctrl Pts',(-0.5004819949382,-1.108444747226,-2.298707800312));
#26850=CARTESIAN_POINT('Ctrl Pts',(-1.104479823299,-0.5091721726955,-2.355582800312));
#26851=CARTESIAN_POINT('Ctrl Pts',(-1.167905052019,0.3393077836576,-2.412457800312));
#26852=CARTESIAN_POINT('Ctrl Pts',(-0.6597150647482,1.02171816845,-2.469332800312));
#26853=CARTESIAN_POINT('Ctrl Pts',(0.1713634724997,1.204062516105,-2.526207800312));
#26854=CARTESIAN_POINT('Ctrl Pts',(0.9185704929214,0.7970948701029,-2.583082800312));
#26855=CARTESIAN_POINT('Ctrl Pts',(1.216195700701,0.,-2.639957800312));
#26856=CARTESIAN_POINT('Ctrl Pts',(0.9185704929214,-0.7970948701029,-2.696832800312));
#26857=CARTESIAN_POINT('Ctrl Pts',(0.1713634724997,-1.204062516105,-2.753707800312));
#26858=CARTESIAN_POINT('Ctrl Pts',(-0.6597150647482,-1.02171816845,-2.810582800312));
#26859=CARTESIAN_POINT('Ctrl Pts',(-1.167905052019,-0.3393077836576,-2.867457800312));
#26860=CARTESIAN_POINT('Ctrl Pts',(-1.104479823299,0.5091721726955,-2.924332800312));
#26861=CARTESIAN_POINT('Ctrl Pts',(-0.5004819949382,1.108444747226,-2.981207800312));
#26862=CARTESIAN_POINT('Ctrl Pts',(0.3484699337469,1.165204139133,-3.038082800312));
#26863=CARTESIAN_POINT('Ctrl Pts',(1.026867975908,0.6516702524068,-3.094957800312));
#26864=CARTESIAN_POINT('Ctrl Pts',(1.202679571961,-0.180814804896,-3.151832800312));
#26865=CARTESIAN_POINT('Ctrl Pts',(0.7898556864549,-0.9248023542725,-3.208707800312));
#26866=CARTESIAN_POINT('Ctrl Pts',(-0.009550993186476,-1.216158607898,-3.265582800312));
#26867=CARTESIAN_POINT('Ctrl Pts',(-0.8042879589087,-0.9122802996697,-3.322457800312));
#26868=CARTESIAN_POINT('Ctrl Pts',(-1.205358893105,-0.1619074151071,-3.379332800312));
#26869=CARTESIAN_POINT('Ctrl Pts',(-1.016551442463,0.6677408946504,-3.436207800312));
#26870=CARTESIAN_POINT('Ctrl Pts',(-0.329952574922,1.170452920957,-3.493082800312));
#26871=CARTESIAN_POINT('Ctrl Pts',(0.2348081643589,1.123983684464,-3.530999466979));
#26872=CARTESIAN_POINT('Ctrl Pts',(0.4755900604755,1.010680324589,-3.549957800312));
#26873=CARTESIAN_POINT('Ctrl Pts',(0.4755900604755,-1.010680324589,-1.759873400937));
#26874=CARTESIAN_POINT('Ctrl Pts',(0.2348081643589,-1.123983684464,-1.77883173427));
#26875=CARTESIAN_POINT('Ctrl Pts',(-0.329952574922,-1.170452920957,-1.816748400937));
#26876=CARTESIAN_POINT('Ctrl Pts',(-1.016551442463,-0.6677408946504,-1.873623400937));
#26877=CARTESIAN_POINT('Ctrl Pts',(-1.205358893105,0.1619074151071,-1.930498400937));
#26878=CARTESIAN_POINT('Ctrl Pts',(-0.8042879589087,0.9122802996697,-1.987373400937));
#26879=CARTESIAN_POINT('Ctrl Pts',(-0.009550993186478,1.216158607898,-2.044248400937));
#26880=CARTESIAN_POINT('Ctrl Pts',(0.7898556864549,0.9248023542725,-2.101123400937));
#26881=CARTESIAN_POINT('Ctrl Pts',(1.202679571961,0.180814804896,-2.157998400937));
#26882=CARTESIAN_POINT('Ctrl Pts',(1.026867975908,-0.6516702524068,-2.214873400937));
#26883=CARTESIAN_POINT('Ctrl Pts',(0.348469933747,-1.165204139133,-2.271748400937));
#26884=CARTESIAN_POINT('Ctrl Pts',(-0.5004819949382,-1.108444747226,-2.328623400937));
#26885=CARTESIAN_POINT('Ctrl Pts',(-1.104479823299,-0.5091721726955,-2.385498400937));
#26886=CARTESIAN_POINT('Ctrl Pts',(-1.167905052019,0.3393077836576,-2.442373400937));
#26887=CARTESIAN_POINT('Ctrl Pts',(-0.6597150647482,1.02171816845,-2.499248400937));
#26888=CARTESIAN_POINT('Ctrl Pts',(0.1713634724997,1.204062516105,-2.556123400937));
#26889=CARTESIAN_POINT('Ctrl Pts',(0.9185704929214,0.7970948701029,-2.612998400937));
#26890=CARTESIAN_POINT('Ctrl Pts',(1.216195700701,0.,-2.669873400937));
#26891=CARTESIAN_POINT('Ctrl Pts',(0.9185704929214,-0.7970948701029,-2.726748400937));
#26892=CARTESIAN_POINT('Ctrl Pts',(0.1713634724997,-1.204062516105,-2.783623400937));
#26893=CARTESIAN_POINT('Ctrl Pts',(-0.6597150647482,-1.02171816845,-2.840498400937));
#26894=CARTESIAN_POINT('Ctrl Pts',(-1.167905052019,-0.3393077836576,-2.897373400937));
#26895=CARTESIAN_POINT('Ctrl Pts',(-1.104479823299,0.5091721726955,-2.954248400937));
#26896=CARTESIAN_POINT('Ctrl Pts',(-0.5004819949382,1.108444747226,-3.011123400937));
#26897=CARTESIAN_POINT('Ctrl Pts',(0.3484699337469,1.165204139133,-3.067998400937));
#26898=CARTESIAN_POINT('Ctrl Pts',(1.026867975908,0.6516702524068,-3.124873400937));
#26899=CARTESIAN_POINT('Ctrl Pts',(1.202679571961,-0.180814804896,-3.181748400937));
#26900=CARTESIAN_POINT('Ctrl Pts',(0.7898556864549,-0.9248023542725,-3.238623400937));
#26901=CARTESIAN_POINT('Ctrl Pts',(-0.009550993186476,-1.216158607898,-3.295498400937));
#26902=CARTESIAN_POINT('Ctrl Pts',(-0.8042879589087,-0.9122802996697,-3.352373400937));
#26903=CARTESIAN_POINT('Ctrl Pts',(-1.205358893105,-0.1619074151071,-3.409248400937));
#26904=CARTESIAN_POINT('Ctrl Pts',(-1.016551442463,0.6677408946504,-3.466123400937));
#26905=CARTESIAN_POINT('Ctrl Pts',(-0.329952574922,1.170452920957,-3.522998400937));
#26906=CARTESIAN_POINT('Ctrl Pts',(0.2348081643589,1.123983684464,-3.560915067604));
#26907=CARTESIAN_POINT('Ctrl Pts',(0.4755900604755,1.010680324589,-3.579873400937));
#26908=CARTESIAN_POINT('',(-3.4898201487235E-10,1.11698717731251,-3.52886751164369));
#26909=CARTESIAN_POINT('',(0.,1.116987298108,-3.471132486541));
#26910=CARTESIAN_POINT('Ctrl Pts',(-1.8872157446454E-6,-1.11628565378659,
-1.77884910577848));
#26911=CARTESIAN_POINT('Ctrl Pts',(-0.0945476136912763,-1.11645975869106,
-1.78558517666919));
#26912=CARTESIAN_POINT('Ctrl Pts',(-0.189124462134139,-1.10484916429063,
-1.79232726977651));
#26913=CARTESIAN_POINT('Ctrl Pts',(-0.372801878429928,-1.05728988862637,
-1.80586972723853));
#26914=CARTESIAN_POINT('Ctrl Pts',(-0.461203748610714,-1.0212041755292,
-1.81262550562908));
#26915=CARTESIAN_POINT('Ctrl Pts',(-0.668471432388827,-0.904915646636025,
-1.82955576649842));
#26916=CARTESIAN_POINT('Ctrl Pts',(-0.780383055419241,-0.811029500761452,
-1.83976498118422));
#26917=CARTESIAN_POINT('Ctrl Pts',(-0.977352549963109,-0.567498199932465,
-1.86210279000144));
#26918=CARTESIAN_POINT('Ctrl Pts',(-1.03703915589554,-0.431145768277838,
-1.87249380692754));
#26919=CARTESIAN_POINT('Ctrl Pts',(-1.11066616674449,-0.178042375581421,
-1.89126431930581));
#26920=CARTESIAN_POINT('Ctrl Pts',(-1.1250370353998,-0.0352369170928321,
-1.90130636574828));
#26921=CARTESIAN_POINT('Ctrl Pts',(-1.09418460733438,0.296790717289773,
-1.92509692704671));
#26922=CARTESIAN_POINT('Ctrl Pts',(-1.02997735713432,0.440477084842074,
-1.93601884316657));
#26923=CARTESIAN_POINT('Ctrl Pts',(-0.925588908242807,0.636392952388529,
-1.95182493170545));
#26924=CARTESIAN_POINT('Ctrl Pts',(-0.840538191683139,0.751460714065266,
-1.96183701528019));
#26925=CARTESIAN_POINT('Ctrl Pts',(-0.61118224779974,0.946513834085734,
-1.98331976958516));
#26926=CARTESIAN_POINT('Ctrl Pts',(-0.478234529751121,1.0191711099922,-1.99390080177507));
#26927=CARTESIAN_POINT('Ctrl Pts',(-0.222597234321247,1.1004636264182,-2.01300274809229));
#26928=CARTESIAN_POINT('Ctrl Pts',(-0.0794663775051977,1.12675755955542,
-2.02317074675688));
#26929=CARTESIAN_POINT('Ctrl Pts',(0.232981315456759,1.10176800386665,-2.04552756527266));
#26930=CARTESIAN_POINT('Ctrl Pts',(0.37770060510901,1.06037143957915,-2.0560369702747));
#26931=CARTESIAN_POINT('Ctrl Pts',(0.604852724324514,0.944731736167629,
-2.07419440550631));
#26932=CARTESIAN_POINT('Ctrl Pts',(0.73133122698844,0.863974006299962,-2.08465639462863));
#26933=CARTESIAN_POINT('Ctrl Pts',(0.943397907937853,0.613934547622003,
-2.1080266301717));
#26934=CARTESIAN_POINT('Ctrl Pts',(1.01607631574406,0.484189787750191,-2.11841215189081));
#26935=CARTESIAN_POINT('Ctrl Pts',(1.11857306467121,0.173002860562993,-2.14176437012636));
#26936=CARTESIAN_POINT('Ctrl Pts',(1.12165266273671,0.0230529286474099,
-2.15222238737627));
#26937=CARTESIAN_POINT('Ctrl Pts',(1.10179845703878,-0.228016486144731,
-2.17016430609243));
#26938=CARTESIAN_POINT('Ctrl Pts',(1.06324590215938,-0.369253565391361,
-2.18039583379269));
#26939=CARTESIAN_POINT('Ctrl Pts',(0.924464855646204,-0.649976757040022,
-2.20272861706242));
#26940=CARTESIAN_POINT('Ctrl Pts',(0.825915661788621,-0.761161572818573,
-2.21310258159157));
#26941=CARTESIAN_POINT('Ctrl Pts',(0.626214316349864,-0.934430304671196,
-2.23193040825594));
#26942=CARTESIAN_POINT('Ctrl Pts',(0.50221499693755,-1.00732385711169,-2.24199298816798));
#26943=CARTESIAN_POINT('Ctrl Pts',(0.191201997533729,-1.11682300306852,
-2.26551693664132));
#26944=CARTESIAN_POINT('Ctrl Pts',(0.0349012702549763,-1.12007370080307,
-2.27638015858152));
#26945=CARTESIAN_POINT('Ctrl Pts',(-0.203851405860729,-1.1061171885703,
-2.29340869558083));
#26946=CARTESIAN_POINT('Ctrl Pts',(-0.341786112597017,-1.07261170247852,
-2.30334911559688));
#26947=CARTESIAN_POINT('Ctrl Pts',(-0.603413551668513,-0.951563052462853,
-2.32391815996146));
#26948=CARTESIAN_POINT('Ctrl Pts',(-0.725113385898934,-0.861211673415836,
-2.33450451982865));
#26949=CARTESIAN_POINT('Ctrl Pts',(-0.905273423514474,-0.663857977873341,
-2.35353245208202));
#26950=CARTESIAN_POINT('Ctrl Pts',(-0.989304020610889,-0.545163021076617,
-2.36369254095246));
#26951=CARTESIAN_POINT('Ctrl Pts',(-1.09791444748826,-0.250846118613211,
-2.38607028582539));
#26952=CARTESIAN_POINT('Ctrl Pts',(-1.12102369397598,-0.101931202388129,
-2.39659192327522));
#26953=CARTESIAN_POINT('Ctrl Pts',(-1.11127472608704,0.152382998725973,
-2.41472029922507));
#26954=CARTESIAN_POINT('Ctrl Pts',(-1.09120934524513,0.300938815206496,
-2.42517036237664));
#26955=CARTESIAN_POINT('Ctrl Pts',(-0.953355092950197,0.598483057720635,
-2.44854743454185));
#26956=CARTESIAN_POINT('Ctrl Pts',(-0.865889506205137,0.719096632405866,
-2.45895154517146));
#26957=CARTESIAN_POINT('Ctrl Pts',(-0.630908211369345,0.938430669099268,
-2.48186059631056));
#26958=CARTESIAN_POINT('Ctrl Pts',(-0.499473987912825,1.00559671816686,
-2.49216596514538));
#26959=CARTESIAN_POINT('Ctrl Pts',(-0.254954649474666,1.09592824110064,
-2.51073734053109));
#26960=CARTESIAN_POINT('Ctrl Pts',(-0.110233508147556,1.12012616746575,
-2.52099044678715));
#26961=CARTESIAN_POINT('Ctrl Pts',(0.202625788977262,1.11169037854405,-2.54330877782005));
#26962=CARTESIAN_POINT('Ctrl Pts',(0.344594062564991,1.06910154094398,-2.55366009735837));
#26963=CARTESIAN_POINT('Ctrl Pts',(0.586363065095521,0.959974916638415,
-2.57255024413075));
#26964=CARTESIAN_POINT('Ctrl Pts',(0.704733656287596,0.877644037487909,
-2.58263575715875));
#26965=CARTESIAN_POINT('Ctrl Pts',(0.924445762808999,0.651144082671885,
-2.60514789486952));
#26966=CARTESIAN_POINT('Ctrl Pts',(0.99587830302718,0.517818669122217,-2.61569215217414));
#26967=CARTESIAN_POINT('Ctrl Pts',(1.08982166380632,0.277939862987316,-2.63403504577381));
#26968=CARTESIAN_POINT('Ctrl Pts',(1.1169872981078,0.139044412854726,-2.64394629670335));
#26969=CARTESIAN_POINT('Ctrl Pts',(1.1169872981078,-0.139044412854725,-2.66378873021465));
#26970=CARTESIAN_POINT('Ctrl Pts',(1.08982166380632,-0.277939862987314,
-2.67369998114575));
#26971=CARTESIAN_POINT('Ctrl Pts',(0.995878303027182,-0.517818669122213,
-2.69204287474531));
#26972=CARTESIAN_POINT('Ctrl Pts',(0.924445762809003,-0.651144082671879,
-2.70258713204978));
#26973=CARTESIAN_POINT('Ctrl Pts',(0.704733656287605,-0.877644037487902,
-2.72509926976052));
#26974=CARTESIAN_POINT('Ctrl Pts',(0.586363065095532,-0.959974916638408,
-2.7351847827886));
#26975=CARTESIAN_POINT('Ctrl Pts',(0.344594062565008,-1.06910154094397,
-2.75407492956103));
#26976=CARTESIAN_POINT('Ctrl Pts',(0.202625788977281,-1.11169037854405,
-2.76442624909944));
#26977=CARTESIAN_POINT('Ctrl Pts',(-0.110233508147534,-1.12012616746575,
-2.78674458013225));
#26978=CARTESIAN_POINT('Ctrl Pts',(-0.254954649474639,-1.09592824110065,
-2.79699768638819));
#26979=CARTESIAN_POINT('Ctrl Pts',(-0.499473987912779,-1.00559671816688,
-2.81556906177376));
#26980=CARTESIAN_POINT('Ctrl Pts',(-0.6309082113693,-0.938430669099301,
-2.82587443060851));
#26981=CARTESIAN_POINT('Ctrl Pts',(-0.865889506205103,-0.719096632405906,
-2.84878348174746));
#26982=CARTESIAN_POINT('Ctrl Pts',(-0.953355092950165,-0.598483057720684,
-2.85918759237696));
#26983=CARTESIAN_POINT('Ctrl Pts',(-1.09120934524511,-0.300938815206566,
-2.88256466454204));
#26984=CARTESIAN_POINT('Ctrl Pts',(-1.11127472608703,-0.15238299872605,
-2.89301472769358));
#26985=CARTESIAN_POINT('Ctrl Pts',(-1.12102369397598,0.101931202388061,
-2.91114310364352));
#26986=CARTESIAN_POINT('Ctrl Pts',(-1.09791444748828,0.250846118613146,
-2.92166474109352));
#26987=CARTESIAN_POINT('Ctrl Pts',(-0.989304020610919,0.545163021076564,
-2.94404248596658));
#26988=CARTESIAN_POINT('Ctrl Pts',(-0.905273423514507,0.663857977873298,
-2.95420257483704));
#26989=CARTESIAN_POINT('Ctrl Pts',(-0.725113385898971,0.861211673415808,
-2.97323050709035));
#26990=CARTESIAN_POINT('Ctrl Pts',(-0.603413551668552,0.951563052462833,
-2.98381686695739));
#26991=CARTESIAN_POINT('Ctrl Pts',(-0.341786112597064,1.07261170247852,
-3.00438591132201));
#26992=CARTESIAN_POINT('Ctrl Pts',(-0.203851405860783,1.10611718857029,
-3.0143263313382));
#26993=CARTESIAN_POINT('Ctrl Pts',(0.0349012702549246,1.12007370080308,
-3.03135486833769));
#26994=CARTESIAN_POINT('Ctrl Pts',(0.191201997533667,1.11682300306852,-3.04221809027818));
#26995=CARTESIAN_POINT('Ctrl Pts',(0.502214996937503,1.00732385711169,-3.06574203875153));
#26996=CARTESIAN_POINT('Ctrl Pts',(0.626214316349839,0.934430304671182,
-3.0758046186634));
#26997=CARTESIAN_POINT('Ctrl Pts',(0.825915661788615,0.761161572818546,
-3.09463244532758));
#26998=CARTESIAN_POINT('Ctrl Pts',(0.924464855646201,0.64997675704,-3.10500640985651));
#26999=CARTESIAN_POINT('Ctrl Pts',(1.06324590215937,0.36925356539136,-3.12733919312616));
#27000=CARTESIAN_POINT('Ctrl Pts',(1.10179845703877,0.228016486144748,-3.13757072082647));
#27001=CARTESIAN_POINT('Ctrl Pts',(1.12165266273671,-0.0230529286473686,
-3.15551263954268));
#27002=CARTESIAN_POINT('Ctrl Pts',(1.11857306467121,-0.173002860562954,
-3.16597065679267));
#27003=CARTESIAN_POINT('Ctrl Pts',(1.01607631574407,-0.484189787750162,
-3.18932287502831));
#27004=CARTESIAN_POINT('Ctrl Pts',(0.94339790793787,-0.613934547621978,
-3.19970839674746));
#27005=CARTESIAN_POINT('Ctrl Pts',(0.731331226988465,-0.86397400629994,
-3.22307863229059));
#27006=CARTESIAN_POINT('Ctrl Pts',(0.604852724324542,-0.944731736167613,
-3.23354062141293));
#27007=CARTESIAN_POINT('Ctrl Pts',(0.377700605109028,-1.06037143957914,
-3.25169805664457));
#27008=CARTESIAN_POINT('Ctrl Pts',(0.232981315456776,-1.10176800386664,
-3.26220746164662));
#27009=CARTESIAN_POINT('Ctrl Pts',(-0.0794663775051832,-1.12675755955542,
-3.28456428016241));
#27010=CARTESIAN_POINT('Ctrl Pts',(-0.222597234321235,-1.1004636264182,
-3.294732278827));
#27011=CARTESIAN_POINT('Ctrl Pts',(-0.47823452975111,-1.0191711099922,-3.31383422514422));
#27012=CARTESIAN_POINT('Ctrl Pts',(-0.61118224779973,-0.946513834085741,
-3.32441525733414));
#27013=CARTESIAN_POINT('Ctrl Pts',(-0.840538191683135,-0.751460714065271,
-3.345898011639));
#27014=CARTESIAN_POINT('Ctrl Pts',(-0.9255889082428,-0.636392952388535,
-3.3559100952136));
#27015=CARTESIAN_POINT('Ctrl Pts',(-1.02997735713433,-0.440477084842065,
-3.37171618375233));
#27016=CARTESIAN_POINT('Ctrl Pts',(-1.09418460733438,-0.296790717289765,
-3.38263809987196));
#27017=CARTESIAN_POINT('Ctrl Pts',(-1.1250370353998,0.0352369170928032,
-3.40642866117045));
#27018=CARTESIAN_POINT('Ctrl Pts',(-1.11066616674449,0.178042375581391,
-3.41647070761312));
#27019=CARTESIAN_POINT('Ctrl Pts',(-1.03703915589555,0.431145768277807,
-3.4352412199916));
#27020=CARTESIAN_POINT('Ctrl Pts',(-0.977352549963121,0.567498199932441,
-3.44563223691794));
#27021=CARTESIAN_POINT('Ctrl Pts',(-0.78038305541925,0.811029500761437,
-3.46797004573511));
#27022=CARTESIAN_POINT('Ctrl Pts',(-0.668471432388838,0.904915646636014,
-3.47817926042074));
#27023=CARTESIAN_POINT('Ctrl Pts',(-0.461203748610943,1.02120417552907,
-3.49510952128985));
#27024=CARTESIAN_POINT('Ctrl Pts',(-0.372801878430417,1.05728988862616,
-3.50186529968027));
#27025=CARTESIAN_POINT('Ctrl Pts',(-0.189124507262864,1.1048491526056,-3.51540775381488));
#27026=CARTESIAN_POINT('Ctrl Pts',(-0.0945477069597182,1.11645974724111,
-3.52214984360044));
#27027=CARTESIAN_POINT('Ctrl Pts',(-2.02707199615241E-6,1.11628565404413,
-3.52888591117587));
#27028=CARTESIAN_POINT('Ctrl Pts',(0.4696881186261,-0.9981380597272,-1.735864569721));
#27029=CARTESIAN_POINT('Ctrl Pts',(0.2318942596183,-1.110035356068,-1.754822903054));
#27030=CARTESIAN_POINT('Ctrl Pts',(-0.3258579542137,-1.155927922117,-1.792739569721));
#27031=CARTESIAN_POINT('Ctrl Pts',(-1.003936318643,-0.6594544137959,-1.849614569721));
#27032=CARTESIAN_POINT('Ctrl Pts',(-1.190400720751,0.1598981886148,-1.906489569721));
#27033=CARTESIAN_POINT('Ctrl Pts',(-0.7943069665412,0.9009591520544,-1.963364569721));
#27034=CARTESIAN_POINT('Ctrl Pts',(-0.009432467987834,1.201066414053,-2.020239569721));
#27035=CARTESIAN_POINT('Ctrl Pts',(0.7800537946193,0.9133258114035,-2.077114569721));
#27036=CARTESIAN_POINT('Ctrl Pts',(1.187754649245,0.1785709428966,-2.133989569721));
#27037=CARTESIAN_POINT('Ctrl Pts',(1.014124826746,-0.6435832038027,-2.190864569721));
#27038=CARTESIAN_POINT('Ctrl Pts',(0.3441455177085,-1.150744276231,-2.247739569721));
#27039=CARTESIAN_POINT('Ctrl Pts',(-0.4942711510281,-1.094689252768,-2.304614569721));
#27040=CARTESIAN_POINT('Ctrl Pts',(-1.090773532456,-0.5028534860695,-2.361489569721));
#27041=CARTESIAN_POINT('Ctrl Pts',(-1.153411671532,0.3350970673819,-2.418364569721));
#27042=CARTESIAN_POINT('Ctrl Pts',(-0.6515281822355,1.009038926982,-2.475239569721));
#27043=CARTESIAN_POINT('Ctrl Pts',(0.169236898936,1.189120431432,-2.532114569721));
#27044=CARTESIAN_POINT('Ctrl Pts',(0.9071712857378,0.7872031419892,-2.588989569721));
#27045=CARTESIAN_POINT('Ctrl Pts',(1.201103046544,0.,-2.645864569721));
#27046=CARTESIAN_POINT('Ctrl Pts',(0.9071712857378,-0.7872031419892,-2.702739569721));
#27047=CARTESIAN_POINT('Ctrl Pts',(0.169236898936,-1.189120431432,-2.759614569721));
#27048=CARTESIAN_POINT('Ctrl Pts',(-0.6515281822355,-1.009038926982,-2.816489569721));
#27049=CARTESIAN_POINT('Ctrl Pts',(-1.153411671532,-0.3350970673819,-2.873364569721));
#27050=CARTESIAN_POINT('Ctrl Pts',(-1.090773532456,0.5028534860695,-2.930239569721));
#27051=CARTESIAN_POINT('Ctrl Pts',(-0.4942711510281,1.094689252768,-2.987114569721));
#27052=CARTESIAN_POINT('Ctrl Pts',(0.3441455177085,1.150744276231,-3.043989569721));
#27053=CARTESIAN_POINT('Ctrl Pts',(1.014124826746,0.6435832038027,-3.100864569721));
#27054=CARTESIAN_POINT('Ctrl Pts',(1.187754649245,-0.1785709428966,-3.157739569721));
#27055=CARTESIAN_POINT('Ctrl Pts',(0.7800537946193,-0.9133258114035,-3.214614569721));
#27056=CARTESIAN_POINT('Ctrl Pts',(-0.009432467987832,-1.201066414053,-3.271489569721));
#27057=CARTESIAN_POINT('Ctrl Pts',(-0.7943069665412,-0.9009591520544,-3.328364569721));
#27058=CARTESIAN_POINT('Ctrl Pts',(-1.190400720751,-0.1598981886148,-3.385239569721));
#27059=CARTESIAN_POINT('Ctrl Pts',(-1.003936318643,0.6594544137959,-3.442114569721));
#27060=CARTESIAN_POINT('Ctrl Pts',(-0.3258579542138,1.155927922117,-3.498989569721));
#27061=CARTESIAN_POINT('Ctrl Pts',(0.2318942596183,1.110035356068,-3.536906236387));
#27062=CARTESIAN_POINT('Ctrl Pts',(0.4696881186261,0.9981380597272,-3.555864569721));
#27063=CARTESIAN_POINT('Ctrl Pts',(0.5279823721497,-1.122019654338,-1.814910694393));
#27064=CARTESIAN_POINT('Ctrl Pts',(0.2606752788197,-1.247804824574,-1.833869027727));
#27065=CARTESIAN_POINT('Ctrl Pts',(-0.3663010598456,-1.299393240218,-1.871785694393));
#27066=CARTESIAN_POINT('Ctrl Pts',(-1.128537550737,-0.7413010717389,-1.928660694393));
#27067=CARTESIAN_POINT('Ctrl Pts',(-1.33814455045,0.1797435821333,-1.985535694393));
#27068=CARTESIAN_POINT('Ctrl Pts',(-0.892890536887,1.012779611507,-2.042410694393));
#27069=CARTESIAN_POINT('Ctrl Pts',(-0.01060315691615,1.350133991585,-2.099285694393));
#27070=CARTESIAN_POINT('Ctrl Pts',(0.8768683655278,1.026681130153,-2.156160694393));
#27071=CARTESIAN_POINT('Ctrl Pts',(1.335170067905,0.2007338620856,-2.213035694393));
#27072=CARTESIAN_POINT('Ctrl Pts',(1.139990581936,-0.723460043259,-2.269910694393));
#27073=CARTESIAN_POINT('Ctrl Pts',(0.3868583419482,-1.293566238123,-2.326785694393));
#27074=CARTESIAN_POINT('Ctrl Pts',(-0.555616470709,-1.230554075189,-2.383660694393));
#27075=CARTESIAN_POINT('Ctrl Pts',(-1.226152364316,-0.5652639823961,-2.440535694393));
#27076=CARTESIAN_POINT('Ctrl Pts',(-1.296564691016,0.3766868641562,-2.497410694393));
#27077=CARTESIAN_POINT('Ctrl Pts',(-0.7323910942975,1.134273457497,-2.554285694393));
#27078=CARTESIAN_POINT('Ctrl Pts',(0.190241344867,1.336705360987,-2.611160694393));
#27079=CARTESIAN_POINT('Ctrl Pts',(1.019762749782,0.8849050375959,-2.668035694393));
#27080=CARTESIAN_POINT('Ctrl Pts',(1.350175170634,0.,-2.724910694393));
#27081=CARTESIAN_POINT('Ctrl Pts',(1.019762749782,-0.8849050375959,-2.781785694393));
#27082=CARTESIAN_POINT('Ctrl Pts',(0.190241344867,-1.336705360987,-2.838660694393));
#27083=CARTESIAN_POINT('Ctrl Pts',(-0.7323910942975,-1.134273457497,-2.895535694393));
#27084=CARTESIAN_POINT('Ctrl Pts',(-1.296564691016,-0.3766868641562,-2.952410694393));
#27085=CARTESIAN_POINT('Ctrl Pts',(-1.226152364316,0.5652639823961,-3.009285694393));
#27086=CARTESIAN_POINT('Ctrl Pts',(-0.555616470709,1.230554075189,-3.066160694393));
#27087=CARTESIAN_POINT('Ctrl Pts',(0.3868583419482,1.293566238123,-3.123035694393));
#27088=CARTESIAN_POINT('Ctrl Pts',(1.139990581936,0.723460043259,-3.179910694393));
#27089=CARTESIAN_POINT('Ctrl Pts',(1.335170067905,-0.2007338620856,-3.236785694393));
#27090=CARTESIAN_POINT('Ctrl Pts',(0.8768683655278,-1.026681130153,-3.293660694393));
#27091=CARTESIAN_POINT('Ctrl Pts',(-0.01060315691615,-1.350133991585,-3.350535694393));
#27092=CARTESIAN_POINT('Ctrl Pts',(-0.892890536887,-1.012779611507,-3.407410694393));
#27093=CARTESIAN_POINT('Ctrl Pts',(-1.33814455045,-0.1797435821333,-3.464285694393));
#27094=CARTESIAN_POINT('Ctrl Pts',(-1.128537550737,0.7413010717389,-3.521160694393));
#27095=CARTESIAN_POINT('Ctrl Pts',(-0.3663010598456,1.299393240218,-3.578035694393));
#27096=CARTESIAN_POINT('Ctrl Pts',(0.2606752788197,1.247804824574,-3.61595236106));
#27097=CARTESIAN_POINT('Ctrl Pts',(0.5279823721497,1.122019654338,-3.634910694393));
#27098=CARTESIAN_POINT('Ctrl Pts',(0.5862766256734,-1.24590124895,-1.893956819066));
#27099=CARTESIAN_POINT('Ctrl Pts',(0.2894562980212,-1.38557429308,-1.912915152399));
#27100=CARTESIAN_POINT('Ctrl Pts',(-0.4067441654775,-1.442858558319,-1.950831819066));
#27101=CARTESIAN_POINT('Ctrl Pts',(-1.253138782831,-0.823147729682,-2.007706819066));
#27102=CARTESIAN_POINT('Ctrl Pts',(-1.48588838015,0.1995889756518,-2.064581819066));
#27103=CARTESIAN_POINT('Ctrl Pts',(-0.9914741072328,1.12460007096,-2.121456819066));
#27104=CARTESIAN_POINT('Ctrl Pts',(-0.01177384584446,1.499201569118,-2.178331819066));
#27105=CARTESIAN_POINT('Ctrl Pts',(0.9736829364363,1.140036448902,-2.235206819066));
#27106=CARTESIAN_POINT('Ctrl Pts',(1.482585486565,0.2228967812747,-2.292081819066));
#27107=CARTESIAN_POINT('Ctrl Pts',(1.265856337127,-0.8033368827153,-2.348956819066));
#27108=CARTESIAN_POINT('Ctrl Pts',(0.4295711661878,-1.436388200015,-2.405831819066));
#27109=CARTESIAN_POINT('Ctrl Pts',(-0.61696179039,-1.36641889761,-2.462706819066));
#27110=CARTESIAN_POINT('Ctrl Pts',(-1.361531196175,-0.6276744787227,-2.519581819066));
#27111=CARTESIAN_POINT('Ctrl Pts',(-1.439717710501,0.4182766609306,-2.576456819066));
#27112=CARTESIAN_POINT('Ctrl Pts',(-0.8132540063595,1.259507988013,-2.633331819066));
#27113=CARTESIAN_POINT('Ctrl Pts',(0.211245790798,1.484290290542,-2.690206819066));
#27114=CARTESIAN_POINT('Ctrl Pts',(1.132354213826,0.9826069332027,-2.747081819066));
#27115=CARTESIAN_POINT('Ctrl Pts',(1.499247294724,0.,-2.803956819066));
#27116=CARTESIAN_POINT('Ctrl Pts',(1.132354213826,-0.9826069332027,-2.860831819066));
#27117=CARTESIAN_POINT('Ctrl Pts',(0.211245790798,-1.484290290542,-2.917706819066));
#27118=CARTESIAN_POINT('Ctrl Pts',(-0.8132540063595,-1.259507988013,-2.974581819066));
#27119=CARTESIAN_POINT('Ctrl Pts',(-1.439717710501,-0.4182766609306,-3.031456819066));
#27120=CARTESIAN_POINT('Ctrl Pts',(-1.361531196175,0.6276744787227,-3.088331819066));
#27121=CARTESIAN_POINT('Ctrl Pts',(-0.61696179039,1.36641889761,-3.145206819066));
#27122=CARTESIAN_POINT('Ctrl Pts',(0.4295711661878,1.436388200015,-3.202081819066));
#27123=CARTESIAN_POINT('Ctrl Pts',(1.265856337127,0.8033368827153,-3.258956819066));
#27124=CARTESIAN_POINT('Ctrl Pts',(1.482585486565,-0.2228967812747,-3.315831819066));
#27125=CARTESIAN_POINT('Ctrl Pts',(0.9736829364363,-1.140036448902,-3.372706819066));
#27126=CARTESIAN_POINT('Ctrl Pts',(-0.01177384584446,-1.499201569118,-3.429581819066));
#27127=CARTESIAN_POINT('Ctrl Pts',(-0.9914741072328,-1.12460007096,-3.486456819066));
#27128=CARTESIAN_POINT('Ctrl Pts',(-1.48588838015,-0.1995889756517,-3.543331819066));
#27129=CARTESIAN_POINT('Ctrl Pts',(-1.253138782831,0.823147729682,-3.600206819066));
#27130=CARTESIAN_POINT('Ctrl Pts',(-0.4067441654775,1.442858558319,-3.657081819066));
#27131=CARTESIAN_POINT('Ctrl Pts',(0.2894562980212,1.38557429308,-3.694998485733));
#27132=CARTESIAN_POINT('Ctrl Pts',(0.5862766256734,1.24590124895,-3.713956819066));
#27133=CARTESIAN_POINT('Ctrl Pts',(0.644570879197,-1.369782843561,-1.973002943739));
#27134=CARTESIAN_POINT('Ctrl Pts',(0.3182373172226,-1.523343761587,-1.991961277072));
#27135=CARTESIAN_POINT('Ctrl Pts',(-0.4471872711094,-1.586323876419,-2.029877943739));
#27136=CARTESIAN_POINT('Ctrl Pts',(-1.377740014924,-0.904994387625,-2.086752943739));
#27137=CARTESIAN_POINT('Ctrl Pts',(-1.633632209849,0.2194343691702,-2.143627943739));
#27138=CARTESIAN_POINT('Ctrl Pts',(-1.090057677579,1.236420530413,-2.200502943739));
#27139=CARTESIAN_POINT('Ctrl Pts',(-0.01294453477278,1.648269146651,-2.257377943739));
#27140=CARTESIAN_POINT('Ctrl Pts',(1.070497507345,1.253391767652,-2.314252943739));
#27141=CARTESIAN_POINT('Ctrl Pts',(1.630000905225,0.2450597004638,-2.371127943739));
#27142=CARTESIAN_POINT('Ctrl Pts',(1.391722092318,-0.8832137221716,-2.428002943739));
#27143=CARTESIAN_POINT('Ctrl Pts',(0.4722839904274,-1.579210161907,-2.484877943739));
#27144=CARTESIAN_POINT('Ctrl Pts',(-0.6783071100709,-1.502283720031,-2.541752943739));
#27145=CARTESIAN_POINT('Ctrl Pts',(-1.496910028035,-0.6900849750494,-2.598627943739));
#27146=CARTESIAN_POINT('Ctrl Pts',(-1.582870729986,0.4598664577049,-2.655502943739));
#27147=CARTESIAN_POINT('Ctrl Pts',(-0.8941169184215,1.384742518528,-2.712377943739));
#27148=CARTESIAN_POINT('Ctrl Pts',(0.232250236729,1.631875220096,-2.769252943739));
#27149=CARTESIAN_POINT('Ctrl Pts',(1.24494567787,1.080308828809,-2.826127943739));
#27150=CARTESIAN_POINT('Ctrl Pts',(1.648319418813,0.,-2.883002943739));
#27151=CARTESIAN_POINT('Ctrl Pts',(1.24494567787,-1.080308828809,-2.939877943739));
#27152=CARTESIAN_POINT('Ctrl Pts',(0.232250236729,-1.631875220096,-2.996752943739));
#27153=CARTESIAN_POINT('Ctrl Pts',(-0.8941169184215,-1.384742518528,-3.053627943739));
#27154=CARTESIAN_POINT('Ctrl Pts',(-1.582870729986,-0.4598664577049,-3.110502943739));
#27155=CARTESIAN_POINT('Ctrl Pts',(-1.496910028035,0.6900849750494,-3.167377943739));
#27156=CARTESIAN_POINT('Ctrl Pts',(-0.6783071100709,1.502283720031,-3.224252943739));
#27157=CARTESIAN_POINT('Ctrl Pts',(0.4722839904274,1.579210161907,-3.281127943739));
#27158=CARTESIAN_POINT('Ctrl Pts',(1.391722092318,0.8832137221716,-3.338002943739));
#27159=CARTESIAN_POINT('Ctrl Pts',(1.630000905225,-0.2450597004638,-3.394877943739));
#27160=CARTESIAN_POINT('Ctrl Pts',(1.070497507345,-1.253391767652,-3.451752943739));
#27161=CARTESIAN_POINT('Ctrl Pts',(-0.01294453477277,-1.648269146651,-3.508627943739));
#27162=CARTESIAN_POINT('Ctrl Pts',(-1.090057677579,-1.236420530413,-3.565502943739));
#27163=CARTESIAN_POINT('Ctrl Pts',(-1.633632209849,-0.2194343691702,-3.622377943739));
#27164=CARTESIAN_POINT('Ctrl Pts',(-1.377740014924,0.904994387625,-3.679252943739));
#27165=CARTESIAN_POINT('Ctrl Pts',(-0.4471872711094,1.586323876419,-3.736127943739));
#27166=CARTESIAN_POINT('Ctrl Pts',(0.3182373172226,1.523343761587,-3.774044610405));
#27167=CARTESIAN_POINT('Ctrl Pts',(0.644570879197,1.369782843561,-3.793002943739));
#27168=CARTESIAN_POINT('',(-1.98293436576097E-9,1.49923261688451,-3.74955700104142));
#27169=CARTESIAN_POINT('',(0.,1.116987298108,-3.528867513459));
#27170=CARTESIAN_POINT('Ctrl Pts',(-2.23097736339398E-5,1.49898153286063,
-3.74997329818232));
#27171=CARTESIAN_POINT('Ctrl Pts',(-0.134297990364599,1.49921292012494,
-3.74284084449308));
#27172=CARTESIAN_POINT('Ctrl Pts',(-0.268638579334411,1.4817717682223,-3.73571955672579));
#27173=CARTESIAN_POINT('Ctrl Pts',(-0.528263299353071,1.41043848354384,
-3.7214835046435));
#27174=CARTESIAN_POINT('Ctrl Pts',(-0.652764717085495,1.35640654604196,
-3.71435338885275));
#27175=CARTESIAN_POINT('Ctrl Pts',(-0.93173523235398,1.1891402211788,-3.69707781285224));
#27176=CARTESIAN_POINT('Ctrl Pts',(-1.07750856874978,1.05993244186351,-3.68689192394793));
#27177=CARTESIAN_POINT('Ctrl Pts',(-1.25254458058096,0.831135438061306,
-3.67160665077089));
#27178=CARTESIAN_POINT('Ctrl Pts',(-1.30304061564861,0.74921731834058,-3.66653951792222));
#27179=CARTESIAN_POINT('Ctrl Pts',(-1.43181232730633,0.485623094910584,
-3.65097008072865));
#27180=CARTESIAN_POINT('Ctrl Pts',(-1.48316632248211,0.291366952803233,
-3.64048349674964));
#27181=CARTESIAN_POINT('Ctrl Pts',(-1.50934594069338,-0.102298203372775,
-3.61953593410385));
#27182=CARTESIAN_POINT('Ctrl Pts',(-1.48352322466648,-0.297075624561851,
-3.60935212892794));
#27183=CARTESIAN_POINT('Ctrl Pts',(-1.35557800746622,-0.667978453013121,
-3.58851892695713));
#27184=CARTESIAN_POINT('Ctrl Pts',(-1.25672305133621,-0.839706849423558,
-3.57816968266589));
#27185=CARTESIAN_POINT('Ctrl Pts',(-1.06762968939388,-1.05767327012927,
-3.5628546682347));
#27186=CARTESIAN_POINT('Ctrl Pts',(-0.999122949219283,-1.12299757074587,
-3.55786874093753));
#27187=CARTESIAN_POINT('Ctrl Pts',(-0.767475932851098,-1.30345310761049,
-3.54230752101967));
#27188=CARTESIAN_POINT('Ctrl Pts',(-0.585984095946929,-1.39346685040132,
-3.53173765623922));
#27189=CARTESIAN_POINT('Ctrl Pts',(-0.300277764313124,-1.47207219521031,
-3.51599600554029));
#27190=CARTESIAN_POINT('Ctrl Pts',(-0.203413451744069,-1.48897913532964,
-3.51079851028164));
#27191=CARTESIAN_POINT('Ctrl Pts',(-0.0102966124493356,-1.50310836142732,
-3.50053281146868));
#27192=CARTESIAN_POINT('Ctrl Pts',(0.0847306681168998,-1.50057826174177,
-3.49552882854339));
#27193=CARTESIAN_POINT('Ctrl Pts',(0.371065755655233,-1.46518483944735,
-3.48022026878835));
#27194=CARTESIAN_POINT('Ctrl Pts',(0.558528693198532,-1.4040395721907,-3.46992086661752));
#27195=CARTESIAN_POINT('Ctrl Pts',(0.90153284875694,-1.21492375687663,-3.44911971811302));
#27196=CARTESIAN_POINT('Ctrl Pts',(1.05210335279266,-1.08744425337218,-3.43889366904479));
#27197=CARTESIAN_POINT('Ctrl Pts',(1.29645238593754,-0.777009497911457,
-3.41791551601252));
#27198=CARTESIAN_POINT('Ctrl Pts',(1.38796572683809,-0.59897640207039,-3.40746395634614));
#27199=CARTESIAN_POINT('Ctrl Pts',(1.49653070285487,-0.222284526241667,
-3.38665963898178));
#27200=CARTESIAN_POINT('Ctrl Pts',(1.51209522337162,-0.030383558262909,
-3.37667624280134));
#27201=CARTESIAN_POINT('Ctrl Pts',(1.46756784636134,0.362285640434857,-3.35568821166625));
#27202=CARTESIAN_POINT('Ctrl Pts',(1.4068673977224,0.555204171359176,-3.34513613647265));
#27203=CARTESIAN_POINT('Ctrl Pts',(1.2647554046479,0.812299723145478,-3.32955745876526));
#27204=CARTESIAN_POINT('Ctrl Pts',(1.21076623735938,0.890422663210658,-3.32455458934434));
#27205=CARTESIAN_POINT('Ctrl Pts',(1.02479816055779,1.11092233383098,-3.30923718460512));
#27206=CARTESIAN_POINT('Ctrl Pts',(0.871086100543727,1.23469586808278,-3.29892246712298));
#27207=CARTESIAN_POINT('Ctrl Pts',(0.593490819192611,1.38245304443696,-3.28222967441605));
#27208=CARTESIAN_POINT('Ctrl Pts',(0.479555239505383,1.42667704405794,-3.27581122112143));
#27209=CARTESIAN_POINT('Ctrl Pts',(0.242844402015829,1.48495859802652,-3.26291338963858));
#27210=CARTESIAN_POINT('Ctrl Pts',(0.121403313286431,1.49919069968979,-3.25647421623353));
#27211=CARTESIAN_POINT('Ctrl Pts',(2.23097736028535E-5,1.49898153286063,
-3.25002670181768));
#27212=CARTESIAN_POINT('Ctrl Pts',(-0.644570879197,1.369782843561,-3.206997056261));
#27213=CARTESIAN_POINT('Ctrl Pts',(-0.3182373172226,1.523343761587,-3.225955389595));
#27214=CARTESIAN_POINT('Ctrl Pts',(0.4471872711094,1.586323876419,-3.263872056261));
#27215=CARTESIAN_POINT('Ctrl Pts',(1.377740014924,0.904994387625,-3.320747056261));
#27216=CARTESIAN_POINT('Ctrl Pts',(1.633632209849,-0.2194343691702,-3.377622056261));
#27217=CARTESIAN_POINT('Ctrl Pts',(1.090057677579,-1.236420530413,-3.434497056261));
#27218=CARTESIAN_POINT('Ctrl Pts',(0.01294453477278,-1.648269146651,-3.491372056261));
#27219=CARTESIAN_POINT('Ctrl Pts',(-1.070497507345,-1.253391767652,-3.548247056261));
#27220=CARTESIAN_POINT('Ctrl Pts',(-1.630000905225,-0.2450597004638,-3.605122056261));
#27221=CARTESIAN_POINT('Ctrl Pts',(-1.391722092318,0.8832137221716,-3.661997056261));
#27222=CARTESIAN_POINT('Ctrl Pts',(-0.4722839904274,1.579210161907,-3.718872056261));
#27223=CARTESIAN_POINT('Ctrl Pts',(0.6783071100709,1.502283720031,-3.775747056261));
#27224=CARTESIAN_POINT('Ctrl Pts',(1.496910028035,0.6900849750494,-3.832622056261));
#27225=CARTESIAN_POINT('Ctrl Pts',(1.582870729986,-0.4598664577049,-3.889497056261));
#27226=CARTESIAN_POINT('Ctrl Pts',(0.8941169184216,-1.384742518528,-3.946372056261));
#27227=CARTESIAN_POINT('Ctrl Pts',(-0.232250236729,-1.631875220096,-4.003247056261));
#27228=CARTESIAN_POINT('Ctrl Pts',(-1.24494567787,-1.080308828809,-4.060122056261));
#27229=CARTESIAN_POINT('Ctrl Pts',(-1.648319418813,0.,-4.116997056261));
#27230=CARTESIAN_POINT('Ctrl Pts',(-1.24494567787,1.080308828809,-4.173872056261));
#27231=CARTESIAN_POINT('Ctrl Pts',(-0.232250236729,1.631875220096,-4.230747056261));
#27232=CARTESIAN_POINT('Ctrl Pts',(0.8941169184215,1.384742518528,-4.287622056261));
#27233=CARTESIAN_POINT('Ctrl Pts',(1.582870729986,0.4598664577049,-4.344497056261));
#27234=CARTESIAN_POINT('Ctrl Pts',(1.496910028035,-0.6900849750494,-4.401372056261));
#27235=CARTESIAN_POINT('Ctrl Pts',(0.6783071100709,-1.502283720031,-4.458247056261));
#27236=CARTESIAN_POINT('Ctrl Pts',(-0.4722839904274,-1.579210161907,-4.515122056261));
#27237=CARTESIAN_POINT('Ctrl Pts',(-1.391722092318,-0.8832137221716,-4.571997056261));
#27238=CARTESIAN_POINT('Ctrl Pts',(-1.630000905225,0.2450597004637,-4.628872056261));
#27239=CARTESIAN_POINT('Ctrl Pts',(-1.070497507345,1.253391767652,-4.685747056261));
#27240=CARTESIAN_POINT('Ctrl Pts',(0.01294453477278,1.648269146651,-4.742622056261));
#27241=CARTESIAN_POINT('Ctrl Pts',(1.090057677579,1.236420530413,-4.799497056261));
#27242=CARTESIAN_POINT('Ctrl Pts',(1.633632209849,0.2194343691702,-4.856372056261));
#27243=CARTESIAN_POINT('Ctrl Pts',(1.377740014924,-0.904994387625,-4.913247056261));
#27244=CARTESIAN_POINT('Ctrl Pts',(0.4471872711094,-1.586323876419,-4.970122056261));
#27245=CARTESIAN_POINT('Ctrl Pts',(-0.3182373172226,-1.523343761587,-5.008038722928));
#27246=CARTESIAN_POINT('Ctrl Pts',(-0.644570879197,-1.369782843561,-5.026997056261));
#27247=CARTESIAN_POINT('Ctrl Pts',(-0.5862766256734,1.24590124895,-3.286043180934));
#27248=CARTESIAN_POINT('Ctrl Pts',(-0.2894562980212,1.38557429308,-3.305001514267));
#27249=CARTESIAN_POINT('Ctrl Pts',(0.4067441654775,1.442858558319,-3.342918180934));
#27250=CARTESIAN_POINT('Ctrl Pts',(1.253138782831,0.823147729682,-3.399793180934));
#27251=CARTESIAN_POINT('Ctrl Pts',(1.48588838015,-0.1995889756518,-3.456668180934));
#27252=CARTESIAN_POINT('Ctrl Pts',(0.9914741072328,-1.12460007096,-3.513543180934));
#27253=CARTESIAN_POINT('Ctrl Pts',(0.01177384584447,-1.499201569118,-3.570418180934));
#27254=CARTESIAN_POINT('Ctrl Pts',(-0.9736829364363,-1.140036448902,-3.627293180934));
#27255=CARTESIAN_POINT('Ctrl Pts',(-1.482585486565,-0.2228967812747,-3.684168180934));
#27256=CARTESIAN_POINT('Ctrl Pts',(-1.265856337127,0.8033368827153,-3.741043180934));
#27257=CARTESIAN_POINT('Ctrl Pts',(-0.4295711661878,1.436388200015,-3.797918180934));
#27258=CARTESIAN_POINT('Ctrl Pts',(0.61696179039,1.36641889761,-3.854793180934));
#27259=CARTESIAN_POINT('Ctrl Pts',(1.361531196175,0.6276744787227,-3.911668180934));
#27260=CARTESIAN_POINT('Ctrl Pts',(1.439717710501,-0.4182766609306,-3.968543180934));
#27261=CARTESIAN_POINT('Ctrl Pts',(0.8132540063595,-1.259507988013,-4.025418180934));
#27262=CARTESIAN_POINT('Ctrl Pts',(-0.211245790798,-1.484290290542,-4.082293180934));
#27263=CARTESIAN_POINT('Ctrl Pts',(-1.132354213826,-0.9826069332027,-4.139168180934));
#27264=CARTESIAN_POINT('Ctrl Pts',(-1.499247294724,0.,-4.196043180934));
#27265=CARTESIAN_POINT('Ctrl Pts',(-1.132354213826,0.9826069332027,-4.252918180934));
#27266=CARTESIAN_POINT('Ctrl Pts',(-0.211245790798,1.484290290542,-4.309793180934));
#27267=CARTESIAN_POINT('Ctrl Pts',(0.8132540063595,1.259507988013,-4.366668180934));
#27268=CARTESIAN_POINT('Ctrl Pts',(1.439717710501,0.4182766609306,-4.423543180934));
#27269=CARTESIAN_POINT('Ctrl Pts',(1.361531196175,-0.6276744787227,-4.480418180934));
#27270=CARTESIAN_POINT('Ctrl Pts',(0.61696179039,-1.36641889761,-4.537293180934));
#27271=CARTESIAN_POINT('Ctrl Pts',(-0.4295711661878,-1.436388200015,-4.594168180934));
#27272=CARTESIAN_POINT('Ctrl Pts',(-1.265856337127,-0.8033368827153,-4.651043180934));
#27273=CARTESIAN_POINT('Ctrl Pts',(-1.482585486565,0.2228967812747,-4.707918180934));
#27274=CARTESIAN_POINT('Ctrl Pts',(-0.9736829364363,1.140036448902,-4.764793180934));
#27275=CARTESIAN_POINT('Ctrl Pts',(0.01177384584446,1.499201569118,-4.821668180934));
#27276=CARTESIAN_POINT('Ctrl Pts',(0.9914741072328,1.12460007096,-4.878543180934));
#27277=CARTESIAN_POINT('Ctrl Pts',(1.48588838015,0.1995889756517,-4.935418180934));
#27278=CARTESIAN_POINT('Ctrl Pts',(1.253138782831,-0.823147729682,-4.992293180934));
#27279=CARTESIAN_POINT('Ctrl Pts',(0.4067441654775,-1.442858558319,-5.049168180934));
#27280=CARTESIAN_POINT('Ctrl Pts',(-0.2894562980212,-1.38557429308,-5.087084847601));
#27281=CARTESIAN_POINT('Ctrl Pts',(-0.5862766256734,-1.24590124895,-5.106043180934));
#27282=CARTESIAN_POINT('Ctrl Pts',(-0.5279823721497,1.122019654338,-3.365089305607));
#27283=CARTESIAN_POINT('Ctrl Pts',(-0.2606752788197,1.247804824574,-3.38404763894));
#27284=CARTESIAN_POINT('Ctrl Pts',(0.3663010598456,1.299393240218,-3.421964305607));
#27285=CARTESIAN_POINT('Ctrl Pts',(1.128537550737,0.7413010717389,-3.478839305607));
#27286=CARTESIAN_POINT('Ctrl Pts',(1.33814455045,-0.1797435821333,-3.535714305607));
#27287=CARTESIAN_POINT('Ctrl Pts',(0.892890536887,-1.012779611507,-3.592589305607));
#27288=CARTESIAN_POINT('Ctrl Pts',(0.01060315691615,-1.350133991585,-3.649464305607));
#27289=CARTESIAN_POINT('Ctrl Pts',(-0.8768683655278,-1.026681130153,-3.706339305607));
#27290=CARTESIAN_POINT('Ctrl Pts',(-1.335170067905,-0.2007338620856,-3.763214305607));
#27291=CARTESIAN_POINT('Ctrl Pts',(-1.139990581936,0.723460043259,-3.820089305607));
#27292=CARTESIAN_POINT('Ctrl Pts',(-0.3868583419482,1.293566238123,-3.876964305607));
#27293=CARTESIAN_POINT('Ctrl Pts',(0.555616470709,1.230554075189,-3.933839305607));
#27294=CARTESIAN_POINT('Ctrl Pts',(1.226152364316,0.5652639823961,-3.990714305607));
#27295=CARTESIAN_POINT('Ctrl Pts',(1.296564691016,-0.3766868641562,-4.047589305607));
#27296=CARTESIAN_POINT('Ctrl Pts',(0.7323910942975,-1.134273457497,-4.104464305607));
#27297=CARTESIAN_POINT('Ctrl Pts',(-0.190241344867,-1.336705360987,-4.161339305607));
#27298=CARTESIAN_POINT('Ctrl Pts',(-1.019762749782,-0.8849050375959,-4.218214305607));
#27299=CARTESIAN_POINT('Ctrl Pts',(-1.350175170634,0.,-4.275089305607));
#27300=CARTESIAN_POINT('Ctrl Pts',(-1.019762749782,0.8849050375959,-4.331964305607));
#27301=CARTESIAN_POINT('Ctrl Pts',(-0.190241344867,1.336705360987,-4.388839305607));
#27302=CARTESIAN_POINT('Ctrl Pts',(0.7323910942975,1.134273457497,-4.445714305607));
#27303=CARTESIAN_POINT('Ctrl Pts',(1.296564691016,0.3766868641562,-4.502589305607));
#27304=CARTESIAN_POINT('Ctrl Pts',(1.226152364316,-0.5652639823961,-4.559464305607));
#27305=CARTESIAN_POINT('Ctrl Pts',(0.555616470709,-1.230554075189,-4.616339305607));
#27306=CARTESIAN_POINT('Ctrl Pts',(-0.3868583419482,-1.293566238123,-4.673214305607));
#27307=CARTESIAN_POINT('Ctrl Pts',(-1.139990581936,-0.723460043259,-4.730089305607));
#27308=CARTESIAN_POINT('Ctrl Pts',(-1.335170067905,0.2007338620856,-4.786964305607));
#27309=CARTESIAN_POINT('Ctrl Pts',(-0.8768683655278,1.026681130153,-4.843839305607));
#27310=CARTESIAN_POINT('Ctrl Pts',(0.01060315691615,1.350133991585,-4.900714305607));
#27311=CARTESIAN_POINT('Ctrl Pts',(0.892890536887,1.012779611507,-4.957589305607));
#27312=CARTESIAN_POINT('Ctrl Pts',(1.33814455045,0.1797435821333,-5.014464305607));
#27313=CARTESIAN_POINT('Ctrl Pts',(1.128537550737,-0.7413010717389,-5.071339305607));
#27314=CARTESIAN_POINT('Ctrl Pts',(0.3663010598456,-1.299393240218,-5.128214305607));
#27315=CARTESIAN_POINT('Ctrl Pts',(-0.2606752788197,-1.247804824574,-5.166130972273));
#27316=CARTESIAN_POINT('Ctrl Pts',(-0.5279823721497,-1.122019654338,-5.185089305607));
#27317=CARTESIAN_POINT('Ctrl Pts',(-0.4696881186261,0.9981380597272,-3.444135430279));
#27318=CARTESIAN_POINT('Ctrl Pts',(-0.2318942596183,1.110035356068,-3.463093763613));
#27319=CARTESIAN_POINT('Ctrl Pts',(0.3258579542137,1.155927922117,-3.501010430279));
#27320=CARTESIAN_POINT('Ctrl Pts',(1.003936318643,0.6594544137959,-3.557885430279));
#27321=CARTESIAN_POINT('Ctrl Pts',(1.190400720751,-0.1598981886148,-3.614760430279));
#27322=CARTESIAN_POINT('Ctrl Pts',(0.7943069665412,-0.9009591520544,-3.671635430279));
#27323=CARTESIAN_POINT('Ctrl Pts',(0.009432467987836,-1.201066414053,-3.728510430279));
#27324=CARTESIAN_POINT('Ctrl Pts',(-0.7800537946193,-0.9133258114035,-3.785385430279));
#27325=CARTESIAN_POINT('Ctrl Pts',(-1.187754649245,-0.1785709428966,-3.842260430279));
#27326=CARTESIAN_POINT('Ctrl Pts',(-1.014124826746,0.6435832038027,-3.899135430279));
#27327=CARTESIAN_POINT('Ctrl Pts',(-0.3441455177085,1.150744276231,-3.956010430279));
#27328=CARTESIAN_POINT('Ctrl Pts',(0.4942711510281,1.094689252768,-4.012885430279));
#27329=CARTESIAN_POINT('Ctrl Pts',(1.090773532456,0.5028534860695,-4.069760430279));
#27330=CARTESIAN_POINT('Ctrl Pts',(1.153411671532,-0.3350970673819,-4.126635430279));
#27331=CARTESIAN_POINT('Ctrl Pts',(0.6515281822355,-1.009038926982,-4.183510430279));
#27332=CARTESIAN_POINT('Ctrl Pts',(-0.169236898936,-1.189120431432,-4.240385430279));
#27333=CARTESIAN_POINT('Ctrl Pts',(-0.9071712857378,-0.7872031419892,-4.297260430279));
#27334=CARTESIAN_POINT('Ctrl Pts',(-1.201103046544,0.,-4.354135430279));
#27335=CARTESIAN_POINT('Ctrl Pts',(-0.9071712857378,0.7872031419892,-4.411010430279));
#27336=CARTESIAN_POINT('Ctrl Pts',(-0.169236898936,1.189120431432,-4.467885430279));
#27337=CARTESIAN_POINT('Ctrl Pts',(0.6515281822355,1.009038926982,-4.524760430279));
#27338=CARTESIAN_POINT('Ctrl Pts',(1.153411671532,0.3350970673819,-4.581635430279));
#27339=CARTESIAN_POINT('Ctrl Pts',(1.090773532456,-0.5028534860695,-4.638510430279));
#27340=CARTESIAN_POINT('Ctrl Pts',(0.4942711510281,-1.094689252768,-4.695385430279));
#27341=CARTESIAN_POINT('Ctrl Pts',(-0.3441455177085,-1.150744276231,-4.752260430279));
#27342=CARTESIAN_POINT('Ctrl Pts',(-1.014124826746,-0.6435832038027,-4.809135430279));
#27343=CARTESIAN_POINT('Ctrl Pts',(-1.187754649245,0.1785709428966,-4.866010430279));
#27344=CARTESIAN_POINT('Ctrl Pts',(-0.7800537946193,0.9133258114035,-4.922885430279));
#27345=CARTESIAN_POINT('Ctrl Pts',(0.009432467987837,1.201066414053,-4.979760430279));
#27346=CARTESIAN_POINT('Ctrl Pts',(0.7943069665412,0.9009591520544,-5.036635430279));
#27347=CARTESIAN_POINT('Ctrl Pts',(1.190400720751,0.1598981886148,-5.093510430279));
#27348=CARTESIAN_POINT('Ctrl Pts',(1.003936318643,-0.6594544137959,-5.150385430279));
#27349=CARTESIAN_POINT('Ctrl Pts',(0.3258579542137,-1.155927922117,-5.207260430279));
#27350=CARTESIAN_POINT('Ctrl Pts',(-0.2318942596183,-1.110035356068,-5.245177096946));
#27351=CARTESIAN_POINT('Ctrl Pts',(-0.4696881186261,-0.9981380597272,-5.264135430279));
#27352=CARTESIAN_POINT('',(-1.98293436122935E-9,-1.49923261688425,-5.00044299895813));
#27353=CARTESIAN_POINT('Ctrl Pts',(-2.06854461059408E-5,1.49901358627223,
-3.74995486355702));
#27354=CARTESIAN_POINT('Ctrl Pts',(0.0953214838108722,1.49902491199573,
-3.75491761318045));
#27355=CARTESIAN_POINT('Ctrl Pts',(0.190691030215867,1.49011947635385,-3.75989138992608));
#27356=CARTESIAN_POINT('Ctrl Pts',(0.372498933869856,1.4554667038667,-3.76973052378357));
#27357=CARTESIAN_POINT('Ctrl Pts',(0.458525227543786,1.43085386099119,-3.77459116547234));
#27358=CARTESIAN_POINT('Ctrl Pts',(0.722446426616915,1.32838383657262,-3.79004693335256));
#27359=CARTESIAN_POINT('Ctrl Pts',(0.866454933804677,1.23164641754742,-3.79893369151964));
#27360=CARTESIAN_POINT('Ctrl Pts',(1.06600265467696,1.0603973538125,-3.81260503313005));
#27361=CARTESIAN_POINT('Ctrl Pts',(1.14683835565651,0.97298033137476,-3.81875630933353));
#27362=CARTESIAN_POINT('Ctrl Pts',(1.29967423550168,0.762168700626042,-3.83268102999226));
#27363=CARTESIAN_POINT('Ctrl Pts',(1.36539620478676,0.636646697395098,-3.84046986466727));
#27364=CARTESIAN_POINT('Ctrl Pts',(1.44568091735346,0.409137312957459,-3.85325803431838));
#27365=CARTESIAN_POINT('Ctrl Pts',(1.46940771045131,0.312321550321848,-3.85841762364376));
#27366=CARTESIAN_POINT('Ctrl Pts',(1.50054215939582,0.0968012311807324,
-3.86974762234647));
#27367=CARTESIAN_POINT('Ctrl Pts',(1.50386336583334,-0.0225864242439717,
-3.87592790099484));
#27368=CARTESIAN_POINT('Ctrl Pts',(1.48028992278844,-0.279075253883447,
-3.88972651028424));
#27369=CARTESIAN_POINT('Ctrl Pts',(1.44824876150166,-0.413867874229844,
-3.89734526453951));
#27370=CARTESIAN_POINT('Ctrl Pts',(1.36138274914184,-0.635627037819925,
-3.90997498794205));
#27371=CARTESIAN_POINT('Ctrl Pts',(1.31601337842991,-0.724432162572956,
-3.91513698024775));
#27372=CARTESIAN_POINT('Ctrl Pts',(1.1985813070018,-0.907957044093197,-3.92647071223722));
#27373=CARTESIAN_POINT('Ctrl Pts',(1.12297157880747,-1.00051622230352,-3.93265174258831));
#27374=CARTESIAN_POINT('Ctrl Pts',(0.935510734630078,-1.18096930350538,
-3.94658311814019));
#27375=CARTESIAN_POINT('Ctrl Pts',(0.82085370381211,-1.26317291479204,-3.95433952071051));
#27376=CARTESIAN_POINT('Ctrl Pts',(0.607361198665975,-1.3742110709498,-3.96709317469488));
#27377=CARTESIAN_POINT('Ctrl Pts',(0.514819503017504,-1.41125178892118,
-3.97225152016788));
#27378=CARTESIAN_POINT('Ctrl Pts',(0.306211258635138,-1.47211310867903,
-3.98355595013962));
#27379=CARTESIAN_POINT('Ctrl Pts',(0.188926596878288,-1.49208312971452,
-3.98971190758976));
#27380=CARTESIAN_POINT('Ctrl Pts',(-0.0670817760633412,-1.50479893204468,
-4.00344188021202));
#27381=CARTESIAN_POINT('Ctrl Pts',(-0.204264061836427,-1.49224160547226,
-4.01101759022916));
#27382=CARTESIAN_POINT('Ctrl Pts',(-0.435383240178148,-1.43800305381015,
-4.02361014831978));
#27383=CARTESIAN_POINT('Ctrl Pts',(-0.529759724212074,-1.40572556203709,
-4.02877412817637));
#27384=CARTESIAN_POINT('Ctrl Pts',(-0.728440094304539,-1.31545684930298,
-4.04012620086496));
#27385=CARTESIAN_POINT('Ctrl Pts',(-0.831081185799221,-1.25358147405089,
-4.04632332229975));
#27386=CARTESIAN_POINT('Ctrl Pts',(-1.03747315158834,-1.09264013452199,
-4.06033406844491));
#27387=CARTESIAN_POINT('Ctrl Pts',(-1.13578892642194,-0.989806391524769,
-4.06815505599112));
#27388=CARTESIAN_POINT('Ctrl Pts',(-1.27616339680925,-0.79292350020094,
-4.08096631701665));
#27389=CARTESIAN_POINT('Ctrl Pts',(-1.32572981587319,-0.706468967379275,
-4.08612261921322));
#27390=CARTESIAN_POINT('Ctrl Pts',(-1.41494914035009,-0.508669815653088,
-4.09741077045872));
#27391=CARTESIAN_POINT('Ctrl Pts',(-1.45101571447823,-0.395608673695437,
-4.10355276851211));
#27392=CARTESIAN_POINT('Ctrl Pts',(-1.49905455000182,-0.145868247220127,
-4.11717831536221));
#27393=CARTESIAN_POINT('Ctrl Pts',(-1.50597375104998,-0.00999053376809994,
-4.12466154019219));
#27394=CARTESIAN_POINT('Ctrl Pts',(-1.48555860957934,0.224860674033037,
-4.13717178661237));
#27395=CARTESIAN_POINT('Ctrl Pts',(-1.46712396673882,0.32292021535189,-4.14233879547487));
#27396=CARTESIAN_POINT('Ctrl Pts',(-1.40609716643174,0.532947437375313,
-4.15371621536766));
#27397=CARTESIAN_POINT('Ctrl Pts',(-1.35932684529104,0.643798827202036,
-4.15993516379194));
#27398=CARTESIAN_POINT('Ctrl Pts',(-1.22813604202709,0.873215485968564,
-4.17407803827426));
#27399=CARTESIAN_POINT('Ctrl Pts',(-1.13881445511541,0.986617888170726,
-4.18201228151039));
#27400=CARTESIAN_POINT('Ctrl Pts',(-0.961751173064932,1.15426033407093,
-4.19492489192118));
#27401=CARTESIAN_POINT('Ctrl Pts',(-0.883016083174209,1.21528568040051,
-4.20007785607496));
#27402=CARTESIAN_POINT('Ctrl Pts',(-0.699907663242897,1.33073761999726,
-4.21133910588142));
#27403=CARTESIAN_POINT('Ctrl Pts',(-0.59339436076046,1.38193694102476,-4.21745797747921));
#27404=CARTESIAN_POINT('Ctrl Pts',(-0.356452332247489,1.4630284072985,-4.23088037938893));
#27405=CARTESIAN_POINT('Ctrl Pts',(-0.226267156170153,1.48861703792723,
-4.2381799877178));
#27406=CARTESIAN_POINT('Ctrl Pts',(0.00575573259620276,1.50249422398779,
-4.25052727259274));
#27407=CARTESIAN_POINT('Ctrl Pts',(0.105522727996987,1.49854594605214,-4.25570057131407));
#27408=CARTESIAN_POINT('Ctrl Pts',(0.323231911347154,1.46862568093766,-4.26713232860675));
#27409=CARTESIAN_POINT('Ctrl Pts',(0.440651133512366,1.43814338966245,-4.27339821195148));
#27410=CARTESIAN_POINT('Ctrl Pts',(0.691202779825676,1.33949753157944,-4.28779882845233));
#27411=CARTESIAN_POINT('Ctrl Pts',(0.819432220535704,1.26490268988052,-4.29594988333619));
#27412=CARTESIAN_POINT('Ctrl Pts',(1.01263927792164,1.10985318182305,-4.3090569998956));
#27413=CARTESIAN_POINT('Ctrl Pts',(1.08376671441976,1.04021565780867,-4.31420386152154));
#27414=CARTESIAN_POINT('Ctrl Pts',(1.22248539198388,0.875270661352502,-4.32541672165898));
#27415=CARTESIAN_POINT('Ctrl Pts',(1.28731113077411,0.777524084484609,-4.33149402762996));
#27416=CARTESIAN_POINT('Ctrl Pts',(1.39385162400454,0.566766273420988,-4.34415987801976));
#27417=CARTESIAN_POINT('Ctrl Pts',(1.43435322284828,0.454479793977223,-4.35073445226797));
#27418=CARTESIAN_POINT('Ctrl Pts',(1.50158127237526,0.16035036256143,-4.36683902084268));
#27419=CARTESIAN_POINT('Ctrl Pts',(1.50960418346802,-0.024600845584221,
-4.37616861592655));
#27420=CARTESIAN_POINT('Ctrl Pts',(1.45976216022343,-0.392156499866828,
-4.39565249615808));
#27421=CARTESIAN_POINT('Ctrl Pts',(1.39976156558948,-0.571423312178124,
-4.40599198974702));
#27422=CARTESIAN_POINT('Ctrl Pts',(1.2396181854439,-0.853752427360892,-4.42322630594188));
#27423=CARTESIAN_POINT('Ctrl Pts',(1.15716102195368,-0.962143722097524,
-4.43020040010785));
#27424=CARTESIAN_POINT('Ctrl Pts',(0.992056672639983,-1.12835719191808,
-4.44241776529972));
#27425=CARTESIAN_POINT('Ctrl Pts',(0.915130849967703,-1.19202945764122,
-4.44763968365768));
#27426=CARTESIAN_POINT('Ctrl Pts',(0.751015587707874,-1.30203114853202,
-4.458282264193));
#27427=CARTESIAN_POINT('Ctrl Pts',(0.664441333631893,-1.34825382205082,
-4.46368412404472));
#27428=CARTESIAN_POINT('Ctrl Pts',(0.469866631067643,-1.42827884860942,
-4.47497345546702));
#27429=CARTESIAN_POINT('Ctrl Pts',(0.361429858991136,-1.45911306466684,
-4.48082613074989));
#27430=CARTESIAN_POINT('Ctrl Pts',(0.0868762359092743,-1.50558560899775,
-4.49531699283451));
#27431=CARTESIAN_POINT('Ctrl Pts',(-0.108524317716607,-1.51122808335893,
-4.50529891944146));
#27432=CARTESIAN_POINT('Ctrl Pts',(-0.523722674797389,-1.42104336266443,
-4.52848372599792));
#27433=CARTESIAN_POINT('Ctrl Pts',(-0.694234730239479,-1.33806699523359,
-4.53820584742696));
#27434=CARTESIAN_POINT('Ctrl Pts',(-0.910861496374433,-1.19466783514413,
-4.55172096812832));
#27435=CARTESIAN_POINT('Ctrl Pts',(-0.98867136206926,-1.13146867135376,
-4.55691876600439));
#27436=CARTESIAN_POINT('Ctrl Pts',(-1.15071022637616,-0.970526548867814,
-4.56906886005236));
#27437=CARTESIAN_POINT('Ctrl Pts',(-1.22919775433432,-0.86912994570599,
-4.57612660127595));
#27438=CARTESIAN_POINT('Ctrl Pts',(-1.35102651289326,-0.66008878878192,
-4.58909822282328));
#27439=CARTESIAN_POINT('Ctrl Pts',(-1.39685081727062,-0.555601837992771,
-4.59501522777262));
#27440=CARTESIAN_POINT('Ctrl Pts',(-1.46023242591247,-0.35263118015693,
-4.60607893598703));
#27441=CARTESIAN_POINT('Ctrl Pts',(-1.48061440505115,-0.254942345678531,
-4.61123656160695));
#27442=CARTESIAN_POINT('Ctrl Pts',(-1.50710266895417,-0.00828580751651268,
-4.62435255893666));
#27443=CARTESIAN_POINT('Ctrl Pts',(-1.50081675130974,0.14007412730559,-4.63250645615578));
#27444=CARTESIAN_POINT('Ctrl Pts',(-1.44962171172692,0.400100283576456,
-4.64669155693514));
#27445=CARTESIAN_POINT('Ctrl Pts',(-1.41383856371387,0.511332352490623,
-4.65273927950174));
#27446=CARTESIAN_POINT('Ctrl Pts',(-1.32508034509336,0.707735304809056,
-4.66395129249828));
#27447=CARTESIAN_POINT('Ctrl Pts',(-1.27525799313722,0.794428647654011,
-4.66912511463795));
#27448=CARTESIAN_POINT('Ctrl Pts',(-1.13603749863021,0.989120951306691,
-4.68180966008535));
#27449=CARTESIAN_POINT('Ctrl Pts',(-1.039783729169,1.09007739184694,-4.68947685530421));
#27450=CARTESIAN_POINT('Ctrl Pts',(-0.839992920828512,1.24722356599085,
-4.70309675364886));
#27451=CARTESIAN_POINT('Ctrl Pts',(-0.742007099499302,1.30747183338976,
-4.709058034298));
#27452=CARTESIAN_POINT('Ctrl Pts',(-0.548714342600776,1.39841818027375,
-4.72017198315358));
#27453=CARTESIAN_POINT('Ctrl Pts',(-0.454659915595358,1.43197845452504,
-4.72533518699329));
#27454=CARTESIAN_POINT('Ctrl Pts',(-0.216974120292315,1.49111903235912,
-4.7382953841698));
#27455=CARTESIAN_POINT('Ctrl Pts',(-0.0724161569414992,1.50527557455243,
-4.74627396486505));
#27456=CARTESIAN_POINT('Ctrl Pts',(0.188277504903036,1.49194501788249,-4.76025172537461));
#27457=CARTESIAN_POINT('Ctrl Pts',(0.302762928080303,1.47261448509728,-4.76626424532973));
#27458=CARTESIAN_POINT('Ctrl Pts',(0.509166190956025,1.41331142809291,-4.77743639057917));
#27459=CARTESIAN_POINT('Ctrl Pts',(0.602092049133723,1.37653010345847,-4.78260599265093));
#27460=CARTESIAN_POINT('Ctrl Pts',(0.816798907969054,1.26585681257779,-4.79539924148338));
#27461=CARTESIAN_POINT('Ctrl Pts',(0.932266966022699,1.18361839847875,-4.80318933375506));
#27462=CARTESIAN_POINT('Ctrl Pts',(1.11767176119119,1.00598881419239,-4.81694380600376));
#27463=CARTESIAN_POINT('Ctrl Pts',(1.19119922319881,0.917143963828736,-4.8229188128383));
#27464=CARTESIAN_POINT('Ctrl Pts',(1.30836409219123,0.738141596019945,-4.83404861925251));
#27465=CARTESIAN_POINT('Ctrl Pts',(1.35471182572177,0.649655711812843,-4.83921376341602));
#27466=CARTESIAN_POINT('Ctrl Pts',(1.44584034292757,0.423842525840391,-4.8521023404286));
#27467=CARTESIAN_POINT('Ctrl Pts',(1.47984174077659,0.284133317597195,-4.860001653993));
#27468=CARTESIAN_POINT('Ctrl Pts',(1.50356071468381,0.0257340761359156,
-4.87390253859832));
#27469=CARTESIAN_POINT('Ctrl Pts',(1.50070694923776,-0.0902601036702479,
-4.87991376788426));
#27470=CARTESIAN_POINT('Ctrl Pts',(1.47138357560968,-0.3028900573086,-4.8910824294789));
#27471=CARTESIAN_POINT('Ctrl Pts',(1.44820663630591,-0.400068083839261,
-4.89625016146622));
#27472=CARTESIAN_POINT('Ctrl Pts',(1.36846871474656,-0.630511787660118,
-4.90916112595295));
#27473=CARTESIAN_POINT('Ctrl Pts',(1.30213290035627,-0.75843222776214,-4.91707761328718));
#27474=CARTESIAN_POINT('Ctrl Pts',(1.1501446460106,-0.968689653567613,-4.93095602028381));
#27475=CARTESIAN_POINT('Ctrl Pts',(1.07203283432548,-1.05396027144246,-4.93693871001663));
#27476=CARTESIAN_POINT('Ctrl Pts',(0.872606659872905,-1.22786655368374,
-4.95069608904956));
#27477=CARTESIAN_POINT('Ctrl Pts',(0.726903650728373,-1.32597814557149,
-4.95968126963874));
#27478=CARTESIAN_POINT('Ctrl Pts',(0.46234340839985,-1.42967442692867,-4.97519006837574));
#27479=CARTESIAN_POINT('Ctrl Pts',(0.375674252659661,-1.45470533198711,
-4.98009449424626));
#27480=CARTESIAN_POINT('Ctrl Pts',(0.192359458102347,-1.4899630079936,-4.99002156504881));
#27481=CARTESIAN_POINT('Ctrl Pts',(0.096155412570898,-1.49902501105836,
-4.99503897916822));
#27482=CARTESIAN_POINT('Ctrl Pts',(-2.06854460854666E-5,-1.49901358627223,
-5.00004513644297));
#27483=CARTESIAN_POINT('',(3.24550813202643E-10,-1.11698717744401,-5.22113249718027));
#27484=CARTESIAN_POINT('',(0.,-1.5,-5.));
#27485=CARTESIAN_POINT('Ctrl Pts',(2.02707198384535E-6,1.11628565404413,
-3.47111408882413));
#27486=CARTESIAN_POINT('Ctrl Pts',(0.0945477069597151,1.11645974724111,
-3.47785015639956));
#27487=CARTESIAN_POINT('Ctrl Pts',(0.189124507262868,1.1048491526056,-3.48459224618512));
#27488=CARTESIAN_POINT('Ctrl Pts',(0.37280187843043,1.05728988862616,-3.49813470031972));
#27489=CARTESIAN_POINT('Ctrl Pts',(0.46120374861096,1.02120417552907,-3.50489047871014));
#27490=CARTESIAN_POINT('Ctrl Pts',(0.668471432388854,0.904915646636005,
-3.52182073957925));
#27491=CARTESIAN_POINT('Ctrl Pts',(0.780383055419262,0.81102950076143,-3.53202995426488));
#27492=CARTESIAN_POINT('Ctrl Pts',(0.977352549963127,0.567498199932436,
-3.55436776308206));
#27493=CARTESIAN_POINT('Ctrl Pts',(1.03703915589555,0.431145768277802,-3.5647587800084));
#27494=CARTESIAN_POINT('Ctrl Pts',(1.11066616674449,0.178042375581387,-3.58352929238688));
#27495=CARTESIAN_POINT('Ctrl Pts',(1.1250370353998,0.0352369170927974,-3.59357133882956));
#27496=CARTESIAN_POINT('Ctrl Pts',(1.09418460733437,-0.296790717289763,
-3.61736190012804));
#27497=CARTESIAN_POINT('Ctrl Pts',(1.02997735713433,-0.440477084842063,
-3.62828381624767));
#27498=CARTESIAN_POINT('Ctrl Pts',(0.9255889082428,-0.636392952388534,-3.64408990478641));
#27499=CARTESIAN_POINT('Ctrl Pts',(0.840538191683136,-0.751460714065273,
-3.65410198836101));
#27500=CARTESIAN_POINT('Ctrl Pts',(0.61118224779972,-0.946513834085747,
-3.67558474266587));
#27501=CARTESIAN_POINT('Ctrl Pts',(0.4782345297511,-1.0191711099922,-3.68616577485579));
#27502=CARTESIAN_POINT('Ctrl Pts',(0.222597234321225,-1.1004636264182,-3.705267721173));
#27503=CARTESIAN_POINT('Ctrl Pts',(0.0794663775051739,-1.12675755955542,
-3.71543571983759));
#27504=CARTESIAN_POINT('Ctrl Pts',(-0.232981315456785,-1.10176800386664,
-3.73779253835339));
#27505=CARTESIAN_POINT('Ctrl Pts',(-0.377700605109036,-1.06037143957914,
-3.74830194335543));
#27506=CARTESIAN_POINT('Ctrl Pts',(-0.604852724324544,-0.94473173616761,
-3.76645937858707));
#27507=CARTESIAN_POINT('Ctrl Pts',(-0.731331226988469,-0.863974006299937,
-3.77692136770941));
#27508=CARTESIAN_POINT('Ctrl Pts',(-0.943397907937875,-0.61393454762197,
-3.80029160325254));
#27509=CARTESIAN_POINT('Ctrl Pts',(-1.01607631574408,-0.484189787750154,
-3.81067712497169));
#27510=CARTESIAN_POINT('Ctrl Pts',(-1.11857306467123,-0.173002860562893,
-3.83402934320733));
#27511=CARTESIAN_POINT('Ctrl Pts',(-1.1216526627367,-0.0230529286472856,
-3.84448736045733));
#27512=CARTESIAN_POINT('Ctrl Pts',(-1.10179845703877,0.228016486144775,
-3.86242927917354));
#27513=CARTESIAN_POINT('Ctrl Pts',(-1.06324590215936,0.369253565391399,
-3.87266080687385));
#27514=CARTESIAN_POINT('Ctrl Pts',(-0.924464855646186,0.649976757040046,
-3.89499359014349));
#27515=CARTESIAN_POINT('Ctrl Pts',(-0.825915661788603,0.761161572818591,
-3.90536755467241));
#27516=CARTESIAN_POINT('Ctrl Pts',(-0.626214316349842,0.934430304671211,
-3.92419538133658));
#27517=CARTESIAN_POINT('Ctrl Pts',(-0.502214996937528,1.0073238571117,-3.93425796124846));
#27518=CARTESIAN_POINT('Ctrl Pts',(-0.19120199753371,1.11682300306852,-3.95778190972181));
#27519=CARTESIAN_POINT('Ctrl Pts',(-0.0349012702549547,1.12007370080308,
-3.96864513166231));
#27520=CARTESIAN_POINT('Ctrl Pts',(0.203851405860764,1.10611718857029,-3.98567366866181));
#27521=CARTESIAN_POINT('Ctrl Pts',(0.341786112597055,1.07261170247851,-3.995614088678));
#27522=CARTESIAN_POINT('Ctrl Pts',(0.603413551668548,0.951563052462829,
-4.01618313304261));
#27523=CARTESIAN_POINT('Ctrl Pts',(0.725113385898965,0.86121167341581,-4.02676949290965));
#27524=CARTESIAN_POINT('Ctrl Pts',(0.905273423514502,0.663857977873305,
-4.04579742516296));
#27525=CARTESIAN_POINT('Ctrl Pts',(0.989304020610915,0.545163021076572,
-4.05595751403342));
#27526=CARTESIAN_POINT('Ctrl Pts',(1.09791444748827,0.250846118613153,-4.07833525890648));
#27527=CARTESIAN_POINT('Ctrl Pts',(1.12102369397598,0.101931202388067,-4.08885689635648));
#27528=CARTESIAN_POINT('Ctrl Pts',(1.11127472608703,-0.152382998726041,
-4.10698527230642));
#27529=CARTESIAN_POINT('Ctrl Pts',(1.09120934524511,-0.300938815206558,
-4.11743533545796));
#27530=CARTESIAN_POINT('Ctrl Pts',(0.953355092950169,-0.598483057720678,
-4.14081240762304));
#27531=CARTESIAN_POINT('Ctrl Pts',(0.865889506205107,-0.719096632405901,
-4.15121651825254));
#27532=CARTESIAN_POINT('Ctrl Pts',(0.630908211369321,-0.938430669099282,
-4.17412556939149));
#27533=CARTESIAN_POINT('Ctrl Pts',(0.499473987912806,-1.00559671816687,
-4.18443093822623));
#27534=CARTESIAN_POINT('Ctrl Pts',(0.254954649474644,-1.09592824110065,
-4.20300231361181));
#27535=CARTESIAN_POINT('Ctrl Pts',(0.110233508147538,-1.12012616746575,
-4.21325541986775));
#27536=CARTESIAN_POINT('Ctrl Pts',(-0.202625788977277,-1.11169037854405,
-4.23557375090056));
#27537=CARTESIAN_POINT('Ctrl Pts',(-0.344594062565005,-1.06910154094397,
-4.24592507043897));
#27538=CARTESIAN_POINT('Ctrl Pts',(-0.586363065095529,-0.95997491663841,
-4.2648152172114));
#27539=CARTESIAN_POINT('Ctrl Pts',(-0.704733656287602,-0.877644037487904,
-4.27490073023948));
#27540=CARTESIAN_POINT('Ctrl Pts',(-0.924445762809004,-0.651144082671878,
-4.29741286795022));
#27541=CARTESIAN_POINT('Ctrl Pts',(-0.995878303027182,-0.517818669122211,
-4.30795712525469));
#27542=CARTESIAN_POINT('Ctrl Pts',(-1.08982166380632,-0.277939862987314,
-4.32630001885425));
#27543=CARTESIAN_POINT('Ctrl Pts',(-1.1169872981078,-0.139044412854724,
-4.33621126978535));
#27544=CARTESIAN_POINT('Ctrl Pts',(-1.1169872981078,0.139044412854727,-4.35605370329665));
#27545=CARTESIAN_POINT('Ctrl Pts',(-1.08982166380632,0.277939862987316,
-4.36596495422619));
#27546=CARTESIAN_POINT('Ctrl Pts',(-0.995878303027179,0.517818669122219,
-4.38430784782586));
#27547=CARTESIAN_POINT('Ctrl Pts',(-0.924445762808998,0.651144082671885,
-4.39485210513048));
#27548=CARTESIAN_POINT('Ctrl Pts',(-0.704733656287599,0.877644037487907,
-4.41736424284125));
#27549=CARTESIAN_POINT('Ctrl Pts',(-0.586363065095524,0.959974916638413,
-4.42744975586925));
#27550=CARTESIAN_POINT('Ctrl Pts',(-0.344594062564994,1.06910154094398,
-4.44633990264163));
#27551=CARTESIAN_POINT('Ctrl Pts',(-0.202625788977266,1.11169037854405,
-4.45669122217995));
#27552=CARTESIAN_POINT('Ctrl Pts',(0.110233508147553,1.12012616746575,-4.47900955321285));
#27553=CARTESIAN_POINT('Ctrl Pts',(0.254954649474663,1.09592824110064,-4.48926265946891));
#27554=CARTESIAN_POINT('Ctrl Pts',(0.499473987912846,1.00559671816685,-4.50783403485462));
#27555=CARTESIAN_POINT('Ctrl Pts',(0.630908211369362,0.938430669099253,
-4.51813940368944));
#27556=CARTESIAN_POINT('Ctrl Pts',(0.865889506205137,0.719096632405866,
-4.54104845482854));
#27557=CARTESIAN_POINT('Ctrl Pts',(0.953355092950198,0.598483057720634,
-4.55145256545815));
#27558=CARTESIAN_POINT('Ctrl Pts',(1.09120934524514,0.300938815206483,-4.57482963762336));
#27559=CARTESIAN_POINT('Ctrl Pts',(1.11127472608704,0.152382998725954,-4.58527970077493));
#27560=CARTESIAN_POINT('Ctrl Pts',(1.12102369397598,-0.10193120238813,-4.60340807672478));
#27561=CARTESIAN_POINT('Ctrl Pts',(1.09791444748826,-0.250846118613211,
-4.61392971417461));
#27562=CARTESIAN_POINT('Ctrl Pts',(0.989304020610889,-0.545163021076618,
-4.63630745904754));
#27563=CARTESIAN_POINT('Ctrl Pts',(0.905273423514473,-0.663857977873342,
-4.64646754791798));
#27564=CARTESIAN_POINT('Ctrl Pts',(0.725113385898935,-0.861211673415836,
-4.66549548017135));
#27565=CARTESIAN_POINT('Ctrl Pts',(0.603413551668514,-0.951563052462852,
-4.67608184003854));
#27566=CARTESIAN_POINT('Ctrl Pts',(0.341786112597019,-1.07261170247852,
-4.69665088440312));
#27567=CARTESIAN_POINT('Ctrl Pts',(0.203851405860731,-1.1061171885703,-4.70659130441917));
#27568=CARTESIAN_POINT('Ctrl Pts',(-0.034901270254981,-1.12007370080307,
-4.72361984141848));
#27569=CARTESIAN_POINT('Ctrl Pts',(-0.191201997533732,-1.11682300306852,
-4.73448306335868));
#27570=CARTESIAN_POINT('Ctrl Pts',(-0.502214996937548,-1.00732385711169,
-4.75800701183202));
#27571=CARTESIAN_POINT('Ctrl Pts',(-0.626214316349861,-0.934430304671198,
-4.76806959174406));
#27572=CARTESIAN_POINT('Ctrl Pts',(-0.82591566178862,-0.761161572818574,
-4.78689741840843));
#27573=CARTESIAN_POINT('Ctrl Pts',(-0.924464855646204,-0.649976757040023,
-4.79727138293758));
#27574=CARTESIAN_POINT('Ctrl Pts',(-1.06324590215937,-0.369253565391362,
-4.81960416620731));
#27575=CARTESIAN_POINT('Ctrl Pts',(-1.10179845703878,-0.228016486144732,
-4.82983569390757));
#27576=CARTESIAN_POINT('Ctrl Pts',(-1.12165266273671,0.0230529286474007,
-4.84777761262373));
#27577=CARTESIAN_POINT('Ctrl Pts',(-1.11857306467121,0.173002860562986,
-4.85823562987364));
#27578=CARTESIAN_POINT('Ctrl Pts',(-1.01607631574406,0.484189787750189,
-4.88158784810919));
#27579=CARTESIAN_POINT('Ctrl Pts',(-0.943397907937854,0.613934547622001,
-4.8919733698283));
#27580=CARTESIAN_POINT('Ctrl Pts',(-0.731331226988424,0.863974006299981,
-4.91534360537137));
#27581=CARTESIAN_POINT('Ctrl Pts',(-0.604852724324483,0.944731736167644,
-4.92580559449369));
#27582=CARTESIAN_POINT('Ctrl Pts',(-0.377700605109008,1.06037143957915,
-4.9439630297253));
#27583=CARTESIAN_POINT('Ctrl Pts',(-0.232981315456755,1.10176800386665,
-4.95447243472734));
#27584=CARTESIAN_POINT('Ctrl Pts',(0.0794663775052038,1.12675755955542,
-4.97682925324312));
#27585=CARTESIAN_POINT('Ctrl Pts',(0.222597234321253,1.1004636264182,-4.98699725190771));
#27586=CARTESIAN_POINT('Ctrl Pts',(0.478234529751118,1.01917110999219,-5.00609919822493));
#27587=CARTESIAN_POINT('Ctrl Pts',(0.611182247799728,0.946513834085734,
-5.01668023041484));
#27588=CARTESIAN_POINT('Ctrl Pts',(0.840538191683134,0.751460714065251,
-5.03816298471982));
#27589=CARTESIAN_POINT('Ctrl Pts',(0.925588908242794,0.636392952388502,
-5.04817506829456));
#27590=CARTESIAN_POINT('Ctrl Pts',(1.02997735713434,0.440477084842007,-5.06398115683345));
#27591=CARTESIAN_POINT('Ctrl Pts',(1.09418460733438,0.296790717289679,-5.07490307295331));
#27592=CARTESIAN_POINT('Ctrl Pts',(1.1250370353998,-0.0352369170928775,
-5.09869363425173));
#27593=CARTESIAN_POINT('Ctrl Pts',(1.11066616674449,-0.178042375581458,
-5.10873568069418));
#27594=CARTESIAN_POINT('Ctrl Pts',(1.03703915589554,-0.431145768277862,
-5.12750619307245));
#27595=CARTESIAN_POINT('Ctrl Pts',(0.977352549963114,-0.567498199932472,
-5.13789720999855));
#27596=CARTESIAN_POINT('Ctrl Pts',(0.780383055419248,-0.811029500761452,
-5.16023501881578));
#27597=CARTESIAN_POINT('Ctrl Pts',(0.668471432388827,-0.904915646636028,
-5.17044423350158));
#27598=CARTESIAN_POINT('Ctrl Pts',(0.461203748610708,-1.02120417552921,
-5.18737449437092));
#27599=CARTESIAN_POINT('Ctrl Pts',(0.372801878429925,-1.05728988862637,
-5.19413027276147));
#27600=CARTESIAN_POINT('Ctrl Pts',(0.189124462134141,-1.10484916429063,
-5.20767273022349));
#27601=CARTESIAN_POINT('Ctrl Pts',(0.0945476136912826,-1.11645975869105,
-5.21441482333081));
#27602=CARTESIAN_POINT('Ctrl Pts',(1.88721575241811E-6,-1.11628565378659,
-5.22115089422152));
#27603=CARTESIAN_POINT('Ctrl Pts',(-0.4755900604755,1.010680324589,-3.420126599063));
#27604=CARTESIAN_POINT('Ctrl Pts',(-0.2348081643589,1.123983684464,-3.439084932396));
#27605=CARTESIAN_POINT('Ctrl Pts',(0.329952574922,1.170452920957,-3.477001599063));
#27606=CARTESIAN_POINT('Ctrl Pts',(1.016551442463,0.6677408946504,-3.533876599063));
#27607=CARTESIAN_POINT('Ctrl Pts',(1.205358893105,-0.1619074151071,-3.590751599063));
#27608=CARTESIAN_POINT('Ctrl Pts',(0.8042879589087,-0.9122802996697,-3.647626599063));
#27609=CARTESIAN_POINT('Ctrl Pts',(0.009550993186479,-1.216158607898,-3.704501599063));
#27610=CARTESIAN_POINT('Ctrl Pts',(-0.7898556864549,-0.9248023542725,-3.761376599063));
#27611=CARTESIAN_POINT('Ctrl Pts',(-1.202679571961,-0.180814804896,-3.818251599063));
#27612=CARTESIAN_POINT('Ctrl Pts',(-1.026867975908,0.6516702524068,-3.875126599063));
#27613=CARTESIAN_POINT('Ctrl Pts',(-0.348469933747,1.165204139133,-3.932001599063));
#27614=CARTESIAN_POINT('Ctrl Pts',(0.5004819949382,1.108444747226,-3.988876599063));
#27615=CARTESIAN_POINT('Ctrl Pts',(1.104479823299,0.5091721726955,-4.045751599063));
#27616=CARTESIAN_POINT('Ctrl Pts',(1.167905052019,-0.3393077836576,-4.102626599063));
#27617=CARTESIAN_POINT('Ctrl Pts',(0.6597150647482,-1.02171816845,-4.159501599063));
#27618=CARTESIAN_POINT('Ctrl Pts',(-0.1713634724997,-1.204062516105,-4.216376599063));
#27619=CARTESIAN_POINT('Ctrl Pts',(-0.9185704929214,-0.7970948701029,-4.273251599063));
#27620=CARTESIAN_POINT('Ctrl Pts',(-1.216195700701,0.,-4.330126599063));
#27621=CARTESIAN_POINT('Ctrl Pts',(-0.9185704929214,0.7970948701029,-4.387001599063));
#27622=CARTESIAN_POINT('Ctrl Pts',(-0.1713634724997,1.204062516105,-4.443876599063));
#27623=CARTESIAN_POINT('Ctrl Pts',(0.6597150647482,1.02171816845,-4.500751599063));
#27624=CARTESIAN_POINT('Ctrl Pts',(1.167905052019,0.3393077836576,-4.557626599063));
#27625=CARTESIAN_POINT('Ctrl Pts',(1.104479823299,-0.5091721726955,-4.614501599063));
#27626=CARTESIAN_POINT('Ctrl Pts',(0.5004819949382,-1.108444747226,-4.671376599063));
#27627=CARTESIAN_POINT('Ctrl Pts',(-0.348469933747,-1.165204139133,-4.728251599063));
#27628=CARTESIAN_POINT('Ctrl Pts',(-1.026867975908,-0.6516702524068,-4.785126599063));
#27629=CARTESIAN_POINT('Ctrl Pts',(-1.202679571961,0.180814804896,-4.842001599063));
#27630=CARTESIAN_POINT('Ctrl Pts',(-0.7898556864549,0.9248023542725,-4.898876599063));
#27631=CARTESIAN_POINT('Ctrl Pts',(0.00955099318648,1.216158607898,-4.955751599063));
#27632=CARTESIAN_POINT('Ctrl Pts',(0.8042879589087,0.9122802996697,-5.012626599063));
#27633=CARTESIAN_POINT('Ctrl Pts',(1.205358893105,0.161907415107,-5.069501599063));
#27634=CARTESIAN_POINT('Ctrl Pts',(1.016551442463,-0.6677408946504,-5.126376599063));
#27635=CARTESIAN_POINT('Ctrl Pts',(0.329952574922,-1.170452920957,-5.183251599063));
#27636=CARTESIAN_POINT('Ctrl Pts',(-0.2348081643589,-1.123983684464,-5.22116826573));
#27637=CARTESIAN_POINT('Ctrl Pts',(-0.4755900604755,-1.010680324589,-5.240126599063));
#27638=CARTESIAN_POINT('Ctrl Pts',(-0.4755900604755,1.010680324589,-3.450042199688));
#27639=CARTESIAN_POINT('Ctrl Pts',(-0.2348081643589,1.123983684464,-3.469000533021));
#27640=CARTESIAN_POINT('Ctrl Pts',(0.329952574922,1.170452920957,-3.506917199688));
#27641=CARTESIAN_POINT('Ctrl Pts',(1.016551442463,0.6677408946504,-3.563792199688));
#27642=CARTESIAN_POINT('Ctrl Pts',(1.205358893105,-0.1619074151071,-3.620667199688));
#27643=CARTESIAN_POINT('Ctrl Pts',(0.8042879589087,-0.9122802996697,-3.677542199688));
#27644=CARTESIAN_POINT('Ctrl Pts',(0.009550993186479,-1.216158607898,-3.734417199688));
#27645=CARTESIAN_POINT('Ctrl Pts',(-0.7898556864549,-0.9248023542725,-3.791292199688));
#27646=CARTESIAN_POINT('Ctrl Pts',(-1.202679571961,-0.180814804896,-3.848167199688));
#27647=CARTESIAN_POINT('Ctrl Pts',(-1.026867975908,0.6516702524068,-3.905042199688));
#27648=CARTESIAN_POINT('Ctrl Pts',(-0.348469933747,1.165204139133,-3.961917199688));
#27649=CARTESIAN_POINT('Ctrl Pts',(0.5004819949382,1.108444747226,-4.018792199688));
#27650=CARTESIAN_POINT('Ctrl Pts',(1.104479823299,0.5091721726955,-4.075667199688));
#27651=CARTESIAN_POINT('Ctrl Pts',(1.167905052019,-0.3393077836576,-4.132542199688));
#27652=CARTESIAN_POINT('Ctrl Pts',(0.6597150647482,-1.02171816845,-4.189417199688));
#27653=CARTESIAN_POINT('Ctrl Pts',(-0.1713634724997,-1.204062516105,-4.246292199688));
#27654=CARTESIAN_POINT('Ctrl Pts',(-0.9185704929214,-0.7970948701029,-4.303167199688));
#27655=CARTESIAN_POINT('Ctrl Pts',(-1.216195700701,0.,-4.360042199688));
#27656=CARTESIAN_POINT('Ctrl Pts',(-0.9185704929214,0.7970948701029,-4.416917199688));
#27657=CARTESIAN_POINT('Ctrl Pts',(-0.1713634724997,1.204062516105,-4.473792199688));
#27658=CARTESIAN_POINT('Ctrl Pts',(0.6597150647482,1.02171816845,-4.530667199688));
#27659=CARTESIAN_POINT('Ctrl Pts',(1.167905052019,0.3393077836576,-4.587542199688));
#27660=CARTESIAN_POINT('Ctrl Pts',(1.104479823299,-0.5091721726955,-4.644417199688));
#27661=CARTESIAN_POINT('Ctrl Pts',(0.5004819949382,-1.108444747226,-4.701292199688));
#27662=CARTESIAN_POINT('Ctrl Pts',(-0.348469933747,-1.165204139133,-4.758167199688));
#27663=CARTESIAN_POINT('Ctrl Pts',(-1.026867975908,-0.6516702524068,-4.815042199688));
#27664=CARTESIAN_POINT('Ctrl Pts',(-1.202679571961,0.180814804896,-4.871917199688));
#27665=CARTESIAN_POINT('Ctrl Pts',(-0.7898556864549,0.9248023542725,-4.928792199688));
#27666=CARTESIAN_POINT('Ctrl Pts',(0.00955099318648,1.216158607898,-4.985667199688));
#27667=CARTESIAN_POINT('Ctrl Pts',(0.8042879589087,0.9122802996697,-5.042542199688));
#27668=CARTESIAN_POINT('Ctrl Pts',(1.205358893105,0.161907415107,-5.099417199688));
#27669=CARTESIAN_POINT('Ctrl Pts',(1.016551442463,-0.6677408946504,-5.156292199688));
#27670=CARTESIAN_POINT('Ctrl Pts',(0.329952574922,-1.170452920957,-5.213167199688));
#27671=CARTESIAN_POINT('Ctrl Pts',(-0.2348081643589,-1.123983684464,-5.251083866354));
#27672=CARTESIAN_POINT('Ctrl Pts',(-0.4755900604755,-1.010680324589,-5.270042199688));
#27673=CARTESIAN_POINT('Ctrl Pts',(-0.4755900604755,1.010680324589,-3.479957800312));
#27674=CARTESIAN_POINT('Ctrl Pts',(-0.2348081643589,1.123983684464,-3.498916133646));
#27675=CARTESIAN_POINT('Ctrl Pts',(0.329952574922,1.170452920957,-3.536832800312));
#27676=CARTESIAN_POINT('Ctrl Pts',(1.016551442463,0.6677408946504,-3.593707800312));
#27677=CARTESIAN_POINT('Ctrl Pts',(1.205358893105,-0.1619074151071,-3.650582800312));
#27678=CARTESIAN_POINT('Ctrl Pts',(0.8042879589087,-0.9122802996697,-3.707457800312));
#27679=CARTESIAN_POINT('Ctrl Pts',(0.009550993186479,-1.216158607898,-3.764332800312));
#27680=CARTESIAN_POINT('Ctrl Pts',(-0.7898556864549,-0.9248023542725,-3.821207800312));
#27681=CARTESIAN_POINT('Ctrl Pts',(-1.202679571961,-0.180814804896,-3.878082800312));
#27682=CARTESIAN_POINT('Ctrl Pts',(-1.026867975908,0.6516702524068,-3.934957800312));
#27683=CARTESIAN_POINT('Ctrl Pts',(-0.348469933747,1.165204139133,-3.991832800312));
#27684=CARTESIAN_POINT('Ctrl Pts',(0.5004819949382,1.108444747226,-4.048707800312));
#27685=CARTESIAN_POINT('Ctrl Pts',(1.104479823299,0.5091721726955,-4.105582800312));
#27686=CARTESIAN_POINT('Ctrl Pts',(1.167905052019,-0.3393077836576,-4.162457800312));
#27687=CARTESIAN_POINT('Ctrl Pts',(0.6597150647482,-1.02171816845,-4.219332800312));
#27688=CARTESIAN_POINT('Ctrl Pts',(-0.1713634724997,-1.204062516105,-4.276207800312));
#27689=CARTESIAN_POINT('Ctrl Pts',(-0.9185704929214,-0.7970948701029,-4.333082800312));
#27690=CARTESIAN_POINT('Ctrl Pts',(-1.216195700701,0.,-4.389957800312));
#27691=CARTESIAN_POINT('Ctrl Pts',(-0.9185704929214,0.7970948701029,-4.446832800312));
#27692=CARTESIAN_POINT('Ctrl Pts',(-0.1713634724997,1.204062516105,-4.503707800312));
#27693=CARTESIAN_POINT('Ctrl Pts',(0.6597150647482,1.02171816845,-4.560582800312));
#27694=CARTESIAN_POINT('Ctrl Pts',(1.167905052019,0.3393077836576,-4.617457800312));
#27695=CARTESIAN_POINT('Ctrl Pts',(1.104479823299,-0.5091721726955,-4.674332800312));
#27696=CARTESIAN_POINT('Ctrl Pts',(0.5004819949382,-1.108444747226,-4.731207800312));
#27697=CARTESIAN_POINT('Ctrl Pts',(-0.348469933747,-1.165204139133,-4.788082800312));
#27698=CARTESIAN_POINT('Ctrl Pts',(-1.026867975908,-0.6516702524068,-4.844957800312));
#27699=CARTESIAN_POINT('Ctrl Pts',(-1.202679571961,0.180814804896,-4.901832800312));
#27700=CARTESIAN_POINT('Ctrl Pts',(-0.7898556864549,0.9248023542725,-4.958707800312));
#27701=CARTESIAN_POINT('Ctrl Pts',(0.00955099318648,1.216158607898,-5.015582800312));
#27702=CARTESIAN_POINT('Ctrl Pts',(0.8042879589087,0.9122802996697,-5.072457800312));
#27703=CARTESIAN_POINT('Ctrl Pts',(1.205358893105,0.161907415107,-5.129332800312));
#27704=CARTESIAN_POINT('Ctrl Pts',(1.016551442463,-0.6677408946504,-5.186207800312));
#27705=CARTESIAN_POINT('Ctrl Pts',(0.329952574922,-1.170452920957,-5.243082800312));
#27706=CARTESIAN_POINT('Ctrl Pts',(-0.2348081643589,-1.123983684464,-5.280999466979));
#27707=CARTESIAN_POINT('Ctrl Pts',(-0.4755900604755,-1.010680324589,-5.299957800312));
#27708=CARTESIAN_POINT('Ctrl Pts',(-0.4755900604755,1.010680324589,-3.509873400937));
#27709=CARTESIAN_POINT('Ctrl Pts',(-0.2348081643589,1.123983684464,-3.52883173427));
#27710=CARTESIAN_POINT('Ctrl Pts',(0.329952574922,1.170452920957,-3.566748400937));
#27711=CARTESIAN_POINT('Ctrl Pts',(1.016551442463,0.6677408946504,-3.623623400937));
#27712=CARTESIAN_POINT('Ctrl Pts',(1.205358893105,-0.1619074151071,-3.680498400937));
#27713=CARTESIAN_POINT('Ctrl Pts',(0.8042879589087,-0.9122802996697,-3.737373400937));
#27714=CARTESIAN_POINT('Ctrl Pts',(0.009550993186479,-1.216158607898,-3.794248400937));
#27715=CARTESIAN_POINT('Ctrl Pts',(-0.7898556864549,-0.9248023542725,-3.851123400937));
#27716=CARTESIAN_POINT('Ctrl Pts',(-1.202679571961,-0.180814804896,-3.907998400937));
#27717=CARTESIAN_POINT('Ctrl Pts',(-1.026867975908,0.6516702524068,-3.964873400937));
#27718=CARTESIAN_POINT('Ctrl Pts',(-0.348469933747,1.165204139133,-4.021748400937));
#27719=CARTESIAN_POINT('Ctrl Pts',(0.5004819949382,1.108444747226,-4.078623400937));
#27720=CARTESIAN_POINT('Ctrl Pts',(1.104479823299,0.5091721726955,-4.135498400937));
#27721=CARTESIAN_POINT('Ctrl Pts',(1.167905052019,-0.3393077836576,-4.192373400937));
#27722=CARTESIAN_POINT('Ctrl Pts',(0.6597150647482,-1.02171816845,-4.249248400937));
#27723=CARTESIAN_POINT('Ctrl Pts',(-0.1713634724997,-1.204062516105,-4.306123400937));
#27724=CARTESIAN_POINT('Ctrl Pts',(-0.9185704929214,-0.7970948701029,-4.362998400937));
#27725=CARTESIAN_POINT('Ctrl Pts',(-1.216195700701,0.,-4.419873400937));
#27726=CARTESIAN_POINT('Ctrl Pts',(-0.9185704929214,0.7970948701029,-4.476748400937));
#27727=CARTESIAN_POINT('Ctrl Pts',(-0.1713634724997,1.204062516105,-4.533623400937));
#27728=CARTESIAN_POINT('Ctrl Pts',(0.6597150647482,1.02171816845,-4.590498400937));
#27729=CARTESIAN_POINT('Ctrl Pts',(1.167905052019,0.3393077836576,-4.647373400937));
#27730=CARTESIAN_POINT('Ctrl Pts',(1.104479823299,-0.5091721726955,-4.704248400937));
#27731=CARTESIAN_POINT('Ctrl Pts',(0.5004819949382,-1.108444747226,-4.761123400937));
#27732=CARTESIAN_POINT('Ctrl Pts',(-0.348469933747,-1.165204139133,-4.817998400937));
#27733=CARTESIAN_POINT('Ctrl Pts',(-1.026867975908,-0.6516702524068,-4.874873400937));
#27734=CARTESIAN_POINT('Ctrl Pts',(-1.202679571961,0.180814804896,-4.931748400937));
#27735=CARTESIAN_POINT('Ctrl Pts',(-0.7898556864549,0.9248023542725,-4.988623400937));
#27736=CARTESIAN_POINT('Ctrl Pts',(0.00955099318648,1.216158607898,-5.045498400937));
#27737=CARTESIAN_POINT('Ctrl Pts',(0.8042879589087,0.9122802996697,-5.102373400937));
#27738=CARTESIAN_POINT('Ctrl Pts',(1.205358893105,0.161907415107,-5.159248400937));
#27739=CARTESIAN_POINT('Ctrl Pts',(1.016551442463,-0.6677408946504,-5.216123400937));
#27740=CARTESIAN_POINT('Ctrl Pts',(0.329952574922,-1.170452920957,-5.272998400937));
#27741=CARTESIAN_POINT('Ctrl Pts',(-0.2348081643589,-1.123983684464,-5.310915067604));
#27742=CARTESIAN_POINT('Ctrl Pts',(-0.4755900604755,-1.010680324589,-5.329873400937));
#27743=CARTESIAN_POINT('',(3.48982018972651E-10,-1.11698717731251,-5.27886751164369));
#27744=CARTESIAN_POINT('',(0.,-1.116987298108,-5.221132486541));
#27745=CARTESIAN_POINT('Ctrl Pts',(1.88721574551803E-6,1.11628565378659,
-3.52884910577848));
#27746=CARTESIAN_POINT('Ctrl Pts',(0.094547613691279,1.11645975869105,-3.53558517666919));
#27747=CARTESIAN_POINT('Ctrl Pts',(0.189124462134141,1.10484916429063,-3.5423272697765));
#27748=CARTESIAN_POINT('Ctrl Pts',(0.372801878429929,1.05728988862636,-3.55586972723853));
#27749=CARTESIAN_POINT('Ctrl Pts',(0.461203748610714,1.0212041755292,-3.56262550562908));
#27750=CARTESIAN_POINT('Ctrl Pts',(0.668471432388828,0.904915646636025,
-3.57955576649842));
#27751=CARTESIAN_POINT('Ctrl Pts',(0.780383055419241,0.811029500761451,
-3.58976498118421));
#27752=CARTESIAN_POINT('Ctrl Pts',(0.97735254996311,0.567498199932464,-3.61210279000144));
#27753=CARTESIAN_POINT('Ctrl Pts',(1.03703915589554,0.431145768277837,-3.62249380692754));
#27754=CARTESIAN_POINT('Ctrl Pts',(1.11066616674449,0.17804237558142,-3.64126431930581));
#27755=CARTESIAN_POINT('Ctrl Pts',(1.1250370353998,0.0352369170928312,-3.65130636574828));
#27756=CARTESIAN_POINT('Ctrl Pts',(1.09418460733438,-0.296790717289799,
-3.67509692704671));
#27757=CARTESIAN_POINT('Ctrl Pts',(1.02997735713431,-0.440477084842101,
-3.68601884316657));
#27758=CARTESIAN_POINT('Ctrl Pts',(0.925588908242806,-0.636392952388531,
-3.70182493170545));
#27759=CARTESIAN_POINT('Ctrl Pts',(0.840538191683137,-0.751460714065268,
-3.71183701528019));
#27760=CARTESIAN_POINT('Ctrl Pts',(0.61118224779974,-0.946513834085734,
-3.73331976958516));
#27761=CARTESIAN_POINT('Ctrl Pts',(0.478234529751121,-1.0191711099922,-3.74390080177506));
#27762=CARTESIAN_POINT('Ctrl Pts',(0.222597234321247,-1.1004636264182,-3.76300274809229));
#27763=CARTESIAN_POINT('Ctrl Pts',(0.0794663775051982,-1.12675755955542,
-3.77317074675688));
#27764=CARTESIAN_POINT('Ctrl Pts',(-0.232981315456759,-1.10176800386665,
-3.79552756527266));
#27765=CARTESIAN_POINT('Ctrl Pts',(-0.377700605109011,-1.06037143957915,
-3.8060369702747));
#27766=CARTESIAN_POINT('Ctrl Pts',(-0.604852724324492,-0.94473173616764,
-3.82419440550631));
#27767=CARTESIAN_POINT('Ctrl Pts',(-0.731331226988429,-0.863974006299976,
-3.83465639462863));
#27768=CARTESIAN_POINT('Ctrl Pts',(-0.943397907937854,-0.613934547622002,
-3.8580266301717));
#27769=CARTESIAN_POINT('Ctrl Pts',(-1.01607631574406,-0.484189787750189,
-3.86841215189081));
#27770=CARTESIAN_POINT('Ctrl Pts',(-1.11857306467121,-0.173002860562982,
-3.89176437012636));
#27771=CARTESIAN_POINT('Ctrl Pts',(-1.12165266273671,-0.0230529286473959,
-3.90222238737627));
#27772=CARTESIAN_POINT('Ctrl Pts',(-1.10179845703878,0.228016486144733,
-3.92016430609243));
#27773=CARTESIAN_POINT('Ctrl Pts',(-1.06324590215937,0.369253565391362,
-3.93039583379269));
#27774=CARTESIAN_POINT('Ctrl Pts',(-0.924464855646203,0.649976757040024,
-3.95272861706242));
#27775=CARTESIAN_POINT('Ctrl Pts',(-0.825915661788619,0.761161572818574,
-3.96310258159157));
#27776=CARTESIAN_POINT('Ctrl Pts',(-0.626214316349861,0.934430304671198,
-3.98193040825594));
#27777=CARTESIAN_POINT('Ctrl Pts',(-0.502214996937548,1.00732385711169,
-3.99199298816798));
#27778=CARTESIAN_POINT('Ctrl Pts',(-0.191201997533737,1.11682300306852,
-4.01551693664132));
#27779=CARTESIAN_POINT('Ctrl Pts',(-0.0349012702549876,1.12007370080308,
-4.02638015858152));
#27780=CARTESIAN_POINT('Ctrl Pts',(0.203851405860731,1.1061171885703,-4.04340869558083));
#27781=CARTESIAN_POINT('Ctrl Pts',(0.34178611259702,1.07261170247852,-4.05334911559688));
#27782=CARTESIAN_POINT('Ctrl Pts',(0.603413551668515,0.951563052462852,
-4.07391815996146));
#27783=CARTESIAN_POINT('Ctrl Pts',(0.725113385898937,0.861211673415834,
-4.08450451982865));
#27784=CARTESIAN_POINT('Ctrl Pts',(0.905273423514475,0.663857977873339,
-4.10353245208202));
#27785=CARTESIAN_POINT('Ctrl Pts',(0.989304020610891,0.545163021076615,
-4.11369254095246));
#27786=CARTESIAN_POINT('Ctrl Pts',(1.09791444748826,0.250846118613209,-4.13607028582539));
#27787=CARTESIAN_POINT('Ctrl Pts',(1.12102369397598,0.101931202388127,-4.14659192327522));
#27788=CARTESIAN_POINT('Ctrl Pts',(1.11127472608704,-0.152382998725977,
-4.16472029922507));
#27789=CARTESIAN_POINT('Ctrl Pts',(1.09120934524513,-0.3009388152065,-4.17517036237664));
#27790=CARTESIAN_POINT('Ctrl Pts',(0.953355092950196,-0.598483057720636,
-4.19854743454185));
#27791=CARTESIAN_POINT('Ctrl Pts',(0.865889506205136,-0.719096632405867,
-4.20895154517146));
#27792=CARTESIAN_POINT('Ctrl Pts',(0.630908211369377,-0.938430669099238,
-4.23186059631055));
#27793=CARTESIAN_POINT('Ctrl Pts',(0.499473987912868,-1.00559671816684,
-4.24216596514538));
#27794=CARTESIAN_POINT('Ctrl Pts',(0.254954649474665,-1.09592824110064,
-4.26073734053109));
#27795=CARTESIAN_POINT('Ctrl Pts',(0.110233508147556,-1.12012616746575,
-4.27099044678715));
#27796=CARTESIAN_POINT('Ctrl Pts',(-0.202625788977262,-1.11169037854405,
-4.29330877782005));
#27797=CARTESIAN_POINT('Ctrl Pts',(-0.34459406256499,-1.06910154094398,
-4.30366009735837));
#27798=CARTESIAN_POINT('Ctrl Pts',(-0.586363065095521,-0.959974916638415,
-4.32255024413075));
#27799=CARTESIAN_POINT('Ctrl Pts',(-0.704733656287596,-0.877644037487909,
-4.33263575715875));
#27800=CARTESIAN_POINT('Ctrl Pts',(-0.924445762808999,-0.651144082671885,
-4.35514789486952));
#27801=CARTESIAN_POINT('Ctrl Pts',(-0.99587830302718,-0.517818669122217,
-4.36569215217414));
#27802=CARTESIAN_POINT('Ctrl Pts',(-1.08982166380632,-0.277939862987316,
-4.38403504577381));
#27803=CARTESIAN_POINT('Ctrl Pts',(-1.1169872981078,-0.139044412854727,
-4.39394629670335));
#27804=CARTESIAN_POINT('Ctrl Pts',(-1.1169872981078,0.139044412854725,-4.41378873021465));
#27805=CARTESIAN_POINT('Ctrl Pts',(-1.08982166380632,0.277939862987314,
-4.42369998114575));
#27806=CARTESIAN_POINT('Ctrl Pts',(-0.995878303027181,0.517818669122213,
-4.44204287474531));
#27807=CARTESIAN_POINT('Ctrl Pts',(-0.924445762809003,0.651144082671879,
-4.45258713204978));
#27808=CARTESIAN_POINT('Ctrl Pts',(-0.704733656287605,0.877644037487902,
-4.47509926976052));
#27809=CARTESIAN_POINT('Ctrl Pts',(-0.586363065095532,0.959974916638408,
-4.4851847827886));
#27810=CARTESIAN_POINT('Ctrl Pts',(-0.344594062565008,1.06910154094397,
-4.50407492956103));
#27811=CARTESIAN_POINT('Ctrl Pts',(-0.202625788977281,1.11169037854405,
-4.51442624909944));
#27812=CARTESIAN_POINT('Ctrl Pts',(0.110233508147534,1.12012616746575,-4.53674458013225));
#27813=CARTESIAN_POINT('Ctrl Pts',(0.254954649474639,1.09592824110065,-4.54699768638819));
#27814=CARTESIAN_POINT('Ctrl Pts',(0.499473987912787,1.00559671816687,-4.56556906177377));
#27815=CARTESIAN_POINT('Ctrl Pts',(0.630908211369306,0.938430669099295,
-4.57587443060851));
#27816=CARTESIAN_POINT('Ctrl Pts',(0.865889506205103,0.719096632405906,
-4.59878348174746));
#27817=CARTESIAN_POINT('Ctrl Pts',(0.953355092950165,0.598483057720684,
-4.60918759237697));
#27818=CARTESIAN_POINT('Ctrl Pts',(1.09120934524511,0.300938815206566,-4.63256466454204));
#27819=CARTESIAN_POINT('Ctrl Pts',(1.11127472608703,0.15238299872605,-4.64301472769358));
#27820=CARTESIAN_POINT('Ctrl Pts',(1.12102369397598,-0.101931202388062,
-4.66114310364352));
#27821=CARTESIAN_POINT('Ctrl Pts',(1.09791444748828,-0.250846118613148,
-4.67166474109352));
#27822=CARTESIAN_POINT('Ctrl Pts',(0.989304020610918,-0.545163021076567,
-4.69404248596659));
#27823=CARTESIAN_POINT('Ctrl Pts',(0.905273423514505,-0.663857977873301,
-4.70420257483704));
#27824=CARTESIAN_POINT('Ctrl Pts',(0.725113385898968,-0.861211673415808,
-4.72323050709035));
#27825=CARTESIAN_POINT('Ctrl Pts',(0.603413551668551,-0.951563052462828,
-4.73381686695739));
#27826=CARTESIAN_POINT('Ctrl Pts',(0.341786112597057,-1.07261170247851,
-4.754385911322));
#27827=CARTESIAN_POINT('Ctrl Pts',(0.203851405860766,-1.10611718857029,
-4.76432633133819));
#27828=CARTESIAN_POINT('Ctrl Pts',(-0.0349012702549451,-1.12007370080308,
-4.78135486833769));
#27829=CARTESIAN_POINT('Ctrl Pts',(-0.191201997533703,-1.11682300306853,
-4.79221809027819));
#27830=CARTESIAN_POINT('Ctrl Pts',(-0.502214996937524,-1.0073238571117,
-4.81574203875154));
#27831=CARTESIAN_POINT('Ctrl Pts',(-0.626214316349838,-0.934430304671214,
-4.82580461866342));
#27832=CARTESIAN_POINT('Ctrl Pts',(-0.825915661788601,-0.761161572818594,
-4.84463244532759));
#27833=CARTESIAN_POINT('Ctrl Pts',(-0.924464855646184,-0.64997675704005,
-4.85500640985651));
#27834=CARTESIAN_POINT('Ctrl Pts',(-1.06324590215936,-0.369253565391402,
-4.87733919312616));
#27835=CARTESIAN_POINT('Ctrl Pts',(-1.10179845703877,-0.228016486144777,
-4.88757072082646));
#27836=CARTESIAN_POINT('Ctrl Pts',(-1.1216526627367,0.023052928647293,-4.90551263954267));
#27837=CARTESIAN_POINT('Ctrl Pts',(-1.11857306467123,0.173002860562897,
-4.91597065679267));
#27838=CARTESIAN_POINT('Ctrl Pts',(-1.01607631574408,0.484189787750149,
-4.93932287502831));
#27839=CARTESIAN_POINT('Ctrl Pts',(-0.943397907937877,0.613934547621966,
-4.94970839674746));
#27840=CARTESIAN_POINT('Ctrl Pts',(-0.73133122698847,0.863974006299937,
-4.97307863229059));
#27841=CARTESIAN_POINT('Ctrl Pts',(-0.604852724324544,0.94473173616761,
-4.98354062141293));
#27842=CARTESIAN_POINT('Ctrl Pts',(-0.377700605109039,1.06037143957914,
-5.00169805664457));
#27843=CARTESIAN_POINT('Ctrl Pts',(-0.232981315456788,1.10176800386664,
-5.01220746164662));
#27844=CARTESIAN_POINT('Ctrl Pts',(0.0794663775051714,1.12675755955542,
-5.03456428016241));
#27845=CARTESIAN_POINT('Ctrl Pts',(0.222597234321221,1.1004636264182,-5.044732278827));
#27846=CARTESIAN_POINT('Ctrl Pts',(0.478234529751088,1.01917110999221,-5.06383422514421));
#27847=CARTESIAN_POINT('Ctrl Pts',(0.6111822477997,0.946513834085752,-5.07441525733413));
#27848=CARTESIAN_POINT('Ctrl Pts',(0.84053819168314,0.751460714065252,-5.09589801163899));
#27849=CARTESIAN_POINT('Ctrl Pts',(0.925588908242792,0.636392952388495,
-5.10591009521358));
#27850=CARTESIAN_POINT('Ctrl Pts',(1.02997735713436,0.440477084841974,-5.12171618375232));
#27851=CARTESIAN_POINT('Ctrl Pts',(1.09418460733437,0.296790717289649,-5.13263809987195));
#27852=CARTESIAN_POINT('Ctrl Pts',(1.1250370353998,-0.0352369170928343,
-5.15642866117045));
#27853=CARTESIAN_POINT('Ctrl Pts',(1.1106661667445,-0.178042375581416,-5.16647070761313));
#27854=CARTESIAN_POINT('Ctrl Pts',(1.03703915589556,-0.43114576827782,-5.18524121999161));
#27855=CARTESIAN_POINT('Ctrl Pts',(0.977352549963136,-0.567498199932438,
-5.19563223691795));
#27856=CARTESIAN_POINT('Ctrl Pts',(0.780383055419275,-0.811029500761424,
-5.21797004573512));
#27857=CARTESIAN_POINT('Ctrl Pts',(0.668471432388861,-0.904915646636002,
-5.22817926042075));
#27858=CARTESIAN_POINT('Ctrl Pts',(0.461203748610963,-1.02120417552907,
-5.24510952128986));
#27859=CARTESIAN_POINT('Ctrl Pts',(0.372801878430432,-1.05728988862616,
-5.25186529968028));
#27860=CARTESIAN_POINT('Ctrl Pts',(0.189124507262871,-1.1048491526056,-5.26540775381488));
#27861=CARTESIAN_POINT('Ctrl Pts',(0.094547706959721,-1.11645974724111,
-5.27214984360044));
#27862=CARTESIAN_POINT('Ctrl Pts',(2.02707199375124E-6,-1.11628565404413,
-5.27888591117587));
#27863=CARTESIAN_POINT('Ctrl Pts',(-0.4696881186261,0.9981380597272,-3.485864569721));
#27864=CARTESIAN_POINT('Ctrl Pts',(-0.2318942596183,1.110035356068,-3.504822903054));
#27865=CARTESIAN_POINT('Ctrl Pts',(0.3258579542137,1.155927922117,-3.542739569721));
#27866=CARTESIAN_POINT('Ctrl Pts',(1.003936318643,0.6594544137959,-3.599614569721));
#27867=CARTESIAN_POINT('Ctrl Pts',(1.190400720751,-0.1598981886148,-3.656489569721));
#27868=CARTESIAN_POINT('Ctrl Pts',(0.7943069665412,-0.9009591520544,-3.713364569721));
#27869=CARTESIAN_POINT('Ctrl Pts',(0.009432467987835,-1.201066414053,-3.770239569721));
#27870=CARTESIAN_POINT('Ctrl Pts',(-0.7800537946193,-0.9133258114035,-3.827114569721));
#27871=CARTESIAN_POINT('Ctrl Pts',(-1.187754649245,-0.1785709428966,-3.883989569721));
#27872=CARTESIAN_POINT('Ctrl Pts',(-1.014124826746,0.6435832038027,-3.940864569721));
#27873=CARTESIAN_POINT('Ctrl Pts',(-0.3441455177085,1.150744276231,-3.997739569721));
#27874=CARTESIAN_POINT('Ctrl Pts',(0.4942711510281,1.094689252768,-4.054614569721));
#27875=CARTESIAN_POINT('Ctrl Pts',(1.090773532456,0.5028534860695,-4.111489569721));
#27876=CARTESIAN_POINT('Ctrl Pts',(1.153411671532,-0.3350970673819,-4.168364569721));
#27877=CARTESIAN_POINT('Ctrl Pts',(0.6515281822355,-1.009038926982,-4.225239569721));
#27878=CARTESIAN_POINT('Ctrl Pts',(-0.169236898936,-1.189120431432,-4.282114569721));
#27879=CARTESIAN_POINT('Ctrl Pts',(-0.9071712857378,-0.7872031419892,-4.338989569721));
#27880=CARTESIAN_POINT('Ctrl Pts',(-1.201103046544,0.,-4.395864569721));
#27881=CARTESIAN_POINT('Ctrl Pts',(-0.9071712857378,0.7872031419892,-4.452739569721));
#27882=CARTESIAN_POINT('Ctrl Pts',(-0.169236898936,1.189120431432,-4.509614569721));
#27883=CARTESIAN_POINT('Ctrl Pts',(0.6515281822355,1.009038926982,-4.566489569721));
#27884=CARTESIAN_POINT('Ctrl Pts',(1.153411671532,0.3350970673819,-4.623364569721));
#27885=CARTESIAN_POINT('Ctrl Pts',(1.090773532456,-0.5028534860695,-4.680239569721));
#27886=CARTESIAN_POINT('Ctrl Pts',(0.4942711510281,-1.094689252768,-4.737114569721));
#27887=CARTESIAN_POINT('Ctrl Pts',(-0.3441455177085,-1.150744276231,-4.793989569721));
#27888=CARTESIAN_POINT('Ctrl Pts',(-1.014124826746,-0.6435832038027,-4.850864569721));
#27889=CARTESIAN_POINT('Ctrl Pts',(-1.187754649245,0.1785709428966,-4.907739569721));
#27890=CARTESIAN_POINT('Ctrl Pts',(-0.7800537946193,0.9133258114035,-4.964614569721));
#27891=CARTESIAN_POINT('Ctrl Pts',(0.009432467987837,1.201066414053,-5.021489569721));
#27892=CARTESIAN_POINT('Ctrl Pts',(0.7943069665412,0.9009591520544,-5.078364569721));
#27893=CARTESIAN_POINT('Ctrl Pts',(1.190400720751,0.1598981886148,-5.135239569721));
#27894=CARTESIAN_POINT('Ctrl Pts',(1.003936318643,-0.6594544137959,-5.192114569721));
#27895=CARTESIAN_POINT('Ctrl Pts',(0.3258579542137,-1.155927922117,-5.248989569721));
#27896=CARTESIAN_POINT('Ctrl Pts',(-0.2318942596183,-1.110035356068,-5.286906236387));
#27897=CARTESIAN_POINT('Ctrl Pts',(-0.4696881186261,-0.9981380597272,-5.305864569721));
#27898=CARTESIAN_POINT('Ctrl Pts',(-0.5279823721497,1.122019654338,-3.564910694393));
#27899=CARTESIAN_POINT('Ctrl Pts',(-0.2606752788197,1.247804824574,-3.583869027727));
#27900=CARTESIAN_POINT('Ctrl Pts',(0.3663010598456,1.299393240218,-3.621785694393));
#27901=CARTESIAN_POINT('Ctrl Pts',(1.128537550737,0.7413010717389,-3.678660694393));
#27902=CARTESIAN_POINT('Ctrl Pts',(1.33814455045,-0.1797435821333,-3.735535694393));
#27903=CARTESIAN_POINT('Ctrl Pts',(0.892890536887,-1.012779611507,-3.792410694393));
#27904=CARTESIAN_POINT('Ctrl Pts',(0.01060315691615,-1.350133991585,-3.849285694393));
#27905=CARTESIAN_POINT('Ctrl Pts',(-0.8768683655278,-1.026681130153,-3.906160694393));
#27906=CARTESIAN_POINT('Ctrl Pts',(-1.335170067905,-0.2007338620856,-3.963035694393));
#27907=CARTESIAN_POINT('Ctrl Pts',(-1.139990581936,0.723460043259,-4.019910694393));
#27908=CARTESIAN_POINT('Ctrl Pts',(-0.3868583419482,1.293566238123,-4.076785694393));
#27909=CARTESIAN_POINT('Ctrl Pts',(0.555616470709,1.230554075189,-4.133660694393));
#27910=CARTESIAN_POINT('Ctrl Pts',(1.226152364316,0.5652639823961,-4.190535694393));
#27911=CARTESIAN_POINT('Ctrl Pts',(1.296564691016,-0.3766868641562,-4.247410694393));
#27912=CARTESIAN_POINT('Ctrl Pts',(0.7323910942975,-1.134273457497,-4.304285694393));
#27913=CARTESIAN_POINT('Ctrl Pts',(-0.190241344867,-1.336705360987,-4.361160694393));
#27914=CARTESIAN_POINT('Ctrl Pts',(-1.019762749782,-0.8849050375959,-4.418035694393));
#27915=CARTESIAN_POINT('Ctrl Pts',(-1.350175170634,0.,-4.474910694393));
#27916=CARTESIAN_POINT('Ctrl Pts',(-1.019762749782,0.8849050375959,-4.531785694393));
#27917=CARTESIAN_POINT('Ctrl Pts',(-0.190241344867,1.336705360987,-4.588660694393));
#27918=CARTESIAN_POINT('Ctrl Pts',(0.7323910942975,1.134273457497,-4.645535694393));
#27919=CARTESIAN_POINT('Ctrl Pts',(1.296564691016,0.3766868641562,-4.702410694393));
#27920=CARTESIAN_POINT('Ctrl Pts',(1.226152364316,-0.5652639823961,-4.759285694393));
#27921=CARTESIAN_POINT('Ctrl Pts',(0.555616470709,-1.230554075189,-4.816160694393));
#27922=CARTESIAN_POINT('Ctrl Pts',(-0.3868583419482,-1.293566238123,-4.873035694393));
#27923=CARTESIAN_POINT('Ctrl Pts',(-1.139990581936,-0.723460043259,-4.929910694393));
#27924=CARTESIAN_POINT('Ctrl Pts',(-1.335170067905,0.2007338620856,-4.986785694393));
#27925=CARTESIAN_POINT('Ctrl Pts',(-0.8768683655278,1.026681130153,-5.043660694393));
#27926=CARTESIAN_POINT('Ctrl Pts',(0.01060315691615,1.350133991585,-5.100535694393));
#27927=CARTESIAN_POINT('Ctrl Pts',(0.892890536887,1.012779611507,-5.157410694393));
#27928=CARTESIAN_POINT('Ctrl Pts',(1.33814455045,0.1797435821333,-5.214285694393));
#27929=CARTESIAN_POINT('Ctrl Pts',(1.128537550737,-0.7413010717389,-5.271160694393));
#27930=CARTESIAN_POINT('Ctrl Pts',(0.3663010598456,-1.299393240218,-5.328035694393));
#27931=CARTESIAN_POINT('Ctrl Pts',(-0.2606752788197,-1.247804824574,-5.36595236106));
#27932=CARTESIAN_POINT('Ctrl Pts',(-0.5279823721497,-1.122019654338,-5.384910694393));
#27933=CARTESIAN_POINT('Ctrl Pts',(-0.5862766256734,1.24590124895,-3.643956819066));
#27934=CARTESIAN_POINT('Ctrl Pts',(-0.2894562980212,1.38557429308,-3.662915152399));
#27935=CARTESIAN_POINT('Ctrl Pts',(0.4067441654775,1.442858558319,-3.700831819066));
#27936=CARTESIAN_POINT('Ctrl Pts',(1.253138782831,0.823147729682,-3.757706819066));
#27937=CARTESIAN_POINT('Ctrl Pts',(1.48588838015,-0.1995889756518,-3.814581819066));
#27938=CARTESIAN_POINT('Ctrl Pts',(0.9914741072328,-1.12460007096,-3.871456819066));
#27939=CARTESIAN_POINT('Ctrl Pts',(0.01177384584447,-1.499201569118,-3.928331819066));
#27940=CARTESIAN_POINT('Ctrl Pts',(-0.9736829364363,-1.140036448902,-3.985206819066));
#27941=CARTESIAN_POINT('Ctrl Pts',(-1.482585486565,-0.2228967812747,-4.042081819066));
#27942=CARTESIAN_POINT('Ctrl Pts',(-1.265856337127,0.8033368827153,-4.098956819066));
#27943=CARTESIAN_POINT('Ctrl Pts',(-0.4295711661878,1.436388200015,-4.155831819066));
#27944=CARTESIAN_POINT('Ctrl Pts',(0.61696179039,1.36641889761,-4.212706819066));
#27945=CARTESIAN_POINT('Ctrl Pts',(1.361531196175,0.6276744787227,-4.269581819066));
#27946=CARTESIAN_POINT('Ctrl Pts',(1.439717710501,-0.4182766609306,-4.326456819066));
#27947=CARTESIAN_POINT('Ctrl Pts',(0.8132540063595,-1.259507988013,-4.383331819066));
#27948=CARTESIAN_POINT('Ctrl Pts',(-0.211245790798,-1.484290290542,-4.440206819066));
#27949=CARTESIAN_POINT('Ctrl Pts',(-1.132354213826,-0.9826069332027,-4.497081819066));
#27950=CARTESIAN_POINT('Ctrl Pts',(-1.499247294724,0.,-4.553956819066));
#27951=CARTESIAN_POINT('Ctrl Pts',(-1.132354213826,0.9826069332027,-4.610831819066));
#27952=CARTESIAN_POINT('Ctrl Pts',(-0.211245790798,1.484290290542,-4.667706819066));
#27953=CARTESIAN_POINT('Ctrl Pts',(0.8132540063595,1.259507988013,-4.724581819066));
#27954=CARTESIAN_POINT('Ctrl Pts',(1.439717710501,0.4182766609306,-4.781456819066));
#27955=CARTESIAN_POINT('Ctrl Pts',(1.361531196175,-0.6276744787227,-4.838331819066));
#27956=CARTESIAN_POINT('Ctrl Pts',(0.61696179039,-1.36641889761,-4.895206819066));
#27957=CARTESIAN_POINT('Ctrl Pts',(-0.4295711661878,-1.436388200015,-4.952081819066));
#27958=CARTESIAN_POINT('Ctrl Pts',(-1.265856337127,-0.8033368827153,-5.008956819066));
#27959=CARTESIAN_POINT('Ctrl Pts',(-1.482585486565,0.2228967812747,-5.065831819066));
#27960=CARTESIAN_POINT('Ctrl Pts',(-0.9736829364363,1.140036448902,-5.122706819066));
#27961=CARTESIAN_POINT('Ctrl Pts',(0.01177384584447,1.499201569118,-5.179581819066));
#27962=CARTESIAN_POINT('Ctrl Pts',(0.9914741072328,1.12460007096,-5.236456819066));
#27963=CARTESIAN_POINT('Ctrl Pts',(1.48588838015,0.1995889756517,-5.293331819066));
#27964=CARTESIAN_POINT('Ctrl Pts',(1.253138782831,-0.823147729682,-5.350206819066));
#27965=CARTESIAN_POINT('Ctrl Pts',(0.4067441654775,-1.442858558319,-5.407081819066));
#27966=CARTESIAN_POINT('Ctrl Pts',(-0.2894562980212,-1.38557429308,-5.444998485733));
#27967=CARTESIAN_POINT('Ctrl Pts',(-0.5862766256734,-1.24590124895,-5.463956819066));
#27968=CARTESIAN_POINT('Ctrl Pts',(-0.644570879197,1.369782843561,-3.723002943739));
#27969=CARTESIAN_POINT('Ctrl Pts',(-0.3182373172226,1.523343761587,-3.741961277072));
#27970=CARTESIAN_POINT('Ctrl Pts',(0.4471872711094,1.586323876419,-3.779877943739));
#27971=CARTESIAN_POINT('Ctrl Pts',(1.377740014924,0.904994387625,-3.836752943739));
#27972=CARTESIAN_POINT('Ctrl Pts',(1.633632209849,-0.2194343691702,-3.893627943739));
#27973=CARTESIAN_POINT('Ctrl Pts',(1.090057677579,-1.236420530413,-3.950502943739));
#27974=CARTESIAN_POINT('Ctrl Pts',(0.01294453477278,-1.648269146651,-4.007377943739));
#27975=CARTESIAN_POINT('Ctrl Pts',(-1.070497507345,-1.253391767652,-4.064252943739));
#27976=CARTESIAN_POINT('Ctrl Pts',(-1.630000905225,-0.2450597004638,-4.121127943739));
#27977=CARTESIAN_POINT('Ctrl Pts',(-1.391722092318,0.8832137221716,-4.178002943739));
#27978=CARTESIAN_POINT('Ctrl Pts',(-0.4722839904274,1.579210161907,-4.234877943739));
#27979=CARTESIAN_POINT('Ctrl Pts',(0.6783071100709,1.502283720031,-4.291752943739));
#27980=CARTESIAN_POINT('Ctrl Pts',(1.496910028035,0.6900849750494,-4.348627943739));
#27981=CARTESIAN_POINT('Ctrl Pts',(1.582870729986,-0.4598664577049,-4.405502943739));
#27982=CARTESIAN_POINT('Ctrl Pts',(0.8941169184216,-1.384742518528,-4.462377943739));
#27983=CARTESIAN_POINT('Ctrl Pts',(-0.232250236729,-1.631875220096,-4.519252943739));
#27984=CARTESIAN_POINT('Ctrl Pts',(-1.24494567787,-1.080308828809,-4.576127943739));
#27985=CARTESIAN_POINT('Ctrl Pts',(-1.648319418813,0.,-4.633002943739));
#27986=CARTESIAN_POINT('Ctrl Pts',(-1.24494567787,1.080308828809,-4.689877943739));
#27987=CARTESIAN_POINT('Ctrl Pts',(-0.232250236729,1.631875220096,-4.746752943739));
#27988=CARTESIAN_POINT('Ctrl Pts',(0.8941169184215,1.384742518528,-4.803627943739));
#27989=CARTESIAN_POINT('Ctrl Pts',(1.582870729986,0.4598664577049,-4.860502943739));
#27990=CARTESIAN_POINT('Ctrl Pts',(1.496910028035,-0.6900849750494,-4.917377943739));
#27991=CARTESIAN_POINT('Ctrl Pts',(0.6783071100709,-1.502283720031,-4.974252943739));
#27992=CARTESIAN_POINT('Ctrl Pts',(-0.4722839904274,-1.579210161907,-5.031127943739));
#27993=CARTESIAN_POINT('Ctrl Pts',(-1.391722092318,-0.8832137221716,-5.088002943739));
#27994=CARTESIAN_POINT('Ctrl Pts',(-1.630000905225,0.2450597004637,-5.144877943739));
#27995=CARTESIAN_POINT('Ctrl Pts',(-1.070497507345,1.253391767652,-5.201752943739));
#27996=CARTESIAN_POINT('Ctrl Pts',(0.01294453477278,1.648269146651,-5.258627943739));
#27997=CARTESIAN_POINT('Ctrl Pts',(1.090057677579,1.236420530413,-5.315502943739));
#27998=CARTESIAN_POINT('Ctrl Pts',(1.633632209849,0.2194343691702,-5.372377943739));
#27999=CARTESIAN_POINT('Ctrl Pts',(1.377740014924,-0.904994387625,-5.429252943739));
#28000=CARTESIAN_POINT('Ctrl Pts',(0.4471872711094,-1.586323876419,-5.486127943739));
#28001=CARTESIAN_POINT('Ctrl Pts',(-0.3182373172226,-1.523343761587,-5.524044610405));
#28002=CARTESIAN_POINT('Ctrl Pts',(-0.644570879197,-1.369782843561,-5.543002943739));
#28003=CARTESIAN_POINT('',(2.00265715005522E-9,-1.49923261689948,-5.49955700101554));
#28004=CARTESIAN_POINT('',(0.,-1.116987298108,-5.278867513459));
#28005=CARTESIAN_POINT('Ctrl Pts',(2.25467602528104E-5,-1.49898153326899,
-5.49997328559406));
#28006=CARTESIAN_POINT('Ctrl Pts',(0.134374632780694,-1.49921303139129,
-5.49283677341645));
#28007=CARTESIAN_POINT('Ctrl Pts',(0.268791711313178,-1.48175186835438,
-5.48571144240093));
#28008=CARTESIAN_POINT('Ctrl Pts',(0.528400848841846,-1.41037838885025,
-5.47147567834219));
#28009=CARTESIAN_POINT('Ctrl Pts',(0.652827217258384,-1.35636907961786,
-5.46434951866967));
#28010=CARTESIAN_POINT('Ctrl Pts',(0.931735289868362,-1.18914017573126,
-5.44707780898663));
#28011=CARTESIAN_POINT('Ctrl Pts',(1.0775086183468,-1.05993239151383,-5.4368919202179));
#28012=CARTESIAN_POINT('Ctrl Pts',(1.25254461905446,-0.831135380419128,
-5.42160664710595));
#28013=CARTESIAN_POINT('Ctrl Pts',(1.30304065093549,-0.749217256680278,
-5.41653951416285));
#28014=CARTESIAN_POINT('Ctrl Pts',(1.43181234949439,-0.48562302793946,-5.40097007701216));
#28015=CARTESIAN_POINT('Ctrl Pts',(1.48316633571126,-0.29136688504635,-5.39048349311008));
#28016=CARTESIAN_POINT('Ctrl Pts',(1.50934593665312,0.102298274369429,-5.36953593036026));
#28017=CARTESIAN_POINT('Ctrl Pts',(1.48352321036142,0.29707569525196,-5.35935212513633));
#28018=CARTESIAN_POINT('Ctrl Pts',(1.35557797560351,0.667978516742168,-5.33851892320214));
#28019=CARTESIAN_POINT('Ctrl Pts',(1.25672301292779,0.839706906902107,-5.32816967902004));
#28020=CARTESIAN_POINT('Ctrl Pts',(1.06762964134381,1.05767331909946,-5.31285466460304));
#28021=CARTESIAN_POINT('Ctrl Pts',(0.999122897304844,1.12299761706242,-5.30786873726412));
#28022=CARTESIAN_POINT('Ctrl Pts',(0.767475871655381,1.30345314303507,-5.29230751729651));
#28023=CARTESIAN_POINT('Ctrl Pts',(0.585984031534433,1.39346687732159,-5.28173765255888));
#28024=CARTESIAN_POINT('Ctrl Pts',(0.3002776975602,1.4720722090405,-5.26599600192716));
#28025=CARTESIAN_POINT('Ctrl Pts',(0.203413384541745,1.48897914475702,-5.26079850668725));
#28026=CARTESIAN_POINT('Ctrl Pts',(0.0102965460479719,1.50310836187032,
-5.25053280796051));
#28027=CARTESIAN_POINT('Ctrl Pts',(-0.084730733565112,1.50057825774572,
-5.24552882507392));
#28028=CARTESIAN_POINT('Ctrl Pts',(-0.371065819632636,1.46518482322893,
-5.23022026530771));
#28029=CARTESIAN_POINT('Ctrl Pts',(-0.558528756656742,1.40403954733574,
-5.21992086302571));
#28030=CARTESIAN_POINT('Ctrl Pts',(-0.901532905294185,1.21492371530542,
-5.19911971442108));
#28031=CARTESIAN_POINT('Ctrl Pts',(-1.05210340104688,1.0874442058747,-5.18889366548199));
#28032=CARTESIAN_POINT('Ctrl Pts',(-1.29645242039468,0.777009440525124,
-5.16791551248259));
#28033=CARTESIAN_POINT('Ctrl Pts',(-1.387965754438,0.598976339288918,-5.15746395273279));
#28034=CARTESIAN_POINT('Ctrl Pts',(-1.49653071624039,0.222284446845803,
-5.13665963474268));
#28035=CARTESIAN_POINT('Ctrl Pts',(-1.51209522263139,0.030383479807373,
-5.12667623865883));
#28036=CARTESIAN_POINT('Ctrl Pts',(-1.46756783108178,-0.362285702864463,
-5.10568820827822));
#28037=CARTESIAN_POINT('Ctrl Pts',(-1.40686737422156,-0.555204232228066,
-5.09513613303635));
#28038=CARTESIAN_POINT('Ctrl Pts',(-1.26475536972579,-0.812299777461656,
-5.07955745535228));
#28039=CARTESIAN_POINT('Ctrl Pts',(-1.21076619934412,-0.890422714394832,
-5.07455458596799));
#28040=CARTESIAN_POINT('Ctrl Pts',(-1.02479811336611,-1.11092237734564,
-5.05923718121733));
#28041=CARTESIAN_POINT('Ctrl Pts',(-0.871086046599528,-1.23469590658041,
-5.04892246362952));
#28042=CARTESIAN_POINT('Ctrl Pts',(-0.59349076679898,-1.38245306620357,
-5.03222967142159));
#28043=CARTESIAN_POINT('Ctrl Pts',(-0.479555196543473,-1.42667705756963,
-5.02581121874688));
#28044=CARTESIAN_POINT('Ctrl Pts',(-0.24284437946229,-1.48495860067024,
-5.01291338844306));
#28045=CARTESIAN_POINT('Ctrl Pts',(-0.121403302012765,-1.49919069967036,
-5.0064742156347));
#28046=CARTESIAN_POINT('Ctrl Pts',(-2.23097736033392E-5,-1.49898153286063,
-5.00002670181768));
#28047=CARTESIAN_POINT('Ctrl Pts',(0.644570879197,-1.369782843561,-4.956997056261));
#28048=CARTESIAN_POINT('Ctrl Pts',(0.3182373172226,-1.523343761587,-4.975955389595));
#28049=CARTESIAN_POINT('Ctrl Pts',(-0.4471872711094,-1.586323876419,-5.013872056261));
#28050=CARTESIAN_POINT('Ctrl Pts',(-1.377740014924,-0.904994387625,-5.070747056261));
#28051=CARTESIAN_POINT('Ctrl Pts',(-1.633632209849,0.2194343691702,-5.127622056261));
#28052=CARTESIAN_POINT('Ctrl Pts',(-1.090057677579,1.236420530413,-5.184497056261));
#28053=CARTESIAN_POINT('Ctrl Pts',(-0.01294453477278,1.648269146651,-5.241372056261));
#28054=CARTESIAN_POINT('Ctrl Pts',(1.070497507345,1.253391767652,-5.298247056261));
#28055=CARTESIAN_POINT('Ctrl Pts',(1.630000905225,0.2450597004638,-5.355122056261));
#28056=CARTESIAN_POINT('Ctrl Pts',(1.391722092318,-0.8832137221716,-5.411997056261));
#28057=CARTESIAN_POINT('Ctrl Pts',(0.4722839904274,-1.579210161907,-5.468872056261));
#28058=CARTESIAN_POINT('Ctrl Pts',(-0.6783071100709,-1.502283720031,-5.525747056261));
#28059=CARTESIAN_POINT('Ctrl Pts',(-1.496910028035,-0.6900849750494,-5.582622056261));
#28060=CARTESIAN_POINT('Ctrl Pts',(-1.582870729986,0.4598664577049,-5.639497056261));
#28061=CARTESIAN_POINT('Ctrl Pts',(-0.8941169184216,1.384742518528,-5.696372056261));
#28062=CARTESIAN_POINT('Ctrl Pts',(0.232250236729,1.631875220096,-5.753247056261));
#28063=CARTESIAN_POINT('Ctrl Pts',(1.24494567787,1.080308828809,-5.810122056261));
#28064=CARTESIAN_POINT('Ctrl Pts',(1.648319418813,0.,-5.866997056261));
#28065=CARTESIAN_POINT('Ctrl Pts',(1.24494567787,-1.080308828809,-5.923872056261));
#28066=CARTESIAN_POINT('Ctrl Pts',(0.232250236729,-1.631875220096,-5.980747056261));
#28067=CARTESIAN_POINT('Ctrl Pts',(-0.8941169184215,-1.384742518528,-6.037622056261));
#28068=CARTESIAN_POINT('Ctrl Pts',(-1.582870729986,-0.459866457705,-6.094497056261));
#28069=CARTESIAN_POINT('Ctrl Pts',(-1.496910028035,0.6900849750494,-6.151372056261));
#28070=CARTESIAN_POINT('Ctrl Pts',(-0.6783071100709,1.502283720031,-6.208247056261));
#28071=CARTESIAN_POINT('Ctrl Pts',(0.4722839904274,1.579210161907,-6.265122056261));
#28072=CARTESIAN_POINT('Ctrl Pts',(1.391722092318,0.8832137221716,-6.321997056261));
#28073=CARTESIAN_POINT('Ctrl Pts',(1.630000905225,-0.2450597004637,-6.378872056261));
#28074=CARTESIAN_POINT('Ctrl Pts',(1.070497507345,-1.253391767652,-6.435747056261));
#28075=CARTESIAN_POINT('Ctrl Pts',(-0.01294453477276,-1.648269146651,-6.492622056261));
#28076=CARTESIAN_POINT('Ctrl Pts',(-1.090057677579,-1.236420530413,-6.549497056261));
#28077=CARTESIAN_POINT('Ctrl Pts',(-1.633632209849,-0.2194343691702,-6.606372056261));
#28078=CARTESIAN_POINT('Ctrl Pts',(-1.377740014924,0.904994387625,-6.663247056261));
#28079=CARTESIAN_POINT('Ctrl Pts',(-0.4471872711094,1.586323876419,-6.720122056261));
#28080=CARTESIAN_POINT('Ctrl Pts',(0.3182373172226,1.523343761587,-6.758038722928));
#28081=CARTESIAN_POINT('Ctrl Pts',(0.644570879197,1.369782843561,-6.776997056261));
#28082=CARTESIAN_POINT('Ctrl Pts',(0.5862766256734,-1.24590124895,-5.036043180934));
#28083=CARTESIAN_POINT('Ctrl Pts',(0.2894562980212,-1.38557429308,-5.055001514267));
#28084=CARTESIAN_POINT('Ctrl Pts',(-0.4067441654775,-1.442858558319,-5.092918180934));
#28085=CARTESIAN_POINT('Ctrl Pts',(-1.253138782831,-0.823147729682,-5.149793180934));
#28086=CARTESIAN_POINT('Ctrl Pts',(-1.48588838015,0.1995889756518,-5.206668180934));
#28087=CARTESIAN_POINT('Ctrl Pts',(-0.9914741072328,1.12460007096,-5.263543180934));
#28088=CARTESIAN_POINT('Ctrl Pts',(-0.01177384584447,1.499201569118,-5.320418180934));
#28089=CARTESIAN_POINT('Ctrl Pts',(0.9736829364363,1.140036448902,-5.377293180934));
#28090=CARTESIAN_POINT('Ctrl Pts',(1.482585486565,0.2228967812747,-5.434168180934));
#28091=CARTESIAN_POINT('Ctrl Pts',(1.265856337127,-0.8033368827153,-5.491043180934));
#28092=CARTESIAN_POINT('Ctrl Pts',(0.4295711661878,-1.436388200015,-5.547918180934));
#28093=CARTESIAN_POINT('Ctrl Pts',(-0.61696179039,-1.36641889761,-5.604793180934));
#28094=CARTESIAN_POINT('Ctrl Pts',(-1.361531196175,-0.6276744787227,-5.661668180934));
#28095=CARTESIAN_POINT('Ctrl Pts',(-1.439717710501,0.4182766609306,-5.718543180934));
#28096=CARTESIAN_POINT('Ctrl Pts',(-0.8132540063595,1.259507988013,-5.775418180934));
#28097=CARTESIAN_POINT('Ctrl Pts',(0.211245790798,1.484290290542,-5.832293180934));
#28098=CARTESIAN_POINT('Ctrl Pts',(1.132354213826,0.9826069332027,-5.889168180934));
#28099=CARTESIAN_POINT('Ctrl Pts',(1.499247294724,0.,-5.946043180934));
#28100=CARTESIAN_POINT('Ctrl Pts',(1.132354213826,-0.9826069332027,-6.002918180934));
#28101=CARTESIAN_POINT('Ctrl Pts',(0.211245790798,-1.484290290542,-6.059793180934));
#28102=CARTESIAN_POINT('Ctrl Pts',(-0.8132540063595,-1.259507988013,-6.116668180934));
#28103=CARTESIAN_POINT('Ctrl Pts',(-1.439717710501,-0.4182766609306,-6.173543180934));
#28104=CARTESIAN_POINT('Ctrl Pts',(-1.361531196175,0.6276744787227,-6.230418180934));
#28105=CARTESIAN_POINT('Ctrl Pts',(-0.61696179039,1.36641889761,-6.287293180934));
#28106=CARTESIAN_POINT('Ctrl Pts',(0.4295711661878,1.436388200015,-6.344168180934));
#28107=CARTESIAN_POINT('Ctrl Pts',(1.265856337127,0.8033368827153,-6.401043180934));
#28108=CARTESIAN_POINT('Ctrl Pts',(1.482585486565,-0.2228967812747,-6.457918180934));
#28109=CARTESIAN_POINT('Ctrl Pts',(0.9736829364363,-1.140036448902,-6.514793180934));
#28110=CARTESIAN_POINT('Ctrl Pts',(-0.01177384584445,-1.499201569118,-6.571668180934));
#28111=CARTESIAN_POINT('Ctrl Pts',(-0.9914741072328,-1.12460007096,-6.628543180934));
#28112=CARTESIAN_POINT('Ctrl Pts',(-1.48588838015,-0.1995889756518,-6.685418180934));
#28113=CARTESIAN_POINT('Ctrl Pts',(-1.253138782831,0.823147729682,-6.742293180934));
#28114=CARTESIAN_POINT('Ctrl Pts',(-0.4067441654775,1.442858558319,-6.799168180934));
#28115=CARTESIAN_POINT('Ctrl Pts',(0.2894562980212,1.38557429308,-6.837084847601));
#28116=CARTESIAN_POINT('Ctrl Pts',(0.5862766256734,1.24590124895,-6.856043180934));
#28117=CARTESIAN_POINT('Ctrl Pts',(0.5279823721497,-1.122019654338,-5.115089305607));
#28118=CARTESIAN_POINT('Ctrl Pts',(0.2606752788197,-1.247804824574,-5.13404763894));
#28119=CARTESIAN_POINT('Ctrl Pts',(-0.3663010598456,-1.299393240218,-5.171964305607));
#28120=CARTESIAN_POINT('Ctrl Pts',(-1.128537550737,-0.7413010717389,-5.228839305607));
#28121=CARTESIAN_POINT('Ctrl Pts',(-1.33814455045,0.1797435821333,-5.285714305607));
#28122=CARTESIAN_POINT('Ctrl Pts',(-0.892890536887,1.012779611507,-5.342589305607));
#28123=CARTESIAN_POINT('Ctrl Pts',(-0.01060315691615,1.350133991585,-5.399464305607));
#28124=CARTESIAN_POINT('Ctrl Pts',(0.8768683655278,1.026681130153,-5.456339305607));
#28125=CARTESIAN_POINT('Ctrl Pts',(1.335170067905,0.2007338620856,-5.513214305607));
#28126=CARTESIAN_POINT('Ctrl Pts',(1.139990581936,-0.723460043259,-5.570089305607));
#28127=CARTESIAN_POINT('Ctrl Pts',(0.3868583419482,-1.293566238123,-5.626964305607));
#28128=CARTESIAN_POINT('Ctrl Pts',(-0.555616470709,-1.230554075189,-5.683839305607));
#28129=CARTESIAN_POINT('Ctrl Pts',(-1.226152364316,-0.5652639823961,-5.740714305607));
#28130=CARTESIAN_POINT('Ctrl Pts',(-1.296564691016,0.3766868641562,-5.797589305607));
#28131=CARTESIAN_POINT('Ctrl Pts',(-0.7323910942975,1.134273457497,-5.854464305607));
#28132=CARTESIAN_POINT('Ctrl Pts',(0.190241344867,1.336705360987,-5.911339305607));
#28133=CARTESIAN_POINT('Ctrl Pts',(1.019762749782,0.8849050375959,-5.968214305607));
#28134=CARTESIAN_POINT('Ctrl Pts',(1.350175170634,0.,-6.025089305607));
#28135=CARTESIAN_POINT('Ctrl Pts',(1.019762749782,-0.8849050375959,-6.081964305607));
#28136=CARTESIAN_POINT('Ctrl Pts',(0.190241344867,-1.336705360987,-6.138839305607));
#28137=CARTESIAN_POINT('Ctrl Pts',(-0.7323910942975,-1.134273457497,-6.195714305607));
#28138=CARTESIAN_POINT('Ctrl Pts',(-1.296564691016,-0.3766868641562,-6.252589305607));
#28139=CARTESIAN_POINT('Ctrl Pts',(-1.226152364316,0.5652639823961,-6.309464305607));
#28140=CARTESIAN_POINT('Ctrl Pts',(-0.555616470709,1.230554075189,-6.366339305607));
#28141=CARTESIAN_POINT('Ctrl Pts',(0.3868583419481,1.293566238123,-6.423214305607));
#28142=CARTESIAN_POINT('Ctrl Pts',(1.139990581936,0.723460043259,-6.480089305607));
#28143=CARTESIAN_POINT('Ctrl Pts',(1.335170067905,-0.2007338620856,-6.536964305607));
#28144=CARTESIAN_POINT('Ctrl Pts',(0.8768683655278,-1.026681130153,-6.593839305607));
#28145=CARTESIAN_POINT('Ctrl Pts',(-0.01060315691614,-1.350133991585,-6.650714305607));
#28146=CARTESIAN_POINT('Ctrl Pts',(-0.892890536887,-1.012779611507,-6.707589305607));
#28147=CARTESIAN_POINT('Ctrl Pts',(-1.33814455045,-0.1797435821333,-6.764464305607));
#28148=CARTESIAN_POINT('Ctrl Pts',(-1.128537550737,0.7413010717389,-6.821339305607));
#28149=CARTESIAN_POINT('Ctrl Pts',(-0.3663010598456,1.299393240218,-6.878214305607));
#28150=CARTESIAN_POINT('Ctrl Pts',(0.2606752788197,1.247804824574,-6.916130972273));
#28151=CARTESIAN_POINT('Ctrl Pts',(0.5279823721497,1.122019654338,-6.935089305607));
#28152=CARTESIAN_POINT('Ctrl Pts',(0.4696881186261,-0.9981380597272,-5.194135430279));
#28153=CARTESIAN_POINT('Ctrl Pts',(0.2318942596183,-1.110035356068,-5.213093763613));
#28154=CARTESIAN_POINT('Ctrl Pts',(-0.3258579542138,-1.155927922117,-5.251010430279));
#28155=CARTESIAN_POINT('Ctrl Pts',(-1.003936318643,-0.6594544137959,-5.307885430279));
#28156=CARTESIAN_POINT('Ctrl Pts',(-1.190400720751,0.1598981886148,-5.364760430279));
#28157=CARTESIAN_POINT('Ctrl Pts',(-0.7943069665412,0.9009591520544,-5.421635430279));
#28158=CARTESIAN_POINT('Ctrl Pts',(-0.009432467987835,1.201066414053,-5.478510430279));
#28159=CARTESIAN_POINT('Ctrl Pts',(0.7800537946193,0.9133258114035,-5.535385430279));
#28160=CARTESIAN_POINT('Ctrl Pts',(1.187754649245,0.1785709428966,-5.592260430279));
#28161=CARTESIAN_POINT('Ctrl Pts',(1.014124826746,-0.6435832038027,-5.649135430279));
#28162=CARTESIAN_POINT('Ctrl Pts',(0.3441455177085,-1.150744276231,-5.706010430279));
#28163=CARTESIAN_POINT('Ctrl Pts',(-0.4942711510281,-1.094689252768,-5.762885430279));
#28164=CARTESIAN_POINT('Ctrl Pts',(-1.090773532456,-0.5028534860695,-5.819760430279));
#28165=CARTESIAN_POINT('Ctrl Pts',(-1.153411671532,0.3350970673819,-5.876635430279));
#28166=CARTESIAN_POINT('Ctrl Pts',(-0.6515281822355,1.009038926982,-5.933510430279));
#28167=CARTESIAN_POINT('Ctrl Pts',(0.1692368989359,1.189120431432,-5.990385430279));
#28168=CARTESIAN_POINT('Ctrl Pts',(0.9071712857378,0.7872031419892,-6.047260430279));
#28169=CARTESIAN_POINT('Ctrl Pts',(1.201103046544,0.,-6.104135430279));
#28170=CARTESIAN_POINT('Ctrl Pts',(0.9071712857378,-0.7872031419892,-6.161010430279));
#28171=CARTESIAN_POINT('Ctrl Pts',(0.169236898936,-1.189120431432,-6.217885430279));
#28172=CARTESIAN_POINT('Ctrl Pts',(-0.6515281822355,-1.009038926982,-6.274760430279));
#28173=CARTESIAN_POINT('Ctrl Pts',(-1.153411671532,-0.3350970673819,-6.331635430279));
#28174=CARTESIAN_POINT('Ctrl Pts',(-1.090773532456,0.5028534860695,-6.388510430279));
#28175=CARTESIAN_POINT('Ctrl Pts',(-0.4942711510281,1.094689252768,-6.445385430279));
#28176=CARTESIAN_POINT('Ctrl Pts',(0.3441455177085,1.150744276231,-6.502260430279));
#28177=CARTESIAN_POINT('Ctrl Pts',(1.014124826746,0.6435832038027,-6.559135430279));
#28178=CARTESIAN_POINT('Ctrl Pts',(1.187754649245,-0.1785709428966,-6.616010430279));
#28179=CARTESIAN_POINT('Ctrl Pts',(0.7800537946193,-0.9133258114035,-6.672885430279));
#28180=CARTESIAN_POINT('Ctrl Pts',(-0.009432467987825,-1.201066414053,-6.729760430279));
#28181=CARTESIAN_POINT('Ctrl Pts',(-0.7943069665412,-0.9009591520544,-6.786635430279));
#28182=CARTESIAN_POINT('Ctrl Pts',(-1.190400720751,-0.1598981886148,-6.843510430279));
#28183=CARTESIAN_POINT('Ctrl Pts',(-1.003936318643,0.6594544137959,-6.900385430279));
#28184=CARTESIAN_POINT('Ctrl Pts',(-0.3258579542138,1.155927922117,-6.957260430279));
#28185=CARTESIAN_POINT('Ctrl Pts',(0.2318942596183,1.110035356068,-6.995177096946));
#28186=CARTESIAN_POINT('Ctrl Pts',(0.4696881186261,0.9981380597272,-7.014135430279));
#28187=CARTESIAN_POINT('',(-1.42662358638991,-0.463399121050005,-6.59977593084528));
#28188=CARTESIAN_POINT('Ctrl Pts',(2.15083409534766E-5,-1.49901358617426,
-5.49995482072371));
#28189=CARTESIAN_POINT('Ctrl Pts',(-0.0955496771557089,-1.49902499053276,
-5.50492949105024));
#28190=CARTESIAN_POINT('Ctrl Pts',(-0.191148351530597,-1.49007674570699,
-5.50991524849391));
#28191=CARTESIAN_POINT('Ctrl Pts',(-0.37345699690883,-1.45524191779854,
-5.51978321815194));
#28192=CARTESIAN_POINT('Ctrl Pts',(-0.459741647179676,-1.43048283664789,
-5.52466077371444));
#28193=CARTESIAN_POINT('Ctrl Pts',(-0.723943635231431,-1.32758178810656,
-5.54013816144375));
#28194=CARTESIAN_POINT('Ctrl Pts',(-0.868233405527567,-1.23047251955764,
-5.54904358625072));
#28195=CARTESIAN_POINT('Ctrl Pts',(-1.06773131622946,-1.05862209452624,
-5.5627333617516));
#28196=CARTESIAN_POINT('Ctrl Pts',(-1.148176903769,-0.971365181836879,-5.5688666447238));
#28197=CARTESIAN_POINT('Ctrl Pts',(-1.29946460135078,-0.762178852221788,
-5.58267595377255));
#28198=CARTESIAN_POINT('Ctrl Pts',(-1.3644246712698,-0.638332711836241,
-5.59036492013114));
#28199=CARTESIAN_POINT('Ctrl Pts',(-1.44467601633284,-0.412715739435528,
-5.60306386102242));
#28200=CARTESIAN_POINT('Ctrl Pts',(-1.46864458814352,-0.31592360121861,
-5.60822651143182));
#28201=CARTESIAN_POINT('Ctrl Pts',(-1.50036359445655,-0.0999871267283061,
-5.61958217023767));
#28202=CARTESIAN_POINT('Ctrl Pts',(-1.50392985568841,0.019865718040392,
-5.62578458245811));
#28203=CARTESIAN_POINT('Ctrl Pts',(-1.48048429463456,0.279292867532091,
-5.63973465539427));
#28204=CARTESIAN_POINT('Ctrl Pts',(-1.44774382388466,0.416424110223926,
-5.64748580997274));
#28205=CARTESIAN_POINT('Ctrl Pts',(-1.35926609047163,0.640103090039512,
-5.66023359719478));
#28206=CARTESIAN_POINT('Ctrl Pts',(-1.31363362411102,0.728719647986248,
-5.66539144215515));
#28207=CARTESIAN_POINT('Ctrl Pts',(-1.19597964848409,0.911315227476304,
-5.67669094342594));
#28208=CARTESIAN_POINT('Ctrl Pts',(-1.12053071691648,1.00319337865376,-5.68284249309459));
#28209=CARTESIAN_POINT('Ctrl Pts',(-0.935550208753491,1.18053859482883,
-5.69656896808466));
#28210=CARTESIAN_POINT('Ctrl Pts',(-0.82369018732526,1.26097102014602,-5.70414579650042));
#28211=CARTESIAN_POINT('Ctrl Pts',(-0.613558945192887,1.37147933133676,
-5.71673936389039));
#28212=CARTESIAN_POINT('Ctrl Pts',(-0.521120952615554,1.40895055110257,
-5.72190336975471));
#28213=CARTESIAN_POINT('Ctrl Pts',(-0.311906874910792,1.47097335864444,
-5.73325483817663));
#28214=CARTESIAN_POINT('Ctrl Pts',(-0.193841941583796,1.49150426139673,
-5.73945133073325));
#28215=CARTESIAN_POINT('Ctrl Pts',(0.0674181442853415,1.50520456787866,
-5.75345639078522));
#28216=CARTESIAN_POINT('Ctrl Pts',(0.208979515017795,1.49199060124383,-5.76127229255357));
#28217=CARTESIAN_POINT('Ctrl Pts',(0.443959568703562,1.43534782074056,-5.77407909312804));
#28218=CARTESIAN_POINT('Ctrl Pts',(0.538065159488263,1.40254967053854,-5.77923557246599));
#28219=CARTESIAN_POINT('Ctrl Pts',(0.735133568662664,1.31164462684568,-5.79052555352543));
#28220=CARTESIAN_POINT('Ctrl Pts',(0.836510259935816,1.24988394922922,-5.79666918237583));
#28221=CARTESIAN_POINT('Ctrl Pts',(1.03665883498361,1.0926262425576,-5.81030625510528));
#28222=CARTESIAN_POINT('Ctrl Pts',(1.13105693148402,0.994391982106476,-5.81779953159453));
#28223=CARTESIAN_POINT('Ctrl Pts',(1.26961154927999,0.80344812582879,-5.83031868033029));
#28224=CARTESIAN_POINT('Ctrl Pts',(1.31993116959101,0.717293046852347,-5.83548534136846));
#28225=CARTESIAN_POINT('Ctrl Pts',(1.41141289896438,0.51869512759628,-5.84685969634429));
#28226=CARTESIAN_POINT('Ctrl Pts',(1.448698157511,0.404363257879274,-5.85307598458818));
#28227=CARTESIAN_POINT('Ctrl Pts',(1.4998727100313,0.14538332640125,-5.86720379570343));
#28228=CARTESIAN_POINT('Ctrl Pts',(1.50673344696795,0.00142570670132477,
-5.87512531518636));
#28229=CARTESIAN_POINT('Ctrl Pts',(1.48296882824891,-0.241018735058465,
-5.88802654082655));
#28230=CARTESIAN_POINT('Ctrl Pts',(1.46352511372268,-0.338723080023819,
-5.89317987937783));
#28231=CARTESIAN_POINT('Ctrl Pts',(1.40093612574789,-0.546005230890234,
-5.90444414931358));
#28232=CARTESIAN_POINT('Ctrl Pts',(1.35404796790159,-0.654545916048239,
-5.91056561952626));
#28233=CARTESIAN_POINT('Ctrl Pts',(1.2280422871028,-0.871512931630714,-5.92401256541593));
#28234=CARTESIAN_POINT('Ctrl Pts',(1.14620866841746,-0.976467632406652,
-5.93133452999354));
#28235=CARTESIAN_POINT('Ctrl Pts',(0.979670477537851,-1.13919195358528,
-5.94370162815859));
#28236=CARTESIAN_POINT('Ctrl Pts',(0.90169883049161,-1.20154422240757,-5.94887414087997));
#28237=CARTESIAN_POINT('Ctrl Pts',(0.717694897505955,-1.32144958529579,
-5.96029902439949));
#28238=CARTESIAN_POINT('Ctrl Pts',(0.609119018060983,-1.37527468100387,
-5.966558966059));
#28239=CARTESIAN_POINT('Ctrl Pts',(0.355763322450707,-1.46468560692821,
-5.98092856922058));
#28240=CARTESIAN_POINT('Ctrl Pts',(0.210494732858562,-1.49231468129516,
-5.98905380960265));
#28241=CARTESIAN_POINT('Ctrl Pts',(-0.105114080074204,-1.50463465535023,
-6.00576685814989));
#28242=CARTESIAN_POINT('Ctrl Pts',(-0.27386121530662,-1.4831376416099,-6.01437260132996));
#28243=CARTESIAN_POINT('Ctrl Pts',(-0.598411030756974,-1.38575619535043,
-6.03221195337692));
#28244=CARTESIAN_POINT('Ctrl Pts',(-0.75158847914599,-1.30940033084702,
-6.04158964491971));
#28245=CARTESIAN_POINT('Ctrl Pts',(-0.989426246393969,-1.13320912568185,
-6.05736809915289));
#28246=CARTESIAN_POINT('Ctrl Pts',(-1.0800336556722,-1.04674081478275,-6.06381697470126));
#28247=CARTESIAN_POINT('Ctrl Pts',(-1.22229494730029,-0.873529281935807,
-6.07548158717378));
#28248=CARTESIAN_POINT('Ctrl Pts',(-1.27815266708797,-0.7901040870188,-6.08069815236894));
#28249=CARTESIAN_POINT('Ctrl Pts',(-1.38205526713629,-0.595121412220474,
-6.09249216870023));
#28250=CARTESIAN_POINT('Ctrl Pts',(-1.42533016680916,-0.482483454348762,
-6.09913901550064));
#28251=CARTESIAN_POINT('Ctrl Pts',(-1.48197162704049,-0.25462069220679,
-6.11172344484877));
#28252=CARTESIAN_POINT('Ctrl Pts',(-1.49669181174848,-0.141011276460424,
-6.11766251443455));
#28253=CARTESIAN_POINT('Ctrl Pts',(-1.50048257115899,0.0720827841409691,
-6.12875128354957));
#28254=CARTESIAN_POINT('Ctrl Pts',(-1.4925817600996,0.171597804332129,-6.13391172094632));
#28255=CARTESIAN_POINT('Ctrl Pts',(-1.44893779306281,0.414168561930941,
-6.1469478465354));
#28256=CARTESIAN_POINT('Ctrl Pts',(-1.40194658119633,0.553278086222032,
-6.15501197056988));
#28257=CARTESIAN_POINT('Ctrl Pts',(-1.28142731642128,0.786990633207509,
-6.16908997590994));
#28258=CARTESIAN_POINT('Ctrl Pts',(-1.21639079223807,0.883582018957452,
-6.17511867343625));
#28259=CARTESIAN_POINT('Ctrl Pts',(-1.07692358901623,1.04735283327409,-6.18630911703358));
#28260=CARTESIAN_POINT('Ctrl Pts',(-1.00503668752227,1.11681439646067,-6.19148064302672));
#28261=CARTESIAN_POINT('Ctrl Pts',(-0.81638657738249,1.26600851048286,-6.20422266779974));
#28262=CARTESIAN_POINT('Ctrl Pts',(-0.694798758074129,1.33679445990154,
-6.21195493099225));
#28263=CARTESIAN_POINT('Ctrl Pts',(-0.457751478199051,1.43235899883709,
-6.22564808603858));
#28264=CARTESIAN_POINT('Ctrl Pts',(-0.346640730516119,1.46285087542127,
-6.23161846437896));
#28265=CARTESIAN_POINT('Ctrl Pts',(-0.135420020266238,1.49610457258724,
-6.24274277170832));
#28266=CARTESIAN_POINT('Ctrl Pts',(-0.0357172671648247,1.50200364475123,
-6.24790714213475));
#28267=CARTESIAN_POINT('Ctrl Pts',(0.208376743658017,1.49228253689555,-6.2608353648219));
#28268=CARTESIAN_POINT('Ctrl Pts',(0.350481982480695,1.46562737257418,-6.26877796635645));
#28269=CARTESIAN_POINT('Ctrl Pts',(0.596361493247398,1.38046114911593,-6.28271295732946));
#28270=CARTESIAN_POINT('Ctrl Pts',(0.700793946292286,1.3300816912034,-6.28871804158767));
#28271=CARTESIAN_POINT('Ctrl Pts',(0.882395417781042,1.21576000229937,-6.29988171632431));
#28272=CARTESIAN_POINT('Ctrl Pts',(0.961403242228944,1.15457509213465,-6.30505037166592));
#28273=CARTESIAN_POINT('Ctrl Pts',(1.13715212872892,0.988212767642547,-6.31786557844639));
#28274=CARTESIAN_POINT('Ctrl Pts',(1.22540971732273,0.876686690679965,-6.32568061063726));
#28275=CARTESIAN_POINT('Ctrl Pts',(1.35416353490123,0.653817911199552,-6.33946808234627));
#28276=CARTESIAN_POINT('Ctrl Pts',(1.40001199010802,0.547822025382658,-6.3454511973331));
#28277=CARTESIAN_POINT('Ctrl Pts',(1.46253021302436,0.343048931027685,-6.35658995320548));
#28278=CARTESIAN_POINT('Ctrl Pts',(1.48230247613543,0.245128783009541,-6.36175590353927));
#28279=CARTESIAN_POINT('Ctrl Pts',(1.50667741775337,0.00291603616627232,
-6.3746420306679));
#28280=CARTESIAN_POINT('Ctrl Pts',(1.50028685601091,-0.140646645627876,
-6.38253714167809));
#28281=CARTESIAN_POINT('Ctrl Pts',(1.45093683814447,-0.395056510149083,
-6.39641682863631));
#28282=CARTESIAN_POINT('Ctrl Pts',(1.41589906170439,-0.505396081003056,
-6.40241333582343));
#28283=CARTESIAN_POINT('Ctrl Pts',(1.32853968721372,-0.701191607913635,
-6.41356729502109));
#28284=CARTESIAN_POINT('Ctrl Pts',(1.27917419609213,-0.788061567899416,
-6.41873490810641));
#28285=CARTESIAN_POINT('Ctrl Pts',(1.13908763570199,-0.986058514220784,
-6.43157687978795));
#28286=CARTESIAN_POINT('Ctrl Pts',(1.04075623263226,-1.08958631430917,-6.43942218074782));
#28287=CARTESIAN_POINT('Ctrl Pts',(0.837687259251639,-1.24881371019553,
-6.45324445231495));
#28288=CARTESIAN_POINT('Ctrl Pts',(0.739098733652217,-1.30915826685564,
-6.45923252175412));
#28289=CARTESIAN_POINT('Ctrl Pts',(0.545037632306977,-1.39986256838697,
-6.47037686555309));
#28290=CARTESIAN_POINT('Ctrl Pts',(0.450858267314446,-1.43319321067716,
-6.47554339967615));
#28291=CARTESIAN_POINT('Ctrl Pts',(0.214766811622813,-1.49126585950107,
-6.48841436095777));
#28292=CARTESIAN_POINT('Ctrl Pts',(0.0720492191049348,-1.50511059683625,
-6.49629230690851));
#28293=CARTESIAN_POINT('Ctrl Pts',(-0.186413734920357,-1.49215578677182,
-6.51015284666944));
#28294=CARTESIAN_POINT('Ctrl Pts',(-0.300546677067099,-1.47304380550322,
-6.51614712292677));
#28295=CARTESIAN_POINT('Ctrl Pts',(-0.506664425994047,-1.41420525200107,
-6.52729858106496));
#28296=CARTESIAN_POINT('Ctrl Pts',(-0.599629187953682,-1.37759537526464,
-6.53246594964597));
#28297=CARTESIAN_POINT('Ctrl Pts',(-0.815577659267427,-1.26677413083928,
-6.545317024093));
#28298=CARTESIAN_POINT('Ctrl Pts',(-0.932084746077253,-1.18391075257807,
-6.55317245956912));
#28299=CARTESIAN_POINT('Ctrl Pts',(-1.11841809740179,-1.00517888458096,
-6.56700187774727));
#28300=CARTESIAN_POINT('Ctrl Pts',(-1.19201686999432,-0.916103763121076,
-6.57298747263071));
#28301=CARTESIAN_POINT('Ctrl Pts',(-1.32712308915121,-0.709238017225592,
-6.58584110390239));
#28302=CARTESIAN_POINT('Ctrl Pts',(-1.38514527488612,-0.589022817269641,
-6.59271872607206));
#28303=CARTESIAN_POINT('Ctrl Pts',(-1.42628888349589,-0.463297395395638,
-6.59981789523313));
#28304=CARTESIAN_POINT('',(-1.43217561911112,-0.444902799674129,-6.6008559233962));
#28305=CARTESIAN_POINT('Ctrl Pts',(-1.43217561911112,-0.444902799674129,
-6.6008559233962));
#28306=CARTESIAN_POINT('Ctrl Pts',(-1.43039287381244,-0.451087558329368,
-6.60049242607935));
#28307=CARTESIAN_POINT('Ctrl Pts',(-1.42857006684158,-0.457261655368297,
-6.60012892876249));
#28308=CARTESIAN_POINT('Ctrl Pts',(-1.42670732833463,-0.463424572590093,
-6.59976543144564));
#28309=CARTESIAN_POINT('',(-2.07485480732137E-16,1.43111039753271,-6.78927262721387));
#28310=CARTESIAN_POINT('Ctrl Pts',(3.85108611666851E-15,1.43111039753277,
-6.78927262721387));
#28311=CARTESIAN_POINT('Ctrl Pts',(-0.147800856913735,1.43482343493628,
-6.77907114079013));
#28312=CARTESIAN_POINT('Ctrl Pts',(-0.29534771011176,1.41540626957901,-6.76933892746074));
#28313=CARTESIAN_POINT('Ctrl Pts',(-0.554938120622151,1.34022312493367,
-6.75011994068015));
#28314=CARTESIAN_POINT('Ctrl Pts',(-0.668031110176501,1.29126078102496,
-6.74113820669912));
#28315=CARTESIAN_POINT('Ctrl Pts',(-0.935437445880612,1.13229063520146,
-6.71919854254426));
#28316=CARTESIAN_POINT('Ctrl Pts',(-1.07640515392378,1.00564224957176,-6.70712143470464));
#28317=CARTESIAN_POINT('Ctrl Pts',(-1.28983172346691,0.723669754549612,
-6.68324434603939));
#28318=CARTESIAN_POINT('Ctrl Pts',(-1.36728052837544,0.575354244019802,
-6.67118963644036));
#28319=CARTESIAN_POINT('Ctrl Pts',(-1.46623442521789,0.2678743516873,-6.64885199889988));
#28320=CARTESIAN_POINT('Ctrl Pts',(-1.4899792233694,0.11197065002529,-6.63870486526541));
#28321=CARTESIAN_POINT('Ctrl Pts',(-1.48811140632177,-0.180046254082272,
-6.6195763750769));
#28322=CARTESIAN_POINT('Ctrl Pts',(-1.46902193449905,-0.314743580828287,
-6.61026854950158));
#28323=CARTESIAN_POINT('Ctrl Pts',(-1.43217561911112,-0.444902799674129,
-6.6008559233962));
#28324=CARTESIAN_POINT('',(-7.91239893927046E-11,1.11628565063362,-6.97115102811022));
#28325=CARTESIAN_POINT('Ctrl Pts',(-1.75670886845076E-15,1.43111039753272,
-6.78927262721389));
#28326=CARTESIAN_POINT('Ctrl Pts',(7.53530335141514E-16,1.37865404388881,
-6.81957735335642));
#28327=CARTESIAN_POINT('Ctrl Pts',(4.44448508960574E-12,1.32619769024498,
-6.84988207949911));
#28328=CARTESIAN_POINT('Ctrl Pts',(4.44448508960574E-12,1.22125610800045,
-6.91050821322671));
#28329=CARTESIAN_POINT('Ctrl Pts',(6.22406898798232E-15,1.16877087939972,
-6.94082962081159));
#28330=CARTESIAN_POINT('Ctrl Pts',(1.83311314657105E-15,1.11628565079912,
-6.97115102839669));
#28331=CARTESIAN_POINT('Ctrl Pts',(-2.02707198973761E-6,-1.11628565404413,
-5.22111408882413));
#28332=CARTESIAN_POINT('Ctrl Pts',(-0.0945477069597211,-1.11645974724111,
-5.22785015639956));
#28333=CARTESIAN_POINT('Ctrl Pts',(-0.189124507262874,-1.1048491526056,
-5.23459224618512));
#28334=CARTESIAN_POINT('Ctrl Pts',(-0.372801878430438,-1.05728988862616,
-5.24813470031973));
#28335=CARTESIAN_POINT('Ctrl Pts',(-0.461203748610969,-1.02120417552907,
-5.25489047871015));
#28336=CARTESIAN_POINT('Ctrl Pts',(-0.668471432388862,-0.904915646636,-5.27182073957926));
#28337=CARTESIAN_POINT('Ctrl Pts',(-0.780383055419269,-0.811029500761424,
-5.28202995426489));
#28338=CARTESIAN_POINT('Ctrl Pts',(-0.977352549963132,-0.567498199932429,
-5.30436776308206));
#28339=CARTESIAN_POINT('Ctrl Pts',(-1.03703915589556,-0.431145768277794,
-5.3147587800084));
#28340=CARTESIAN_POINT('Ctrl Pts',(-1.11066616674449,-0.178042375581379,
-5.33352929238688));
#28341=CARTESIAN_POINT('Ctrl Pts',(-1.1250370353998,-0.0352369170927895,
-5.34357133882955));
#28342=CARTESIAN_POINT('Ctrl Pts',(-1.09418460733438,0.296790717289725,
-5.36736190012804));
#28343=CARTESIAN_POINT('Ctrl Pts',(-1.02997735713436,0.440477084842023,
-5.37828381624767));
#28344=CARTESIAN_POINT('Ctrl Pts',(-0.925588908242793,0.636392952388546,
-5.39408990478641));
#28345=CARTESIAN_POINT('Ctrl Pts',(-0.840538191683126,0.751460714065282,
-5.404101988361));
#28346=CARTESIAN_POINT('Ctrl Pts',(-0.611182247799713,0.946513834085752,
-5.42558474266587));
#28347=CARTESIAN_POINT('Ctrl Pts',(-0.478234529751092,1.01917110999221,
-5.43616577485578));
#28348=CARTESIAN_POINT('Ctrl Pts',(-0.222597234321215,1.1004636264182,-5.455267721173));
#28349=CARTESIAN_POINT('Ctrl Pts',(-0.0794663775051641,1.12675755955542,
-5.46543571983759));
#28350=CARTESIAN_POINT('Ctrl Pts',(0.232981315456794,1.10176800386664,-5.48779253835339));
#28351=CARTESIAN_POINT('Ctrl Pts',(0.377700605109044,1.06037143957914,-5.49830194335543));
#28352=CARTESIAN_POINT('Ctrl Pts',(0.604852724324554,0.944731736167605,
-5.51645937858707));
#28353=CARTESIAN_POINT('Ctrl Pts',(0.731331226988477,0.86397400629993,-5.52692136770941));
#28354=CARTESIAN_POINT('Ctrl Pts',(0.94339790793788,0.613934547621962,-5.55029160325254));
#28355=CARTESIAN_POINT('Ctrl Pts',(1.01607631574408,0.484189787750145,-5.56067712497169));
#28356=CARTESIAN_POINT('Ctrl Pts',(1.11857306467123,0.173002860562905,-5.58402934320733));
#28357=CARTESIAN_POINT('Ctrl Pts',(1.12165266273671,0.0230529286473064,
-5.59448736045732));
#28358=CARTESIAN_POINT('Ctrl Pts',(1.10179845703877,-0.228016486144784,
-5.61242927917354));
#28359=CARTESIAN_POINT('Ctrl Pts',(1.06324590215936,-0.369253565391408,
-5.62266080687385));
#28360=CARTESIAN_POINT('Ctrl Pts',(0.92446485564618,-0.649976757040055,
-5.64499359014349));
#28361=CARTESIAN_POINT('Ctrl Pts',(0.825915661788595,-0.761161572818599,
-5.65536755467241));
#28362=CARTESIAN_POINT('Ctrl Pts',(0.626214316349833,-0.934430304671217,
-5.67419538133658));
#28363=CARTESIAN_POINT('Ctrl Pts',(0.502214996937518,-1.00732385711171,
-5.68425796124846));
#28364=CARTESIAN_POINT('Ctrl Pts',(0.191201997533698,-1.11682300306853,
-5.70778190972181));
#28365=CARTESIAN_POINT('Ctrl Pts',(0.0349012702549407,-1.12007370080308,
-5.71864513166231));
#28366=CARTESIAN_POINT('Ctrl Pts',(-0.203851405860774,-1.10611718857029,
-5.73567366866181));
#28367=CARTESIAN_POINT('Ctrl Pts',(-0.341786112597065,-1.07261170247851,
-5.745614088678));
#28368=CARTESIAN_POINT('Ctrl Pts',(-0.603413551668558,-0.951563052462823,
-5.76618313304261));
#28369=CARTESIAN_POINT('Ctrl Pts',(-0.725113385898973,-0.861211673415803,
-5.77676949290965));
#28370=CARTESIAN_POINT('Ctrl Pts',(-0.90527342351451,-0.663857977873294,
-5.79579742516296));
#28371=CARTESIAN_POINT('Ctrl Pts',(-0.989304020610922,-0.54516302107656,
-5.80595751403342));
#28372=CARTESIAN_POINT('Ctrl Pts',(-1.09791444748828,-0.250846118613139,
-5.82833525890648));
#28373=CARTESIAN_POINT('Ctrl Pts',(-1.12102369397598,-0.101931202388053,
-5.83885689635648));
#28374=CARTESIAN_POINT('Ctrl Pts',(-1.11127472608703,0.152382998726055,
-5.85698527230642));
#28375=CARTESIAN_POINT('Ctrl Pts',(-1.09120934524511,0.300938815206572,
-5.86743533545795));
#28376=CARTESIAN_POINT('Ctrl Pts',(-0.953355092950161,0.598483057720691,
-5.89081240762303));
#28377=CARTESIAN_POINT('Ctrl Pts',(-0.865889506205097,0.719096632405912,
-5.90121651825254));
#28378=CARTESIAN_POINT('Ctrl Pts',(-0.630908211369292,0.938430669099306,
-5.92412556939149));
#28379=CARTESIAN_POINT('Ctrl Pts',(-0.499473987912771,1.00559671816688,
-5.93443093822624));
#28380=CARTESIAN_POINT('Ctrl Pts',(-0.254954649474623,1.09592824110065,
-5.95300231361182));
#28381=CARTESIAN_POINT('Ctrl Pts',(-0.11023350814751,1.12012616746575,-5.96325541986776));
#28382=CARTESIAN_POINT('Ctrl Pts',(0.202625788977316,1.11169037854405,-5.98557375090056));
#28383=CARTESIAN_POINT('Ctrl Pts',(0.344594062565046,1.06910154094397,-5.99592507043896));
#28384=CARTESIAN_POINT('Ctrl Pts',(0.58636306509556,0.959974916638408,-6.01481521721138));
#28385=CARTESIAN_POINT('Ctrl Pts',(0.704733656287621,0.87764403748791,-6.02490073023946));
#28386=CARTESIAN_POINT('Ctrl Pts',(0.924445762809005,0.651144082671899,
-6.04741286795021));
#28387=CARTESIAN_POINT('Ctrl Pts',(0.995878303027181,0.517818669122234,
-6.05795712525469));
#28388=CARTESIAN_POINT('Ctrl Pts',(1.08982166380632,0.277939862987329,-6.07630001885425));
#28389=CARTESIAN_POINT('Ctrl Pts',(1.1169872981078,0.139044412854732,-6.08621126978534));
#28390=CARTESIAN_POINT('Ctrl Pts',(1.1169872981078,-0.139044412854731,-6.10605370329665));
#28391=CARTESIAN_POINT('Ctrl Pts',(1.08982166380632,-0.277939862987325,
-6.11596495422619));
#28392=CARTESIAN_POINT('Ctrl Pts',(0.995878303027172,-0.517818669122232,
-6.13430784782587));
#28393=CARTESIAN_POINT('Ctrl Pts',(0.92444576280899,-0.651144082671897,
-6.14485210513048));
#28394=CARTESIAN_POINT('Ctrl Pts',(0.704733656287586,-0.877644037487917,
-6.16736424284125));
#28395=CARTESIAN_POINT('Ctrl Pts',(0.586363065095511,-0.959974916638421,
-6.17744975586925));
#28396=CARTESIAN_POINT('Ctrl Pts',(0.344594062564979,-1.06910154094398,
-6.19633990264163));
#28397=CARTESIAN_POINT('Ctrl Pts',(0.202625788977251,-1.11169037854405,
-6.20669122217995));
#28398=CARTESIAN_POINT('Ctrl Pts',(-0.110233508147567,-1.12012616746575,
-6.22900955321285));
#28399=CARTESIAN_POINT('Ctrl Pts',(-0.254954649474677,-1.09592824110064,
-6.23926265946891));
#28400=CARTESIAN_POINT('Ctrl Pts',(-0.499473987912839,-1.00559671816685,
-6.25783403485462));
#28401=CARTESIAN_POINT('Ctrl Pts',(-0.630908211369357,-0.93843066909926,
-6.26813940368944));
#28402=CARTESIAN_POINT('Ctrl Pts',(-0.865889506205144,-0.719096632405857,
-6.29104845482854));
#28403=CARTESIAN_POINT('Ctrl Pts',(-0.953355092950203,-0.598483057720625,
-6.30145256545815));
#28404=CARTESIAN_POINT('Ctrl Pts',(-1.09120934524514,-0.300938815206476,
-6.32482963762336));
#28405=CARTESIAN_POINT('Ctrl Pts',(-1.11127472608704,-0.152382998725948,
-6.33527970077493));
#28406=CARTESIAN_POINT('Ctrl Pts',(-1.12102369397598,0.101931202388141,
-6.35340807672478));
#28407=CARTESIAN_POINT('Ctrl Pts',(-1.09791444748826,0.250846118613222,
-6.36392971417461));
#28408=CARTESIAN_POINT('Ctrl Pts',(-0.989304020610884,0.545163021076626,
-6.38630745904754));
#28409=CARTESIAN_POINT('Ctrl Pts',(-0.905273423514468,0.66385797787335,
-6.39646754791798));
#28410=CARTESIAN_POINT('Ctrl Pts',(-0.725113385898928,0.861211673415845,
-6.41549548017135));
#28411=CARTESIAN_POINT('Ctrl Pts',(-0.603413551668504,0.951563052462865,
-6.42608184003854));
#28412=CARTESIAN_POINT('Ctrl Pts',(-0.341786112597014,1.07261170247853,
-6.44665088440311));
#28413=CARTESIAN_POINT('Ctrl Pts',(-0.203851405860737,1.1061171885703,-6.45659130441916));
#28414=CARTESIAN_POINT('Ctrl Pts',(0.0349012702549632,1.12007370080307,
-6.47361984141847));
#28415=CARTESIAN_POINT('Ctrl Pts',(0.1912019975337,1.11682300306851,-6.48448306335868));
#28416=CARTESIAN_POINT('Ctrl Pts',(0.502214996937536,1.00732385711167,-6.50800701183203));
#28417=CARTESIAN_POINT('Ctrl Pts',(0.626214316349873,0.934430304671156,
-6.51806959174408));
#28418=CARTESIAN_POINT('Ctrl Pts',(0.825915661788643,0.761161572818513,
-6.53689741840845));
#28419=CARTESIAN_POINT('Ctrl Pts',(0.92446485564623,0.64997675703996,-6.54727138293759));
#28420=CARTESIAN_POINT('Ctrl Pts',(1.06324590215939,0.369253565391305,-6.56960416620732));
#28421=CARTESIAN_POINT('Ctrl Pts',(1.10179845703878,0.228016486144688,-6.57983569390757));
#28422=CARTESIAN_POINT('Ctrl Pts',(1.12165266273671,-0.0230529286474655,
-6.59777761262373));
#28423=CARTESIAN_POINT('Ctrl Pts',(1.1185730646712,-0.173002860563037,-6.60823562987364));
#28424=CARTESIAN_POINT('Ctrl Pts',(1.01607631574405,-0.484189787750213,
-6.63158784810919));
#28425=CARTESIAN_POINT('Ctrl Pts',(0.943397907937839,-0.613934547622025,
-6.6419733698283));
#28426=CARTESIAN_POINT('Ctrl Pts',(0.731331226988405,-0.863974006299998,
-6.66534360537137));
#28427=CARTESIAN_POINT('Ctrl Pts',(0.604852724324464,-0.944731736167658,
-6.6758055944937));
#28428=CARTESIAN_POINT('Ctrl Pts',(0.377700605108989,-1.06037143957916,
-6.6939630297253));
#28429=CARTESIAN_POINT('Ctrl Pts',(0.232981315456739,-1.10176800386665,
-6.70447243472734));
#28430=CARTESIAN_POINT('Ctrl Pts',(-0.0794663775052152,-1.12675755955542,
-6.72682925324312));
#28431=CARTESIAN_POINT('Ctrl Pts',(-0.222597234321263,-1.10046362641819,
-6.73699725190771));
#28432=CARTESIAN_POINT('Ctrl Pts',(-0.478234529751139,-1.01917110999219,
-6.75609919822494));
#28433=CARTESIAN_POINT('Ctrl Pts',(-0.61118224779976,-0.94651383408572,
-6.76668023041484));
#28434=CARTESIAN_POINT('Ctrl Pts',(-0.840538191683147,-0.751460714065253,
-6.78816298471981));
#28435=CARTESIAN_POINT('Ctrl Pts',(-0.925588908242814,-0.636392952388519,
-6.79817506829455));
#28436=CARTESIAN_POINT('Ctrl Pts',(-1.02997735713431,-0.440477084842092,
-6.81398115683343));
#28437=CARTESIAN_POINT('Ctrl Pts',(-1.09418460733438,-0.296790717289793,
-6.82490307295328));
#28438=CARTESIAN_POINT('Ctrl Pts',(-1.1250370353998,0.0352369170928123,
-6.84869363425172));
#28439=CARTESIAN_POINT('Ctrl Pts',(-1.11066616674449,0.178042375581379,
-6.85873568069418));
#28440=CARTESIAN_POINT('Ctrl Pts',(-1.03703915589553,0.43114576827779,-6.87750619307247));
#28441=CARTESIAN_POINT('Ctrl Pts',(-0.977352549963096,0.567498199932421,
-6.88789720999858));
#28442=CARTESIAN_POINT('Ctrl Pts',(-0.780383055419192,0.811029500761444,
-6.91023501881583));
#28443=CARTESIAN_POINT('Ctrl Pts',(-0.668471432388746,0.904915646636041,
-6.92044423350163));
#28444=CARTESIAN_POINT('Ctrl Pts',(-0.461204333421732,1.02120384741813,
-6.93737444660179));
#28445=CARTESIAN_POINT('Ctrl Pts',(-0.372803144127186,1.05728937042922,
-6.94413017602258));
#28446=CARTESIAN_POINT('Ctrl Pts',(-0.189125242780074,1.10484915132565,
-6.95767267606297));
#28447=CARTESIAN_POINT('Ctrl Pts',(-0.0945470498259662,1.11645991446616,
-6.96441486355753));
#28448=CARTESIAN_POINT('Ctrl Pts',(-1.19666163152477E-10,1.11628565030996,
-6.97115102867089));
#28449=CARTESIAN_POINT('Ctrl Pts',(0.4696881186261,-0.9981380597272,-5.235864569721));
#28450=CARTESIAN_POINT('Ctrl Pts',(0.2318942596183,-1.110035356068,-5.254822903054));
#28451=CARTESIAN_POINT('Ctrl Pts',(-0.3258579542137,-1.155927922117,-5.292739569721));
#28452=CARTESIAN_POINT('Ctrl Pts',(-1.003936318643,-0.6594544137959,-5.349614569721));
#28453=CARTESIAN_POINT('Ctrl Pts',(-1.190400720751,0.1598981886148,-5.406489569721));
#28454=CARTESIAN_POINT('Ctrl Pts',(-0.7943069665412,0.9009591520544,-5.463364569721));
#28455=CARTESIAN_POINT('Ctrl Pts',(-0.009432467987834,1.201066414053,-5.520239569721));
#28456=CARTESIAN_POINT('Ctrl Pts',(0.7800537946193,0.9133258114035,-5.577114569721));
#28457=CARTESIAN_POINT('Ctrl Pts',(1.187754649245,0.1785709428966,-5.633989569721));
#28458=CARTESIAN_POINT('Ctrl Pts',(1.014124826746,-0.6435832038027,-5.690864569721));
#28459=CARTESIAN_POINT('Ctrl Pts',(0.3441455177085,-1.150744276231,-5.747739569721));
#28460=CARTESIAN_POINT('Ctrl Pts',(-0.4942711510281,-1.094689252768,-5.804614569721));
#28461=CARTESIAN_POINT('Ctrl Pts',(-1.090773532456,-0.5028534860695,-5.861489569721));
#28462=CARTESIAN_POINT('Ctrl Pts',(-1.153411671532,0.3350970673819,-5.918364569721));
#28463=CARTESIAN_POINT('Ctrl Pts',(-0.6515281822355,1.009038926982,-5.975239569721));
#28464=CARTESIAN_POINT('Ctrl Pts',(0.1692368989359,1.189120431432,-6.032114569721));
#28465=CARTESIAN_POINT('Ctrl Pts',(0.9071712857378,0.7872031419892,-6.088989569721));
#28466=CARTESIAN_POINT('Ctrl Pts',(1.201103046544,0.,-6.145864569721));
#28467=CARTESIAN_POINT('Ctrl Pts',(0.9071712857378,-0.7872031419892,-6.202739569721));
#28468=CARTESIAN_POINT('Ctrl Pts',(0.169236898936,-1.189120431432,-6.259614569721));
#28469=CARTESIAN_POINT('Ctrl Pts',(-0.6515281822355,-1.009038926982,-6.316489569721));
#28470=CARTESIAN_POINT('Ctrl Pts',(-1.153411671532,-0.3350970673819,-6.373364569721));
#28471=CARTESIAN_POINT('Ctrl Pts',(-1.090773532456,0.5028534860695,-6.430239569721));
#28472=CARTESIAN_POINT('Ctrl Pts',(-0.4942711510281,1.094689252768,-6.487114569721));
#28473=CARTESIAN_POINT('Ctrl Pts',(0.3441455177085,1.150744276231,-6.543989569721));
#28474=CARTESIAN_POINT('Ctrl Pts',(1.014124826746,0.6435832038027,-6.600864569721));
#28475=CARTESIAN_POINT('Ctrl Pts',(1.187754649245,-0.1785709428966,-6.657739569721));
#28476=CARTESIAN_POINT('Ctrl Pts',(0.7800537946193,-0.9133258114035,-6.714614569721));
#28477=CARTESIAN_POINT('Ctrl Pts',(-0.009432467987825,-1.201066414053,-6.771489569721));
#28478=CARTESIAN_POINT('Ctrl Pts',(-0.7943069665412,-0.9009591520544,-6.828364569721));
#28479=CARTESIAN_POINT('Ctrl Pts',(-1.190400720751,-0.1598981886148,-6.885239569721));
#28480=CARTESIAN_POINT('Ctrl Pts',(-1.003936318643,0.6594544137959,-6.942114569721));
#28481=CARTESIAN_POINT('Ctrl Pts',(-0.3258579542138,1.155927922117,-6.998989569721));
#28482=CARTESIAN_POINT('Ctrl Pts',(0.2318942596183,1.110035356068,-7.036906236387));
#28483=CARTESIAN_POINT('Ctrl Pts',(0.4696881186261,0.9981380597272,-7.055864569721));
#28484=CARTESIAN_POINT('Ctrl Pts',(0.5279823721497,-1.122019654338,-5.314910694393));
#28485=CARTESIAN_POINT('Ctrl Pts',(0.2606752788197,-1.247804824574,-5.333869027727));
#28486=CARTESIAN_POINT('Ctrl Pts',(-0.3663010598456,-1.299393240218,-5.371785694393));
#28487=CARTESIAN_POINT('Ctrl Pts',(-1.128537550737,-0.7413010717389,-5.428660694393));
#28488=CARTESIAN_POINT('Ctrl Pts',(-1.33814455045,0.1797435821333,-5.485535694393));
#28489=CARTESIAN_POINT('Ctrl Pts',(-0.892890536887,1.012779611507,-5.542410694393));
#28490=CARTESIAN_POINT('Ctrl Pts',(-0.01060315691615,1.350133991585,-5.599285694393));
#28491=CARTESIAN_POINT('Ctrl Pts',(0.8768683655278,1.026681130153,-5.656160694393));
#28492=CARTESIAN_POINT('Ctrl Pts',(1.335170067905,0.2007338620856,-5.713035694393));
#28493=CARTESIAN_POINT('Ctrl Pts',(1.139990581936,-0.723460043259,-5.769910694393));
#28494=CARTESIAN_POINT('Ctrl Pts',(0.3868583419482,-1.293566238123,-5.826785694393));
#28495=CARTESIAN_POINT('Ctrl Pts',(-0.555616470709,-1.230554075189,-5.883660694393));
#28496=CARTESIAN_POINT('Ctrl Pts',(-1.226152364316,-0.5652639823961,-5.940535694393));
#28497=CARTESIAN_POINT('Ctrl Pts',(-1.296564691016,0.3766868641562,-5.997410694393));
#28498=CARTESIAN_POINT('Ctrl Pts',(-0.7323910942975,1.134273457497,-6.054285694393));
#28499=CARTESIAN_POINT('Ctrl Pts',(0.190241344867,1.336705360987,-6.111160694393));
#28500=CARTESIAN_POINT('Ctrl Pts',(1.019762749782,0.8849050375959,-6.168035694393));
#28501=CARTESIAN_POINT('Ctrl Pts',(1.350175170634,0.,-6.224910694393));
#28502=CARTESIAN_POINT('Ctrl Pts',(1.019762749782,-0.8849050375959,-6.281785694393));
#28503=CARTESIAN_POINT('Ctrl Pts',(0.190241344867,-1.336705360987,-6.338660694393));
#28504=CARTESIAN_POINT('Ctrl Pts',(-0.7323910942975,-1.134273457497,-6.395535694393));
#28505=CARTESIAN_POINT('Ctrl Pts',(-1.296564691016,-0.3766868641562,-6.452410694393));
#28506=CARTESIAN_POINT('Ctrl Pts',(-1.226152364316,0.5652639823961,-6.509285694393));
#28507=CARTESIAN_POINT('Ctrl Pts',(-0.555616470709,1.230554075189,-6.566160694393));
#28508=CARTESIAN_POINT('Ctrl Pts',(0.3868583419481,1.293566238123,-6.623035694393));
#28509=CARTESIAN_POINT('Ctrl Pts',(1.139990581936,0.723460043259,-6.679910694393));
#28510=CARTESIAN_POINT('Ctrl Pts',(1.335170067905,-0.2007338620856,-6.736785694393));
#28511=CARTESIAN_POINT('Ctrl Pts',(0.8768683655278,-1.026681130153,-6.793660694393));
#28512=CARTESIAN_POINT('Ctrl Pts',(-0.01060315691614,-1.350133991585,-6.850535694393));
#28513=CARTESIAN_POINT('Ctrl Pts',(-0.892890536887,-1.012779611507,-6.907410694393));
#28514=CARTESIAN_POINT('Ctrl Pts',(-1.33814455045,-0.1797435821333,-6.964285694393));
#28515=CARTESIAN_POINT('Ctrl Pts',(-1.128537550737,0.7413010717389,-7.021160694393));
#28516=CARTESIAN_POINT('Ctrl Pts',(-0.3663010598456,1.299393240218,-7.078035694393));
#28517=CARTESIAN_POINT('Ctrl Pts',(0.2606752788197,1.247804824574,-7.11595236106));
#28518=CARTESIAN_POINT('Ctrl Pts',(0.5279823721497,1.122019654338,-7.134910694393));
#28519=CARTESIAN_POINT('Ctrl Pts',(0.5862766256734,-1.24590124895,-5.393956819066));
#28520=CARTESIAN_POINT('Ctrl Pts',(0.2894562980212,-1.38557429308,-5.412915152399));
#28521=CARTESIAN_POINT('Ctrl Pts',(-0.4067441654775,-1.442858558319,-5.450831819066));
#28522=CARTESIAN_POINT('Ctrl Pts',(-1.253138782831,-0.823147729682,-5.507706819066));
#28523=CARTESIAN_POINT('Ctrl Pts',(-1.48588838015,0.1995889756518,-5.564581819066));
#28524=CARTESIAN_POINT('Ctrl Pts',(-0.9914741072328,1.12460007096,-5.621456819066));
#28525=CARTESIAN_POINT('Ctrl Pts',(-0.01177384584446,1.499201569118,-5.678331819066));
#28526=CARTESIAN_POINT('Ctrl Pts',(0.9736829364363,1.140036448902,-5.735206819066));
#28527=CARTESIAN_POINT('Ctrl Pts',(1.482585486565,0.2228967812747,-5.792081819066));
#28528=CARTESIAN_POINT('Ctrl Pts',(1.265856337127,-0.8033368827153,-5.848956819066));
#28529=CARTESIAN_POINT('Ctrl Pts',(0.4295711661878,-1.436388200015,-5.905831819066));
#28530=CARTESIAN_POINT('Ctrl Pts',(-0.61696179039,-1.36641889761,-5.962706819066));
#28531=CARTESIAN_POINT('Ctrl Pts',(-1.361531196175,-0.6276744787227,-6.019581819066));
#28532=CARTESIAN_POINT('Ctrl Pts',(-1.439717710501,0.4182766609306,-6.076456819066));
#28533=CARTESIAN_POINT('Ctrl Pts',(-0.8132540063595,1.259507988013,-6.133331819066));
#28534=CARTESIAN_POINT('Ctrl Pts',(0.211245790798,1.484290290542,-6.190206819066));
#28535=CARTESIAN_POINT('Ctrl Pts',(1.132354213826,0.9826069332027,-6.247081819066));
#28536=CARTESIAN_POINT('Ctrl Pts',(1.499247294724,0.,-6.303956819066));
#28537=CARTESIAN_POINT('Ctrl Pts',(1.132354213826,-0.9826069332027,-6.360831819066));
#28538=CARTESIAN_POINT('Ctrl Pts',(0.211245790798,-1.484290290542,-6.417706819066));
#28539=CARTESIAN_POINT('Ctrl Pts',(-0.8132540063595,-1.259507988013,-6.474581819066));
#28540=CARTESIAN_POINT('Ctrl Pts',(-1.439717710501,-0.4182766609306,-6.531456819066));
#28541=CARTESIAN_POINT('Ctrl Pts',(-1.361531196175,0.6276744787227,-6.588331819066));
#28542=CARTESIAN_POINT('Ctrl Pts',(-0.61696179039,1.36641889761,-6.645206819066));
#28543=CARTESIAN_POINT('Ctrl Pts',(0.4295711661878,1.436388200015,-6.702081819066));
#28544=CARTESIAN_POINT('Ctrl Pts',(1.265856337127,0.8033368827153,-6.758956819066));
#28545=CARTESIAN_POINT('Ctrl Pts',(1.482585486565,-0.2228967812747,-6.815831819066));
#28546=CARTESIAN_POINT('Ctrl Pts',(0.9736829364363,-1.140036448902,-6.872706819066));
#28547=CARTESIAN_POINT('Ctrl Pts',(-0.01177384584445,-1.499201569118,-6.929581819066));
#28548=CARTESIAN_POINT('Ctrl Pts',(-0.9914741072328,-1.12460007096,-6.986456819066));
#28549=CARTESIAN_POINT('Ctrl Pts',(-1.48588838015,-0.1995889756518,-7.043331819066));
#28550=CARTESIAN_POINT('Ctrl Pts',(-1.253138782831,0.823147729682,-7.100206819066));
#28551=CARTESIAN_POINT('Ctrl Pts',(-0.4067441654775,1.442858558319,-7.157081819066));
#28552=CARTESIAN_POINT('Ctrl Pts',(0.2894562980212,1.38557429308,-7.194998485733));
#28553=CARTESIAN_POINT('Ctrl Pts',(0.5862766256734,1.24590124895,-7.213956819066));
#28554=CARTESIAN_POINT('Ctrl Pts',(0.644570879197,-1.369782843561,-5.473002943739));
#28555=CARTESIAN_POINT('Ctrl Pts',(0.3182373172226,-1.523343761587,-5.491961277072));
#28556=CARTESIAN_POINT('Ctrl Pts',(-0.4471872711094,-1.586323876419,-5.529877943739));
#28557=CARTESIAN_POINT('Ctrl Pts',(-1.377740014924,-0.904994387625,-5.586752943739));
#28558=CARTESIAN_POINT('Ctrl Pts',(-1.633632209849,0.2194343691702,-5.643627943739));
#28559=CARTESIAN_POINT('Ctrl Pts',(-1.090057677579,1.236420530413,-5.700502943739));
#28560=CARTESIAN_POINT('Ctrl Pts',(-0.01294453477278,1.648269146651,-5.757377943739));
#28561=CARTESIAN_POINT('Ctrl Pts',(1.070497507345,1.253391767652,-5.814252943739));
#28562=CARTESIAN_POINT('Ctrl Pts',(1.630000905225,0.2450597004638,-5.871127943739));
#28563=CARTESIAN_POINT('Ctrl Pts',(1.391722092318,-0.8832137221716,-5.928002943739));
#28564=CARTESIAN_POINT('Ctrl Pts',(0.4722839904274,-1.579210161907,-5.984877943739));
#28565=CARTESIAN_POINT('Ctrl Pts',(-0.6783071100709,-1.502283720031,-6.041752943739));
#28566=CARTESIAN_POINT('Ctrl Pts',(-1.496910028035,-0.6900849750494,-6.098627943739));
#28567=CARTESIAN_POINT('Ctrl Pts',(-1.582870729986,0.4598664577049,-6.155502943739));
#28568=CARTESIAN_POINT('Ctrl Pts',(-0.8941169184216,1.384742518528,-6.212377943739));
#28569=CARTESIAN_POINT('Ctrl Pts',(0.232250236729,1.631875220096,-6.269252943739));
#28570=CARTESIAN_POINT('Ctrl Pts',(1.24494567787,1.080308828809,-6.326127943739));
#28571=CARTESIAN_POINT('Ctrl Pts',(1.648319418813,0.,-6.383002943739));
#28572=CARTESIAN_POINT('Ctrl Pts',(1.24494567787,-1.080308828809,-6.439877943739));
#28573=CARTESIAN_POINT('Ctrl Pts',(0.232250236729,-1.631875220096,-6.496752943739));
#28574=CARTESIAN_POINT('Ctrl Pts',(-0.8941169184215,-1.384742518528,-6.553627943739));
#28575=CARTESIAN_POINT('Ctrl Pts',(-1.582870729986,-0.459866457705,-6.610502943739));
#28576=CARTESIAN_POINT('Ctrl Pts',(-1.496910028035,0.6900849750494,-6.667377943739));
#28577=CARTESIAN_POINT('Ctrl Pts',(-0.6783071100709,1.502283720031,-6.724252943739));
#28578=CARTESIAN_POINT('Ctrl Pts',(0.4722839904274,1.579210161907,-6.781127943739));
#28579=CARTESIAN_POINT('Ctrl Pts',(1.391722092317,0.8832137221716,-6.838002943739));
#28580=CARTESIAN_POINT('Ctrl Pts',(1.630000905225,-0.2450597004637,-6.894877943739));
#28581=CARTESIAN_POINT('Ctrl Pts',(1.070497507345,-1.253391767652,-6.951752943739));
#28582=CARTESIAN_POINT('Ctrl Pts',(-0.01294453477276,-1.648269146651,-7.008627943739));
#28583=CARTESIAN_POINT('Ctrl Pts',(-1.090057677579,-1.236420530413,-7.065502943739));
#28584=CARTESIAN_POINT('Ctrl Pts',(-1.633632209849,-0.2194343691702,-7.122377943739));
#28585=CARTESIAN_POINT('Ctrl Pts',(-1.377740014924,0.904994387625,-7.179252943739));
#28586=CARTESIAN_POINT('Ctrl Pts',(-0.4471872711094,1.586323876419,-7.236127943739));
#28587=CARTESIAN_POINT('Ctrl Pts',(0.3182373172226,1.523343761587,-7.274044610405));
#28588=CARTESIAN_POINT('Ctrl Pts',(0.644570879197,1.369782843561,-7.293002943739));
#28589=CARTESIAN_POINT('',(-1.20091586136076,0.574787353946053,-7.06327277934281));
#28590=CARTESIAN_POINT('',(-8.13146573628545E-11,1.31156054413043,-7.14169893232531));
#28591=CARTESIAN_POINT('Ctrl Pts',(-1.20088997011481,0.57477334405161,-7.06335361601562));
#28592=CARTESIAN_POINT('Ctrl Pts',(-1.14929466356377,0.677923899738821,
-7.06887533691862));
#28593=CARTESIAN_POINT('Ctrl Pts',(-1.08473705535376,0.773701846621558,
-7.07461408917595));
#28594=CARTESIAN_POINT('Ctrl Pts',(-0.921494131220331,0.958846554317305,
-7.08757779188294));
#28595=CARTESIAN_POINT('Ctrl Pts',(-0.820291380180567,1.04425249730464,
-7.09454782527836));
#28596=CARTESIAN_POINT('Ctrl Pts',(-0.616359073722479,1.17025704400948,
-7.10694522055062));
#28597=CARTESIAN_POINT('Ctrl Pts',(-0.517773004823371,1.21571828362488,
-7.11240671281841));
#28598=CARTESIAN_POINT('Ctrl Pts',(-0.280644665838941,1.29157780830749,
-7.12560673339976));
#28599=CARTESIAN_POINT('Ctrl Pts',(-0.140554389641116,1.31273804394784,
-7.13370645415391));
#28600=CARTESIAN_POINT('Ctrl Pts',(-1.12267799223797E-10,1.31156054441233,
-7.14169893291116));
#28601=CARTESIAN_POINT('Ctrl Pts',(-1.20091584568251,0.574787346442065,
-7.06327277301645));
#28602=CARTESIAN_POINT('Ctrl Pts',(-1.20141090039729,0.573775732839867,
-7.06324582956765));
#28603=CARTESIAN_POINT('Ctrl Pts',(-1.20190467690673,0.572763479868007,
-7.06321888611885));
#28604=CARTESIAN_POINT('Ctrl Pts',(-1.20239717356391,0.571750590758655,
-7.06319194267005));
#28605=CARTESIAN_POINT('Ctrl Pts',(-2.17187379192296E-14,-1.37969296796376,
-6.93054085392112));
#28606=CARTESIAN_POINT('Ctrl Pts',(0.133087605160917,-1.38199709859499,
-6.92421030704033));
#28607=CARTESIAN_POINT('Ctrl Pts',(0.265891834404468,-1.36490138125464,
-6.91827168076586));
#28608=CARTESIAN_POINT('Ctrl Pts',(0.564996978667766,-1.28167294134465,
-6.90378294700708));
#28609=CARTESIAN_POINT('Ctrl Pts',(0.725362476421252,-1.20192290452996,
-6.89502145187575));
#28610=CARTESIAN_POINT('Ctrl Pts',(1.0047343766773,-0.988626905368938,-6.87819012960697));
#28611=CARTESIAN_POINT('Ctrl Pts',(1.1219964500559,-0.857644336593423,-6.870640991457));
#28612=CARTESIAN_POINT('Ctrl Pts',(1.30451451661986,-0.557337293085704,
-6.85430581013491));
#28613=CARTESIAN_POINT('Ctrl Pts',(1.36739414126712,-0.389358231442156,
-6.84553910894255));
#28614=CARTESIAN_POINT('Ctrl Pts',(1.4117263467245,-0.129929452450397,-6.83326155787653));
#28615=CARTESIAN_POINT('Ctrl Pts',(1.41838750216727,-0.044275804343337,
-6.82944557901815));
#28616=CARTESIAN_POINT('Ctrl Pts',(1.41486309456447,0.228784682413614,-6.81720758348837));
#28617=CARTESIAN_POINT('Ctrl Pts',(1.37535002677926,0.414176360005993,-6.80856054737031));
#28618=CARTESIAN_POINT('Ctrl Pts',(1.26691849065933,0.666439120336986,-6.79547529965858));
#28619=CARTESIAN_POINT('Ctrl Pts',(1.22518517031265,0.743282809540594,-6.79134715792347));
#28620=CARTESIAN_POINT('Ctrl Pts',(1.07499110554378,0.967675000265378,-6.77913679426239));
#28621=CARTESIAN_POINT('Ctrl Pts',(0.944978158008963,1.09873235050051,-6.77131126083146));
#28622=CARTESIAN_POINT('Ctrl Pts',(0.641840694562588,1.30646779072398,-6.75429576162248));
#28623=CARTESIAN_POINT('Ctrl Pts',(0.47047451290788,1.38096292093851,-6.74542631518275));
#28624=CARTESIAN_POINT('Ctrl Pts',(0.200851080407334,1.44038429679966,-6.73326404861856));
#28625=CARTESIAN_POINT('Ctrl Pts',(0.110696145530379,1.45152859668681,-6.72934742419146));
#28626=CARTESIAN_POINT('Ctrl Pts',(-0.173735633177461,1.46004938761469,
-6.71675263066477));
#28627=CARTESIAN_POINT('Ctrl Pts',(-0.367192634459145,1.42716351269212,
-6.70761130652016));
#28628=CARTESIAN_POINT('Ctrl Pts',(-0.70587947037252,1.29691374915499,-6.69101716904001));
#28629=CARTESIAN_POINT('Ctrl Pts',(-0.851660931903767,1.20924258790853,
-6.68402027485137));
#28630=CARTESIAN_POINT('Ctrl Pts',(-1.12823162747451,0.970664562207185,
-6.6679529964483));
#28631=CARTESIAN_POINT('Ctrl Pts',(-1.25031504727381,0.813482669717336,
-6.65869106693004));
#28632=CARTESIAN_POINT('Ctrl Pts',(-1.41079480059823,0.490279494856505,
-6.64255921591799));
#28633=CARTESIAN_POINT('Ctrl Pts',(-1.45867635868021,0.33197073342751,-6.63583629784723));
#28634=CARTESIAN_POINT('Ctrl Pts',(-1.49310076179315,0.0682334676735931,
-6.62423350158303));
#28635=CARTESIAN_POINT('Ctrl Pts',(-1.4959309819233,-0.0339812777594436,
-6.61966622893598));
#28636=CARTESIAN_POINT('Ctrl Pts',(-1.48056746832713,-0.240323919983076,
-6.61025451548057));
#28637=CARTESIAN_POINT('Ctrl Pts',(-1.46177071919185,-0.344019227176078,
-6.60543234520265));
#28638=CARTESIAN_POINT('Ctrl Pts',(-1.43217561911113,-0.44490279967413,
-6.60085592339618));
#28639=CARTESIAN_POINT('',(6.96860469514013E-11,1.11628565060287,-7.02888605611368));
#28640=CARTESIAN_POINT('Ctrl Pts',(-1.88721574946309E-6,-1.11628565378659,
-5.27884910577848));
#28641=CARTESIAN_POINT('Ctrl Pts',(-0.0945476136912823,-1.11645975869105,
-5.28558517666919));
#28642=CARTESIAN_POINT('Ctrl Pts',(-0.189124462134144,-1.10484916429063,
-5.29232726977651));
#28643=CARTESIAN_POINT('Ctrl Pts',(-0.372801878429933,-1.05728988862636,
-5.30586972723854));
#28644=CARTESIAN_POINT('Ctrl Pts',(-0.461203748610719,-1.0212041755292,
-5.31262550562909));
#28645=CARTESIAN_POINT('Ctrl Pts',(-0.668471432388832,-0.904915646636021,
-5.32955576649842));
#28646=CARTESIAN_POINT('Ctrl Pts',(-0.780383055419245,-0.811029500761448,
-5.33976498118422));
#28647=CARTESIAN_POINT('Ctrl Pts',(-0.977352549963112,-0.56749819993246,
-5.36210279000144));
#28648=CARTESIAN_POINT('Ctrl Pts',(-1.03703915589554,-0.431145768277833,
-5.37249380692754));
#28649=CARTESIAN_POINT('Ctrl Pts',(-1.11066616674449,-0.178042375581417,
-5.39126431930582));
#28650=CARTESIAN_POINT('Ctrl Pts',(-1.1250370353998,-0.0352369170928276,
-5.40130636574828));
#28651=CARTESIAN_POINT('Ctrl Pts',(-1.09418460733438,0.2967907172898,-5.42509692704672));
#28652=CARTESIAN_POINT('Ctrl Pts',(-1.02997735713431,0.440477084842102,
-5.43601884316658));
#28653=CARTESIAN_POINT('Ctrl Pts',(-0.925588908242808,0.636392952388525,
-5.45182493170545));
#28654=CARTESIAN_POINT('Ctrl Pts',(-0.840538191683142,0.751460714065264,
-5.46183701528019));
#28655=CARTESIAN_POINT('Ctrl Pts',(-0.611182247799737,0.946513834085736,
-5.48331976958516));
#28656=CARTESIAN_POINT('Ctrl Pts',(-0.478234529751118,1.0191711099922,-5.49390080177507));
#28657=CARTESIAN_POINT('Ctrl Pts',(-0.222597234321242,1.1004636264182,-5.51300274809229));
#28658=CARTESIAN_POINT('Ctrl Pts',(-0.0794663775051934,1.12675755955542,
-5.52317074675688));
#28659=CARTESIAN_POINT('Ctrl Pts',(0.232981315456763,1.10176800386665,-5.54552756527266));
#28660=CARTESIAN_POINT('Ctrl Pts',(0.377700605109014,1.06037143957915,-5.5560369702747));
#28661=CARTESIAN_POINT('Ctrl Pts',(0.604852724324514,0.944731736167629,
-5.57419440550631));
#28662=CARTESIAN_POINT('Ctrl Pts',(0.731331226988442,0.863974006299961,
-5.58465639462863));
#28663=CARTESIAN_POINT('Ctrl Pts',(0.943397907937856,0.613934547621998,
-5.6080266301717));
#28664=CARTESIAN_POINT('Ctrl Pts',(1.01607631574406,0.484189787750186,-5.61841215189081));
#28665=CARTESIAN_POINT('Ctrl Pts',(1.11857306467121,0.173002860562979,-5.64176437012636));
#28666=CARTESIAN_POINT('Ctrl Pts',(1.12165266273671,0.0230529286473931,
-5.65222238737627));
#28667=CARTESIAN_POINT('Ctrl Pts',(1.10179845703878,-0.228016486144737,
-5.67016430609243));
#28668=CARTESIAN_POINT('Ctrl Pts',(1.06324590215937,-0.369253565391366,
-5.68039583379269));
#28669=CARTESIAN_POINT('Ctrl Pts',(0.924464855646201,-0.649976757040027,
-5.70272861706242));
#28670=CARTESIAN_POINT('Ctrl Pts',(0.825915661788616,-0.761161572818578,
-5.71310258159158));
#28671=CARTESIAN_POINT('Ctrl Pts',(0.626214316349858,-0.934430304671199,
-5.73193040825594));
#28672=CARTESIAN_POINT('Ctrl Pts',(0.502214996937545,-1.00732385711169,
-5.74199298816798));
#28673=CARTESIAN_POINT('Ctrl Pts',(0.19120199753373,-1.11682300306852,-5.76551693664133));
#28674=CARTESIAN_POINT('Ctrl Pts',(0.0349012702549799,-1.12007370080307,
-5.77638015858152));
#28675=CARTESIAN_POINT('Ctrl Pts',(-0.203851405860734,-1.1061171885703,
-5.79340869558083));
#28676=CARTESIAN_POINT('Ctrl Pts',(-0.341786112597023,-1.07261170247852,
-5.80334911559688));
#28677=CARTESIAN_POINT('Ctrl Pts',(-0.603413551668519,-0.951563052462849,
-5.82391815996146));
#28678=CARTESIAN_POINT('Ctrl Pts',(-0.72511338589894,-0.861211673415831,
-5.83450451982865));
#28679=CARTESIAN_POINT('Ctrl Pts',(-0.905273423514478,-0.663857977873336,
-5.85353245208202));
#28680=CARTESIAN_POINT('Ctrl Pts',(-0.989304020610893,-0.545163021076611,
-5.86369254095246));
#28681=CARTESIAN_POINT('Ctrl Pts',(-1.09791444748826,-0.250846118613204,
-5.88607028582539));
#28682=CARTESIAN_POINT('Ctrl Pts',(-1.12102369397598,-0.101931202388123,
-5.89659192327522));
#28683=CARTESIAN_POINT('Ctrl Pts',(-1.11127472608704,0.152382998725967,
-5.91472029922507));
#28684=CARTESIAN_POINT('Ctrl Pts',(-1.09120934524513,0.300938815206493,
-5.92517036237664));
#28685=CARTESIAN_POINT('Ctrl Pts',(-0.953355092950194,0.59848305772064,
-5.94854743454185));
#28686=CARTESIAN_POINT('Ctrl Pts',(-0.865889506205132,0.719096632405871,
-5.95895154517146));
#28687=CARTESIAN_POINT('Ctrl Pts',(-0.630908211369359,0.938430669099254,
-5.98186059631056));
#28688=CARTESIAN_POINT('Ctrl Pts',(-0.499473987912845,1.00559671816685,
-5.99216596514537));
#28689=CARTESIAN_POINT('Ctrl Pts',(-0.254954649474659,1.09592824110065,
-6.01073734053109));
#28690=CARTESIAN_POINT('Ctrl Pts',(-0.110233508147547,1.12012616746575,
-6.02099044678716));
#28691=CARTESIAN_POINT('Ctrl Pts',(0.202625788977274,1.11169037854405,-6.04330877782007));
#28692=CARTESIAN_POINT('Ctrl Pts',(0.344594062565003,1.06910154094398,-6.0536600973584));
#28693=CARTESIAN_POINT('Ctrl Pts',(0.58636306509553,0.959974916638413,-6.07255024413077));
#28694=CARTESIAN_POINT('Ctrl Pts',(0.704733656287601,0.877644037487909,
-6.08263575715877));
#28695=CARTESIAN_POINT('Ctrl Pts',(0.924445762809001,0.651144082671887,
-6.10514789486953));
#28696=CARTESIAN_POINT('Ctrl Pts',(0.995878303027181,0.517818669122219,
-6.11569215217414));
#28697=CARTESIAN_POINT('Ctrl Pts',(1.08982166380632,0.277939862987319,-6.13403504577381));
#28698=CARTESIAN_POINT('Ctrl Pts',(1.1169872981078,0.139044412854729,-6.14394629670335));
#28699=CARTESIAN_POINT('Ctrl Pts',(1.1169872981078,-0.139044412854725,-6.16378873021465));
#28700=CARTESIAN_POINT('Ctrl Pts',(1.08982166380632,-0.277939862987315,
-6.17369998114575));
#28701=CARTESIAN_POINT('Ctrl Pts',(0.995878303027181,-0.517818669122214,
-6.19204287474531));
#28702=CARTESIAN_POINT('Ctrl Pts',(0.924445762809002,-0.65114408267188,
-6.20258713204978));
#28703=CARTESIAN_POINT('Ctrl Pts',(0.704733656287603,-0.877644037487904,
-6.22509926976052));
#28704=CARTESIAN_POINT('Ctrl Pts',(0.586363065095529,-0.95997491663841,
-6.2351847827886));
#28705=CARTESIAN_POINT('Ctrl Pts',(0.344594062565005,-1.06910154094397,
-6.25407492956103));
#28706=CARTESIAN_POINT('Ctrl Pts',(0.202625788977278,-1.11169037854405,
-6.26442624909944));
#28707=CARTESIAN_POINT('Ctrl Pts',(-0.110233508147536,-1.12012616746575,
-6.28674458013225));
#28708=CARTESIAN_POINT('Ctrl Pts',(-0.254954649474642,-1.09592824110065,
-6.29699768638819));
#28709=CARTESIAN_POINT('Ctrl Pts',(-0.49947398791277,-1.00559671816688,
-6.31556906177377));
#28710=CARTESIAN_POINT('Ctrl Pts',(-0.630908211369293,-0.938430669099308,
-6.32587443060851));
#28711=CARTESIAN_POINT('Ctrl Pts',(-0.865889506205105,-0.719096632405904,
-6.34878348174746));
#28712=CARTESIAN_POINT('Ctrl Pts',(-0.953355092950167,-0.598483057720682,
-6.35918759237696));
#28713=CARTESIAN_POINT('Ctrl Pts',(-1.09120934524511,-0.300938815206565,
-6.38256466454204));
#28714=CARTESIAN_POINT('Ctrl Pts',(-1.11127472608703,-0.152382998726048,
-6.39301472769358));
#28715=CARTESIAN_POINT('Ctrl Pts',(-1.12102369397598,0.101931202388064,
-6.41114310364352));
#28716=CARTESIAN_POINT('Ctrl Pts',(-1.09791444748827,0.25084611861315,-6.42166474109352));
#28717=CARTESIAN_POINT('Ctrl Pts',(-0.989304020610917,0.545163021076569,
-6.44404248596658));
#28718=CARTESIAN_POINT('Ctrl Pts',(-0.905273423514503,0.663857977873303,
-6.45420257483704));
#28719=CARTESIAN_POINT('Ctrl Pts',(-0.725113385898966,0.861211673415812,
-6.47323050709036));
#28720=CARTESIAN_POINT('Ctrl Pts',(-0.603413551668548,0.951563052462836,
-6.48381686695739));
#28721=CARTESIAN_POINT('Ctrl Pts',(-0.341786112597061,1.07261170247852,
-6.50438591132201));
#28722=CARTESIAN_POINT('Ctrl Pts',(-0.203851405860781,1.10611718857029,
-6.5143263313382));
#28723=CARTESIAN_POINT('Ctrl Pts',(0.0349012702549208,1.12007370080308,
-6.5313548683377));
#28724=CARTESIAN_POINT('Ctrl Pts',(0.191201997533662,1.11682300306852,-6.54221809027818));
#28725=CARTESIAN_POINT('Ctrl Pts',(0.502214996937503,1.00732385711169,-6.56574203875153));
#28726=CARTESIAN_POINT('Ctrl Pts',(0.626214316349841,0.934430304671178,
-6.57580461866341));
#28727=CARTESIAN_POINT('Ctrl Pts',(0.825915661788616,0.761161572818541,
-6.59463244532758));
#28728=CARTESIAN_POINT('Ctrl Pts',(0.924464855646203,0.649976757039995,
-6.60500640985651));
#28729=CARTESIAN_POINT('Ctrl Pts',(1.06324590215937,0.369253565391355,-6.62733919312616));
#28730=CARTESIAN_POINT('Ctrl Pts',(1.10179845703877,0.228016486144744,-6.63757072082647));
#28731=CARTESIAN_POINT('Ctrl Pts',(1.12165266273671,-0.0230529286473764,
-6.65551263954268));
#28732=CARTESIAN_POINT('Ctrl Pts',(1.11857306467121,-0.173002860562959,
-6.66597065679268));
#28733=CARTESIAN_POINT('Ctrl Pts',(1.01607631574407,-0.484189787750162,
-6.68932287502831));
#28734=CARTESIAN_POINT('Ctrl Pts',(0.943397907937869,-0.613934547621979,
-6.69970839674746));
#28735=CARTESIAN_POINT('Ctrl Pts',(0.731331226988447,-0.863974006299962,
-6.72307863229059));
#28736=CARTESIAN_POINT('Ctrl Pts',(0.604852724324511,-0.944731736167631,
-6.73354062141294));
#28737=CARTESIAN_POINT('Ctrl Pts',(0.377700605109025,-1.06037143957915,
-6.75169805664457));
#28738=CARTESIAN_POINT('Ctrl Pts',(0.232981315456777,-1.10176800386664,
-6.76220746164662));
#28739=CARTESIAN_POINT('Ctrl Pts',(-0.0794663775051798,-1.12675755955542,
-6.78456428016241));
#28740=CARTESIAN_POINT('Ctrl Pts',(-0.222597234321231,-1.1004636264182,
-6.794732278827));
#28741=CARTESIAN_POINT('Ctrl Pts',(-0.478234529751108,-1.0191711099922,
-6.81383422514422));
#28742=CARTESIAN_POINT('Ctrl Pts',(-0.61118224779973,-0.946513834085739,
-6.82441525733414));
#28743=CARTESIAN_POINT('Ctrl Pts',(-0.840538191683137,-0.751460714065269,
-6.845898011639));
#28744=CARTESIAN_POINT('Ctrl Pts',(-0.925588908242802,-0.636392952388533,
-6.8559100952136));
#28745=CARTESIAN_POINT('Ctrl Pts',(-1.02997735713434,-0.440477084842058,
-6.87171618375233));
#28746=CARTESIAN_POINT('Ctrl Pts',(-1.09418460733438,-0.29679071728976,
-6.88263809987196));
#28747=CARTESIAN_POINT('Ctrl Pts',(-1.1250370353998,0.0352369170927682,
-6.90642866117045));
#28748=CARTESIAN_POINT('Ctrl Pts',(-1.11066616674449,0.178042375581336,
-6.91647070761312));
#28749=CARTESIAN_POINT('Ctrl Pts',(-1.03703915589555,0.431145768277744,
-6.93524121999159));
#28750=CARTESIAN_POINT('Ctrl Pts',(-0.977352549963121,0.56749819993238,
-6.94563223691791));
#28751=CARTESIAN_POINT('Ctrl Pts',(-0.780383055419225,0.811029500761411,
-6.96797004573509));
#28752=CARTESIAN_POINT('Ctrl Pts',(-0.668471432388786,0.904915646636011,
-6.97817926042072));
#28753=CARTESIAN_POINT('Ctrl Pts',(-0.461204214700216,1.02120391402741,
-6.99510948321823));
#28754=CARTESIAN_POINT('Ctrl Pts',(-0.372802887179955,1.05728947562774,
-7.00186522258021));
#28755=CARTESIAN_POINT('Ctrl Pts',(-0.189124960613764,1.10484918598421,
-7.0154077230962));
#28756=CARTESIAN_POINT('Ctrl Pts',(-0.0945469086635694,1.11645991422468,
-7.02214990053352));
#28757=CARTESIAN_POINT('Ctrl Pts',(1.05351468695941E-10,1.11628565030954,
-7.02888605560556));
#28758=CARTESIAN_POINT('Ctrl Pts',(1.89848396344249E-15,1.11628565075286,
-7.02888605585406));
#28759=CARTESIAN_POINT('Ctrl Pts',(-3.50013929086958E-15,1.14889336813908,
-7.04772396350255));
#28760=CARTESIAN_POINT('Ctrl Pts',(-2.79399731606342E-12,1.18150108552538,
-7.06656187115091));
#28761=CARTESIAN_POINT('Ctrl Pts',(-2.79399731606342E-12,1.24659271658915,
-7.10416616341545));
#28762=CARTESIAN_POINT('Ctrl Pts',(-1.24952051716895E-14,1.27907663026664,
-7.12293254803162));
#28763=CARTESIAN_POINT('Ctrl Pts',(2.20773575809264E-15,1.31156054394421,
-7.14169893264765));
#28764=CARTESIAN_POINT('Origin',(0.,0.,-7.2));
#28765=CARTESIAN_POINT('',(0.,1.331411920116,-7.06319194267));
#28766=CARTESIAN_POINT('Origin',(0.,1.707288968431,-7.2));
#28767=CARTESIAN_POINT('Origin',(0.,0.,-7.06319194267));
#28768=CARTESIAN_POINT('',(0.,-1.707288968431,-7.6));
#28769=CARTESIAN_POINT('Origin',(2.09082597040861E-16,-1.707288968431,-7.2));
#28770=CARTESIAN_POINT('Origin',(0.,0.,-7.6));
#28771=CARTESIAN_POINT('Origin',(0.,0.,-6.89357235801));
#28772=CARTESIAN_POINT('',(0.,1.331411920116,-7.06319194267));
#28773=CARTESIAN_POINT('Origin',(0.,1.5,-7.));
#28774=CARTESIAN_POINT('Ctrl Pts',(-2.59235181799925E-15,1.11628565030974,
-6.97115102811021));
#28775=CARTESIAN_POINT('Ctrl Pts',(-2.33645276180641E-15,1.11628565030974,
-6.98076735207347));
#28776=CARTESIAN_POINT('Ctrl Pts',(2.8796409701215E-15,1.11628565030974,
-6.99038367603674));
#28777=CARTESIAN_POINT('Ctrl Pts',(2.8796409701215E-15,1.11628565030974,
-7.00962868537123));
#28778=CARTESIAN_POINT('Ctrl Pts',(-2.34957117002464E-15,1.11628565030974,
-7.01925737074246));
#28779=CARTESIAN_POINT('Ctrl Pts',(-2.59329306483399E-15,1.11628565030974,
-7.02888605611369));
#28780=CARTESIAN_POINT('Ctrl Pts',(0.4755900604755,-1.010680324589,-5.170126599063));
#28781=CARTESIAN_POINT('Ctrl Pts',(0.2348081643589,-1.123983684464,-5.189084932396));
#28782=CARTESIAN_POINT('Ctrl Pts',(-0.329952574922,-1.170452920957,-5.227001599063));
#28783=CARTESIAN_POINT('Ctrl Pts',(-1.016551442463,-0.6677408946504,-5.283876599063));
#28784=CARTESIAN_POINT('Ctrl Pts',(-1.205358893105,0.1619074151071,-5.340751599063));
#28785=CARTESIAN_POINT('Ctrl Pts',(-0.8042879589087,0.9122802996697,-5.397626599063));
#28786=CARTESIAN_POINT('Ctrl Pts',(-0.009550993186477,1.216158607898,-5.454501599063));
#28787=CARTESIAN_POINT('Ctrl Pts',(0.7898556864549,0.9248023542725,-5.511376599063));
#28788=CARTESIAN_POINT('Ctrl Pts',(1.202679571961,0.180814804896,-5.568251599063));
#28789=CARTESIAN_POINT('Ctrl Pts',(1.026867975908,-0.6516702524068,-5.625126599063));
#28790=CARTESIAN_POINT('Ctrl Pts',(0.348469933747,-1.165204139133,-5.682001599063));
#28791=CARTESIAN_POINT('Ctrl Pts',(-0.5004819949382,-1.108444747226,-5.738876599063));
#28792=CARTESIAN_POINT('Ctrl Pts',(-1.104479823299,-0.5091721726955,-5.795751599063));
#28793=CARTESIAN_POINT('Ctrl Pts',(-1.167905052019,0.3393077836576,-5.852626599063));
#28794=CARTESIAN_POINT('Ctrl Pts',(-0.6597150647482,1.02171816845,-5.909501599063));
#28795=CARTESIAN_POINT('Ctrl Pts',(0.1713634724997,1.204062516105,-5.966376599063));
#28796=CARTESIAN_POINT('Ctrl Pts',(0.9185704929214,0.7970948701029,-6.023251599063));
#28797=CARTESIAN_POINT('Ctrl Pts',(1.216195700701,0.,-6.080126599063));
#28798=CARTESIAN_POINT('Ctrl Pts',(0.9185704929214,-0.7970948701029,-6.137001599063));
#28799=CARTESIAN_POINT('Ctrl Pts',(0.1713634724997,-1.204062516105,-6.193876599063));
#28800=CARTESIAN_POINT('Ctrl Pts',(-0.6597150647482,-1.02171816845,-6.250751599063));
#28801=CARTESIAN_POINT('Ctrl Pts',(-1.167905052019,-0.3393077836576,-6.307626599063));
#28802=CARTESIAN_POINT('Ctrl Pts',(-1.104479823299,0.5091721726955,-6.364501599063));
#28803=CARTESIAN_POINT('Ctrl Pts',(-0.5004819949382,1.108444747226,-6.421376599063));
#28804=CARTESIAN_POINT('Ctrl Pts',(0.3484699337469,1.165204139133,-6.478251599063));
#28805=CARTESIAN_POINT('Ctrl Pts',(1.026867975908,0.6516702524068,-6.535126599063));
#28806=CARTESIAN_POINT('Ctrl Pts',(1.202679571961,-0.180814804896,-6.592001599063));
#28807=CARTESIAN_POINT('Ctrl Pts',(0.7898556864549,-0.9248023542725,-6.648876599063));
#28808=CARTESIAN_POINT('Ctrl Pts',(-0.009550993186468,-1.216158607898,-6.705751599063));
#28809=CARTESIAN_POINT('Ctrl Pts',(-0.8042879589087,-0.9122802996697,-6.762626599063));
#28810=CARTESIAN_POINT('Ctrl Pts',(-1.205358893105,-0.1619074151071,-6.819501599063));
#28811=CARTESIAN_POINT('Ctrl Pts',(-1.016551442463,0.6677408946503,-6.876376599063));
#28812=CARTESIAN_POINT('Ctrl Pts',(-0.329952574922,1.170452920957,-6.933251599063));
#28813=CARTESIAN_POINT('Ctrl Pts',(0.2348081643589,1.123983684464,-6.97116826573));
#28814=CARTESIAN_POINT('Ctrl Pts',(0.4755900604755,1.010680324589,-6.990126599063));
#28815=CARTESIAN_POINT('Ctrl Pts',(0.4755900604755,-1.010680324589,-5.200042199688));
#28816=CARTESIAN_POINT('Ctrl Pts',(0.2348081643589,-1.123983684464,-5.219000533021));
#28817=CARTESIAN_POINT('Ctrl Pts',(-0.329952574922,-1.170452920957,-5.256917199688));
#28818=CARTESIAN_POINT('Ctrl Pts',(-1.016551442463,-0.6677408946504,-5.313792199688));
#28819=CARTESIAN_POINT('Ctrl Pts',(-1.205358893105,0.1619074151071,-5.370667199688));
#28820=CARTESIAN_POINT('Ctrl Pts',(-0.8042879589087,0.9122802996697,-5.427542199688));
#28821=CARTESIAN_POINT('Ctrl Pts',(-0.009550993186478,1.216158607898,-5.484417199688));
#28822=CARTESIAN_POINT('Ctrl Pts',(0.7898556864549,0.9248023542725,-5.541292199688));
#28823=CARTESIAN_POINT('Ctrl Pts',(1.202679571961,0.180814804896,-5.598167199688));
#28824=CARTESIAN_POINT('Ctrl Pts',(1.026867975908,-0.6516702524068,-5.655042199688));
#28825=CARTESIAN_POINT('Ctrl Pts',(0.348469933747,-1.165204139133,-5.711917199688));
#28826=CARTESIAN_POINT('Ctrl Pts',(-0.5004819949382,-1.108444747226,-5.768792199688));
#28827=CARTESIAN_POINT('Ctrl Pts',(-1.104479823299,-0.5091721726955,-5.825667199688));
#28828=CARTESIAN_POINT('Ctrl Pts',(-1.167905052019,0.3393077836576,-5.882542199688));
#28829=CARTESIAN_POINT('Ctrl Pts',(-0.6597150647482,1.02171816845,-5.939417199688));
#28830=CARTESIAN_POINT('Ctrl Pts',(0.1713634724997,1.204062516105,-5.996292199688));
#28831=CARTESIAN_POINT('Ctrl Pts',(0.9185704929214,0.797094870103,-6.053167199688));
#28832=CARTESIAN_POINT('Ctrl Pts',(1.216195700701,0.,-6.110042199688));
#28833=CARTESIAN_POINT('Ctrl Pts',(0.9185704929214,-0.7970948701029,-6.166917199688));
#28834=CARTESIAN_POINT('Ctrl Pts',(0.1713634724997,-1.204062516105,-6.223792199688));
#28835=CARTESIAN_POINT('Ctrl Pts',(-0.6597150647482,-1.02171816845,-6.280667199688));
#28836=CARTESIAN_POINT('Ctrl Pts',(-1.167905052019,-0.3393077836576,-6.337542199688));
#28837=CARTESIAN_POINT('Ctrl Pts',(-1.104479823299,0.5091721726955,-6.394417199688));
#28838=CARTESIAN_POINT('Ctrl Pts',(-0.5004819949382,1.108444747226,-6.451292199688));
#28839=CARTESIAN_POINT('Ctrl Pts',(0.3484699337469,1.165204139133,-6.508167199688));
#28840=CARTESIAN_POINT('Ctrl Pts',(1.026867975908,0.6516702524068,-6.565042199688));
#28841=CARTESIAN_POINT('Ctrl Pts',(1.202679571961,-0.180814804896,-6.621917199688));
#28842=CARTESIAN_POINT('Ctrl Pts',(0.7898556864549,-0.9248023542725,-6.678792199688));
#28843=CARTESIAN_POINT('Ctrl Pts',(-0.009550993186468,-1.216158607898,-6.735667199688));
#28844=CARTESIAN_POINT('Ctrl Pts',(-0.8042879589087,-0.9122802996697,-6.792542199688));
#28845=CARTESIAN_POINT('Ctrl Pts',(-1.205358893105,-0.1619074151071,-6.849417199688));
#28846=CARTESIAN_POINT('Ctrl Pts',(-1.016551442463,0.6677408946503,-6.906292199688));
#28847=CARTESIAN_POINT('Ctrl Pts',(-0.329952574922,1.170452920957,-6.963167199688));
#28848=CARTESIAN_POINT('Ctrl Pts',(0.2348081643589,1.123983684464,-7.001083866354));
#28849=CARTESIAN_POINT('Ctrl Pts',(0.4755900604755,1.010680324589,-7.020042199688));
#28850=CARTESIAN_POINT('Ctrl Pts',(0.4755900604755,-1.010680324589,-5.229957800312));
#28851=CARTESIAN_POINT('Ctrl Pts',(0.2348081643589,-1.123983684464,-5.248916133646));
#28852=CARTESIAN_POINT('Ctrl Pts',(-0.329952574922,-1.170452920957,-5.286832800312));
#28853=CARTESIAN_POINT('Ctrl Pts',(-1.016551442463,-0.6677408946504,-5.343707800312));
#28854=CARTESIAN_POINT('Ctrl Pts',(-1.205358893105,0.1619074151071,-5.400582800312));
#28855=CARTESIAN_POINT('Ctrl Pts',(-0.8042879589087,0.9122802996697,-5.457457800312));
#28856=CARTESIAN_POINT('Ctrl Pts',(-0.009550993186477,1.216158607898,-5.514332800312));
#28857=CARTESIAN_POINT('Ctrl Pts',(0.7898556864549,0.9248023542725,-5.571207800312));
#28858=CARTESIAN_POINT('Ctrl Pts',(1.202679571961,0.180814804896,-5.628082800312));
#28859=CARTESIAN_POINT('Ctrl Pts',(1.026867975908,-0.6516702524068,-5.684957800312));
#28860=CARTESIAN_POINT('Ctrl Pts',(0.348469933747,-1.165204139133,-5.741832800312));
#28861=CARTESIAN_POINT('Ctrl Pts',(-0.5004819949382,-1.108444747226,-5.798707800312));
#28862=CARTESIAN_POINT('Ctrl Pts',(-1.104479823299,-0.5091721726955,-5.855582800312));
#28863=CARTESIAN_POINT('Ctrl Pts',(-1.167905052019,0.3393077836576,-5.912457800312));
#28864=CARTESIAN_POINT('Ctrl Pts',(-0.6597150647482,1.02171816845,-5.969332800312));
#28865=CARTESIAN_POINT('Ctrl Pts',(0.1713634724997,1.204062516105,-6.026207800312));
#28866=CARTESIAN_POINT('Ctrl Pts',(0.9185704929214,0.7970948701029,-6.083082800312));
#28867=CARTESIAN_POINT('Ctrl Pts',(1.216195700701,0.,-6.139957800312));
#28868=CARTESIAN_POINT('Ctrl Pts',(0.9185704929214,-0.7970948701029,-6.196832800312));
#28869=CARTESIAN_POINT('Ctrl Pts',(0.1713634724997,-1.204062516105,-6.253707800312));
#28870=CARTESIAN_POINT('Ctrl Pts',(-0.6597150647482,-1.02171816845,-6.310582800312));
#28871=CARTESIAN_POINT('Ctrl Pts',(-1.167905052019,-0.3393077836576,-6.367457800312));
#28872=CARTESIAN_POINT('Ctrl Pts',(-1.104479823299,0.5091721726955,-6.424332800312));
#28873=CARTESIAN_POINT('Ctrl Pts',(-0.5004819949382,1.108444747226,-6.481207800312));
#28874=CARTESIAN_POINT('Ctrl Pts',(0.3484699337469,1.165204139133,-6.538082800312));
#28875=CARTESIAN_POINT('Ctrl Pts',(1.026867975908,0.6516702524068,-6.594957800312));
#28876=CARTESIAN_POINT('Ctrl Pts',(1.202679571961,-0.180814804896,-6.651832800312));
#28877=CARTESIAN_POINT('Ctrl Pts',(0.7898556864549,-0.9248023542725,-6.708707800312));
#28878=CARTESIAN_POINT('Ctrl Pts',(-0.009550993186468,-1.216158607898,-6.765582800312));
#28879=CARTESIAN_POINT('Ctrl Pts',(-0.8042879589087,-0.9122802996697,-6.822457800312));
#28880=CARTESIAN_POINT('Ctrl Pts',(-1.205358893105,-0.1619074151071,-6.879332800312));
#28881=CARTESIAN_POINT('Ctrl Pts',(-1.016551442463,0.6677408946503,-6.936207800312));
#28882=CARTESIAN_POINT('Ctrl Pts',(-0.329952574922,1.170452920957,-6.993082800312));
#28883=CARTESIAN_POINT('Ctrl Pts',(0.2348081643589,1.123983684464,-7.030999466979));
#28884=CARTESIAN_POINT('Ctrl Pts',(0.4755900604755,1.010680324589,-7.049957800312));
#28885=CARTESIAN_POINT('Ctrl Pts',(0.4755900604755,-1.010680324589,-5.259873400937));
#28886=CARTESIAN_POINT('Ctrl Pts',(0.2348081643589,-1.123983684464,-5.27883173427));
#28887=CARTESIAN_POINT('Ctrl Pts',(-0.329952574922,-1.170452920957,-5.316748400937));
#28888=CARTESIAN_POINT('Ctrl Pts',(-1.016551442463,-0.6677408946504,-5.373623400937));
#28889=CARTESIAN_POINT('Ctrl Pts',(-1.205358893105,0.1619074151071,-5.430498400937));
#28890=CARTESIAN_POINT('Ctrl Pts',(-0.8042879589087,0.9122802996697,-5.487373400937));
#28891=CARTESIAN_POINT('Ctrl Pts',(-0.009550993186477,1.216158607898,-5.544248400937));
#28892=CARTESIAN_POINT('Ctrl Pts',(0.7898556864549,0.9248023542725,-5.601123400937));
#28893=CARTESIAN_POINT('Ctrl Pts',(1.202679571961,0.180814804896,-5.657998400937));
#28894=CARTESIAN_POINT('Ctrl Pts',(1.026867975908,-0.6516702524068,-5.714873400937));
#28895=CARTESIAN_POINT('Ctrl Pts',(0.348469933747,-1.165204139133,-5.771748400937));
#28896=CARTESIAN_POINT('Ctrl Pts',(-0.5004819949382,-1.108444747226,-5.828623400937));
#28897=CARTESIAN_POINT('Ctrl Pts',(-1.104479823299,-0.5091721726955,-5.885498400937));
#28898=CARTESIAN_POINT('Ctrl Pts',(-1.167905052019,0.3393077836576,-5.942373400937));
#28899=CARTESIAN_POINT('Ctrl Pts',(-0.6597150647482,1.02171816845,-5.999248400937));
#28900=CARTESIAN_POINT('Ctrl Pts',(0.1713634724997,1.204062516105,-6.056123400937));
#28901=CARTESIAN_POINT('Ctrl Pts',(0.9185704929214,0.7970948701029,-6.112998400937));
#28902=CARTESIAN_POINT('Ctrl Pts',(1.216195700701,0.,-6.169873400937));
#28903=CARTESIAN_POINT('Ctrl Pts',(0.9185704929214,-0.7970948701029,-6.226748400937));
#28904=CARTESIAN_POINT('Ctrl Pts',(0.1713634724997,-1.204062516105,-6.283623400937));
#28905=CARTESIAN_POINT('Ctrl Pts',(-0.6597150647482,-1.02171816845,-6.340498400937));
#28906=CARTESIAN_POINT('Ctrl Pts',(-1.167905052019,-0.3393077836576,-6.397373400937));
#28907=CARTESIAN_POINT('Ctrl Pts',(-1.104479823299,0.5091721726955,-6.454248400937));
#28908=CARTESIAN_POINT('Ctrl Pts',(-0.5004819949382,1.108444747226,-6.511123400937));
#28909=CARTESIAN_POINT('Ctrl Pts',(0.3484699337469,1.165204139133,-6.567998400937));
#28910=CARTESIAN_POINT('Ctrl Pts',(1.026867975908,0.6516702524068,-6.624873400937));
#28911=CARTESIAN_POINT('Ctrl Pts',(1.202679571961,-0.180814804896,-6.681748400937));
#28912=CARTESIAN_POINT('Ctrl Pts',(0.7898556864549,-0.9248023542725,-6.738623400937));
#28913=CARTESIAN_POINT('Ctrl Pts',(-0.009550993186468,-1.216158607898,-6.795498400937));
#28914=CARTESIAN_POINT('Ctrl Pts',(-0.8042879589087,-0.9122802996697,-6.852373400937));
#28915=CARTESIAN_POINT('Ctrl Pts',(-1.205358893105,-0.1619074151071,-6.909248400937));
#28916=CARTESIAN_POINT('Ctrl Pts',(-1.016551442463,0.6677408946503,-6.966123400937));
#28917=CARTESIAN_POINT('Ctrl Pts',(-0.329952574922,1.170452920957,-7.022998400937));
#28918=CARTESIAN_POINT('Ctrl Pts',(0.2348081643589,1.123983684464,-7.060915067604));
#28919=CARTESIAN_POINT('Ctrl Pts',(0.4755900604755,1.010680324589,-7.079873400937));
#28920=CARTESIAN_POINT('Origin',(0.,0.,-7.6));
#28921=CARTESIAN_POINT('',(0.,-3.,-7.6));
#28922=CARTESIAN_POINT('Origin',(0.,0.,-7.6));
#28923=CARTESIAN_POINT('Origin',(0.,0.,-10.5));
#28924=CARTESIAN_POINT('',(0.,-3.,-8.6));
#28925=CARTESIAN_POINT('',(3.67394039744206E-16,-3.,-10.5));
#28926=CARTESIAN_POINT('',(3.,7.14126831766994E-13,-8.6));
#28927=CARTESIAN_POINT('Origin',(0.,0.,-8.6));
#28928=CARTESIAN_POINT('Origin',(0.,0.,-8.6));
#28929=CARTESIAN_POINT('Ctrl Pts',(3.00000000000014,7.14494225807769E-13,
-8.59999999999797));
#28930=CARTESIAN_POINT('Ctrl Pts',(3.00000000000014,-3.00000000000558,-8.59999999999645));
#28931=CARTESIAN_POINT('Ctrl Pts',(-6.16031515686365E-12,-3.00000000000558,
-8.59999999999894));
#28932=CARTESIAN_POINT('Ctrl Pts',(-3.00000000001246,-3.00000000000558,
-8.60000000000143));
#28933=CARTESIAN_POINT('Ctrl Pts',(-3.00000000001246,7.1449422580777E-13,
-8.60000000000295));
#28934=CARTESIAN_POINT('Ctrl Pts',(-3.00000000001246,3.00000000000701,-8.60000000000448));
#28935=CARTESIAN_POINT('Ctrl Pts',(-6.16031515686112E-12,3.00000000000701,
-8.60000000000199));
#28936=CARTESIAN_POINT('Ctrl Pts',(3.00000000000014,3.00000000000701,-8.5999999999995));
#28937=CARTESIAN_POINT('Ctrl Pts',(3.00000000000014,7.14494225807769E-13,
-8.59999999999797));
#28938=CARTESIAN_POINT('Ctrl Pts',(2.55972036857699,2.46694403342024E-15,
-10.0000000000082));
#28939=CARTESIAN_POINT('Ctrl Pts',(2.55972036857699,-2.55972036858199,-10.0000000000069));
#28940=CARTESIAN_POINT('Ctrl Pts',(-4.99935688766318E-12,-2.55972036858199,
-10.000000000009));
#28941=CARTESIAN_POINT('Ctrl Pts',(-2.55972036858699,-2.55972036858199,
-10.0000000000112));
#28942=CARTESIAN_POINT('Ctrl Pts',(-2.55972036858699,2.4669440334204E-15,
-10.0000000000125));
#28943=CARTESIAN_POINT('Ctrl Pts',(-2.55972036858699,2.55972036858199,-10.0000000000138));
#28944=CARTESIAN_POINT('Ctrl Pts',(-4.99935688766102E-12,2.55972036858199,
-10.0000000000116));
#28945=CARTESIAN_POINT('Ctrl Pts',(2.55972036857699,2.55972036858199,-10.0000000000095));
#28946=CARTESIAN_POINT('Ctrl Pts',(2.55972036857699,2.46694403342024E-15,
-10.0000000000082));
#28947=CARTESIAN_POINT('Ctrl Pts',(1.09212159715655,2.46694403834357E-15,
-9.99999999999975));
#28948=CARTESIAN_POINT('Ctrl Pts',(1.09212159715655,-1.09212159716155,-9.9999999999992));
#28949=CARTESIAN_POINT('Ctrl Pts',(-4.99935688767059E-12,-1.09212159716155,
-10.0000000000001));
#28950=CARTESIAN_POINT('Ctrl Pts',(-1.09212159716655,-1.09212159716155,
-10.000000000001));
#28951=CARTESIAN_POINT('Ctrl Pts',(-1.09212159716655,2.46694403834408E-15,
-10.0000000000016));
#28952=CARTESIAN_POINT('Ctrl Pts',(-1.09212159716655,1.09212159716156,-10.0000000000021));
#28953=CARTESIAN_POINT('Ctrl Pts',(-4.99935688766966E-12,1.09212159716156,
-10.0000000000012));
#28954=CARTESIAN_POINT('Ctrl Pts',(1.09212159715655,1.09212159716156,-10.0000000000003));
#28955=CARTESIAN_POINT('Ctrl Pts',(1.09212159715655,2.46694403834357E-15,
-9.99999999999975));
#28956=CARTESIAN_POINT('',(-0.2485901447084,-1.397638819231,-9.973011580318));
#28957=CARTESIAN_POINT('',(0.2485901447084,-1.397638819231,-9.973011580318));
#28958=CARTESIAN_POINT('Ctrl Pts',(0.24859014470844,-1.39763881923147,-9.97301158031942));
#28959=CARTESIAN_POINT('Ctrl Pts',(0.163988452831422,-1.39785090473685,
-9.97543572873859));
#28960=CARTESIAN_POINT('Ctrl Pts',(0.0808409165723131,-1.39794227815784,
-9.97648013171962));
#28961=CARTESIAN_POINT('Ctrl Pts',(-0.0808409165790198,-1.39794227815785,
-9.97648013171975));
#28962=CARTESIAN_POINT('Ctrl Pts',(-0.163988452834823,-1.39785090473688,
-9.97543572873894));
#28963=CARTESIAN_POINT('Ctrl Pts',(-0.24859014470846,-1.39763881923153,
-9.97301158032012));
#28964=CARTESIAN_POINT('',(0.4994251259956,-1.150376451473,-9.993429160062));
#28965=CARTESIAN_POINT('Ctrl Pts',(0.248590144708445,-1.39763881923184,
-9.97301158031936));
#28966=CARTESIAN_POINT('Ctrl Pts',(0.266345257726262,-1.39759430945868,
-9.97250283128374));
#28967=CARTESIAN_POINT('Ctrl Pts',(0.284094629964267,-1.39567756906844,
-9.97224058239354));
#28968=CARTESIAN_POINT('Ctrl Pts',(0.301536754642562,-1.39189823089679,
-9.97224070208607));
#28969=CARTESIAN_POINT('Ctrl Pts',(0.310675342511096,-1.38991809289162,
-9.9722407647975));
#28970=CARTESIAN_POINT('Ctrl Pts',(0.319697231577847,-1.38743358849169,
-9.9723125850535));
#28971=CARTESIAN_POINT('Ctrl Pts',(0.360053184989107,-1.37387856724409,
-9.97296163608247));
#28972=CARTESIAN_POINT('Ctrl Pts',(0.389149980282598,-1.35721565994091,
-9.97436868233086));
#28973=CARTESIAN_POINT('Ctrl Pts',(0.438990275319011,-1.31376842357764,
-9.97850849048035));
#28974=CARTESIAN_POINT('Ctrl Pts',(0.459310846586711,-1.28745433645393,
-9.98118840839364));
#28975=CARTESIAN_POINT('Ctrl Pts',(0.488183202022476,-1.2290475577898,-9.98684098470683));
#28976=CARTESIAN_POINT('Ctrl Pts',(0.496681676024958,-1.19763175363616,
-9.98974371060822));
#28977=CARTESIAN_POINT('Ctrl Pts',(0.499206546933211,-1.16041155214929,
-9.99267187288286));
#28978=CARTESIAN_POINT('Ctrl Pts',(0.49939251014142,-1.15539199227997,-9.99305635913868));
#28979=CARTESIAN_POINT('Ctrl Pts',(0.499425125995968,-1.15037645147301,
-9.99342916006207));
#28980=CARTESIAN_POINT('',(0.5,-0.9709426260066,-10.));
#28981=CARTESIAN_POINT('Ctrl Pts',(0.499425125995589,-1.15037645147301,
-9.99342916006209));
#28982=CARTESIAN_POINT('Ctrl Pts',(0.499823732040743,-1.08908034523772,
-9.99798524800639));
#28983=CARTESIAN_POINT('Ctrl Pts',(0.499999999999975,-1.02886065465466,
-9.99999999999972));
#28984=CARTESIAN_POINT('Ctrl Pts',(0.499999999999978,-0.970942626013781,
-9.99999999999975));
#28985=CARTESIAN_POINT('',(0.9709426260066,-0.5,-10.));
#28986=CARTESIAN_POINT('Origin',(0.,0.,-10.));
#28987=CARTESIAN_POINT('',(1.150376451473,-0.4994251259956,-9.993429160062));
#28988=CARTESIAN_POINT('Ctrl Pts',(0.970942626011364,-0.499999999999965,
-9.99999999999959));
#28989=CARTESIAN_POINT('Ctrl Pts',(1.02886065465299,-0.49999999999997,-9.99999999999966));
#28990=CARTESIAN_POINT('Ctrl Pts',(1.08908034523686,-0.49982373204072,-9.99798524800613));
#28991=CARTESIAN_POINT('Ctrl Pts',(1.15037645147297,-0.499425125995553,
-9.99342916006167));
#28992=CARTESIAN_POINT('',(1.397638819231,-0.2485901447084,-9.973011580318));
#28993=CARTESIAN_POINT('Ctrl Pts',(1.15037645147297,-0.499425125995932,
-9.99342916006166));
#28994=CARTESIAN_POINT('Ctrl Pts',(1.16585150547838,-0.4993244923594,-9.99227891233267));
#28995=CARTESIAN_POINT('Ctrl Pts',(1.1813119375003,-0.497764366616508,-9.99102091698527));
#28996=CARTESIAN_POINT('Ctrl Pts',(1.22820384051413,-0.488479515534905,
-9.98696801305249));
#28997=CARTESIAN_POINT('Ctrl Pts',(1.2582878105144,-0.476056452234761,-9.98403403393921));
#28998=CARTESIAN_POINT('Ctrl Pts',(1.3120898695489,-0.440364616164326,-9.9787167926228));
#28999=CARTESIAN_POINT('Ctrl Pts',(1.33530269455742,-0.417419016315832,
-9.97639129073107));
#29000=CARTESIAN_POINT('Ctrl Pts',(1.37195593643593,-0.363749347026123,
-9.97313064215981));
#29001=CARTESIAN_POINT('Ctrl Pts',(1.38498091076259,-0.333461063805117,
-9.97224092115826));
#29002=CARTESIAN_POINT('Ctrl Pts',(1.39189823089696,-0.301536754641286,
-9.97224070208509));
#29003=CARTESIAN_POINT('Ctrl Pts',(1.39413558307741,-0.291211090752747,
-9.97224063122762));
#29004=CARTESIAN_POINT('Ctrl Pts',(1.39572483998331,-0.280755792323049,
-9.97233220873014));
#29005=CARTESIAN_POINT('Ctrl Pts',(1.39729372860019,-0.263023020533822,
-9.97263847784447));
#29006=CARTESIAN_POINT('Ctrl Pts',(1.39762074000317,-0.255802015808498,
-9.9728049337899));
#29007=CARTESIAN_POINT('Ctrl Pts',(1.39763881923175,-0.248590144708412,
-9.97301158031834));
#29008=CARTESIAN_POINT('',(1.39794229184068,1.42576569662847E-14,-9.97648028811549));
#29009=CARTESIAN_POINT('Origin',(1.39225353644748,-1.10267882883625E-6,
-9.91145751650082));
#29010=CARTESIAN_POINT('Ctrl Pts',(1.39794226787512,1.44289345718086E-14,
-9.97648013330951));
#29011=CARTESIAN_POINT('Ctrl Pts',(2.62691944453891,1.11142367514289E-13,
-9.78632055714307));
#29012=CARTESIAN_POINT('Ctrl Pts',(3.00000000000014,7.14494225807769E-13,
-8.59999999999797));
#29013=CARTESIAN_POINT('',(1.397638819231,0.2485901447084,-9.973011580318));
#29014=CARTESIAN_POINT('Origin',(1.39225353644748,-1.10267882883625E-6,
-9.91145751650082));
#29015=CARTESIAN_POINT('',(1.150376451473,0.4994251259956,-9.993429160062));
#29016=CARTESIAN_POINT('Ctrl Pts',(1.39763881923178,0.248590144708423,-9.97301158031859));
#29017=CARTESIAN_POINT('Ctrl Pts',(1.39759430945861,0.266345257725831,-9.972502831283));
#29018=CARTESIAN_POINT('Ctrl Pts',(1.39567756906846,0.284094629963428,-9.97224058239284));
#29019=CARTESIAN_POINT('Ctrl Pts',(1.39189823089698,0.301536754641337,-9.97224070208539));
#29020=CARTESIAN_POINT('Ctrl Pts',(1.38991809289194,0.310675342509477,-9.97224076479684));
#29021=CARTESIAN_POINT('Ctrl Pts',(1.38743358849219,0.319697231575848,-9.97231258505284));
#29022=CARTESIAN_POINT('Ctrl Pts',(1.3738785672451,0.360053184986904,-9.97296163608185));
#29023=CARTESIAN_POINT('Ctrl Pts',(1.35721565994219,0.38914998028057,-9.97436868233028));
#29024=CARTESIAN_POINT('Ctrl Pts',(1.31376842357938,0.438990275317438,-9.97850849047988));
#29025=CARTESIAN_POINT('Ctrl Pts',(1.28745433645583,0.459310846585399,-9.98118840839324));
#29026=CARTESIAN_POINT('Ctrl Pts',(1.22904755779197,0.488183202021726,-9.98684098470657));
#29027=CARTESIAN_POINT('Ctrl Pts',(1.1976317536384,0.49668167602451,-9.98974371060802));
#29028=CARTESIAN_POINT('Ctrl Pts',(1.1604115521508,0.499206546933161,-9.99267187288281));
#29029=CARTESIAN_POINT('Ctrl Pts',(1.15539199228073,0.499392510141422,-9.99305635913871));
#29030=CARTESIAN_POINT('Ctrl Pts',(1.15037645147301,0.499425125995976,-9.99342916006216));
#29031=CARTESIAN_POINT('',(0.9709426260066,0.5,-10.));
#29032=CARTESIAN_POINT('Ctrl Pts',(1.15037645147301,0.499425125995597,-9.99342916006217));
#29033=CARTESIAN_POINT('Ctrl Pts',(1.08908034523688,0.499823732040765,-9.99798524800664));
#29034=CARTESIAN_POINT('Ctrl Pts',(1.02886065465299,0.500000000000005,-10.0000000000001));
#29035=CARTESIAN_POINT('Ctrl Pts',(0.970942626011344,0.500000000000009,
-10.0000000000001));
#29036=CARTESIAN_POINT('',(0.5,0.9709426260066,-10.));
#29037=CARTESIAN_POINT('Origin',(0.,0.,-10.));
#29038=CARTESIAN_POINT('',(0.4994251259956,1.150376451473,-9.993429160062));
#29039=CARTESIAN_POINT('Ctrl Pts',(0.500000000000065,0.970942626013742,
-10.0000000000007));
#29040=CARTESIAN_POINT('Ctrl Pts',(0.500000000000081,1.02886065465465,-10.0000000000009));
#29041=CARTESIAN_POINT('Ctrl Pts',(0.499823732040839,1.08908034523776,-9.99798524800749));
#29042=CARTESIAN_POINT('Ctrl Pts',(0.499425125995691,1.15037645147309,-9.99342916006325));
#29043=CARTESIAN_POINT('',(0.2485901447084,1.397638819231,-9.973011580318));
#29044=CARTESIAN_POINT('Ctrl Pts',(0.49942512599607,1.15037645147309,-9.99342916006323));
#29045=CARTESIAN_POINT('Ctrl Pts',(0.499324492359546,1.1658515054781,-9.99227891233432));
#29046=CARTESIAN_POINT('Ctrl Pts',(0.497764366616736,1.18131193749962,-9.99102091698699));
#29047=CARTESIAN_POINT('Ctrl Pts',(0.48847951553546,1.2282038405131,-9.98696801305439));
#29048=CARTESIAN_POINT('Ctrl Pts',(0.476056452235479,1.25828781051344,-9.9840340339412));
#29049=CARTESIAN_POINT('Ctrl Pts',(0.440364616165319,1.31208986954814,-9.97871679262494));
#29050=CARTESIAN_POINT('Ctrl Pts',(0.417419016316943,1.33530269455678,-9.97639129073328));
#29051=CARTESIAN_POINT('Ctrl Pts',(0.363749347027429,1.37195593643556,-9.97313064216213));
#29052=CARTESIAN_POINT('Ctrl Pts',(0.333461063806484,1.38498091076238,-9.97224092116061));
#29053=CARTESIAN_POINT('Ctrl Pts',(0.30153675464268,1.39189823089692,-9.97224070208747));
#29054=CARTESIAN_POINT('Ctrl Pts',(0.291211090753734,1.3941355830775,-9.97224063123));
#29055=CARTESIAN_POINT('Ctrl Pts',(0.280755792323659,1.39572483998349,-9.97233220873254));
#29056=CARTESIAN_POINT('Ctrl Pts',(0.263023020533999,1.39729372860041,-9.97263847784689));
#29057=CARTESIAN_POINT('Ctrl Pts',(0.255802015808621,1.39762074000339,-9.97280493379232));
#29058=CARTESIAN_POINT('Ctrl Pts',(0.248590144708482,1.39763881923197,-9.97301158032077));
#29059=CARTESIAN_POINT('',(-0.2485901447084,1.397638819231,-9.973011580318));
#29060=CARTESIAN_POINT('Ctrl Pts',(0.24859014470848,1.39763881923159,-9.97301158032083));
#29061=CARTESIAN_POINT('Ctrl Pts',(0.163988452831448,1.39785090473697,-9.97543572874));
#29062=CARTESIAN_POINT('Ctrl Pts',(0.080840916572326,1.39794227815797,-9.97648013172102));
#29063=CARTESIAN_POINT('Ctrl Pts',(-0.0808409165790325,1.39794227815798,
-9.97648013172116));
#29064=CARTESIAN_POINT('Ctrl Pts',(-0.163988452834849,1.397850904737,-9.97543572874035));
#29065=CARTESIAN_POINT('Ctrl Pts',(-0.248590144708499,1.39763881923165,
-9.97301158032152));
#29066=CARTESIAN_POINT('',(-0.4994251259956,1.150376451473,-9.993429160062));
#29067=CARTESIAN_POINT('Ctrl Pts',(-0.248590144708506,1.39763881923203,
-9.97301158032146));
#29068=CARTESIAN_POINT('Ctrl Pts',(-0.266345257725687,1.39759430945888,
-9.9725028312859));
#29069=CARTESIAN_POINT('Ctrl Pts',(-0.284094629963059,1.39567756906879,
-9.97224058239576));
#29070=CARTESIAN_POINT('Ctrl Pts',(-0.301536754640759,1.39189823089742,
-9.97224070208831));
#29071=CARTESIAN_POINT('Ctrl Pts',(-0.310675342509529,1.38991809289227,
-9.97224076479976));
#29072=CARTESIAN_POINT('Ctrl Pts',(-0.319697231576514,1.38743358849235,
-9.97231258505576));
#29073=CARTESIAN_POINT('Ctrl Pts',(-0.360053184988087,1.3738785672449,-9.97296163608481));
#29074=CARTESIAN_POINT('Ctrl Pts',(-0.389149980281671,1.35721565994188,
-9.97436868233322));
#29075=CARTESIAN_POINT('Ctrl Pts',(-0.438990275318315,1.3137684235789,-9.97850849048274));
#29076=CARTESIAN_POINT('Ctrl Pts',(-0.459310846586145,1.28745433645531,
-9.98118840839603));
#29077=CARTESIAN_POINT('Ctrl Pts',(-0.488183202022219,1.22904755779138,
-9.98684098470917));
#29078=CARTESIAN_POINT('Ctrl Pts',(-0.496681676024877,1.19763175363781,
-9.9897437106105));
#29079=CARTESIAN_POINT('Ctrl Pts',(-0.499206546933379,1.16041155215047,
-9.99267187288511));
#29080=CARTESIAN_POINT('Ctrl Pts',(-0.49939251014162,1.15539199228065,-9.99305635914096));
#29081=CARTESIAN_POINT('Ctrl Pts',(-0.49942512599617,1.15037645147318,-9.99342916006438));
#29082=CARTESIAN_POINT('',(-0.5,0.9709426260066,-10.));
#29083=CARTESIAN_POINT('Ctrl Pts',(-0.499425125995791,1.15037645147318,
-9.99342916006439));
#29084=CARTESIAN_POINT('Ctrl Pts',(-0.49982373204092,1.08908034523958,-9.99798524800841));
#29085=CARTESIAN_POINT('Ctrl Pts',(-0.500000000000139,1.02886065465818,
-10.0000000000016));
#29086=CARTESIAN_POINT('Ctrl Pts',(-0.500000000000137,0.970942626018854,
-10.0000000000016));
#29087=CARTESIAN_POINT('',(-0.9709426260066,0.5,-10.));
#29088=CARTESIAN_POINT('Origin',(0.,0.,-10.));
#29089=CARTESIAN_POINT('',(-1.150376451473,0.4994251259956,-9.993429160062));
#29090=CARTESIAN_POINT('Ctrl Pts',(-0.97094262602127,0.50000000000015,-10.0000000000017));
#29091=CARTESIAN_POINT('Ctrl Pts',(-1.02886065465985,0.500000000000184,
-10.0000000000021));
#29092=CARTESIAN_POINT('Ctrl Pts',(-1.08908034524044,0.499823732040942,
-9.99798524800866));
#29093=CARTESIAN_POINT('Ctrl Pts',(-1.15037645147321,0.499425125995827,
-9.99342916006481));
#29094=CARTESIAN_POINT('',(-1.397638819231,0.2485901447084,-9.973011580318));
#29095=CARTESIAN_POINT('Ctrl Pts',(-1.1503764514732,0.499425125996206,-9.99342916006479));
#29096=CARTESIAN_POINT('Ctrl Pts',(-1.16585150547846,0.499324492359686,
-9.99227891233591));
#29097=CARTESIAN_POINT('Ctrl Pts',(-1.18131193750023,0.497764366616836,
-9.9910209169886));
#29098=CARTESIAN_POINT('Ctrl Pts',(-1.22820384051396,0.488479515535382,
-9.9869680130561));
#29099=CARTESIAN_POINT('Ctrl Pts',(-1.25828781051428,0.476056452235305,
-9.98403403394297));
#29100=CARTESIAN_POINT('Ctrl Pts',(-1.31208986954888,0.440364616164987,
-9.9787167926268));
#29101=CARTESIAN_POINT('Ctrl Pts',(-1.33530269455747,0.417419016316536,
-9.97639129073516));
#29102=CARTESIAN_POINT('Ctrl Pts',(-1.3719559364361,0.363749347026876,-9.97313064216401));
#29103=CARTESIAN_POINT('Ctrl Pts',(-1.38498091076282,0.333461063805877,
-9.97224092116247));
#29104=CARTESIAN_POINT('Ctrl Pts',(-1.39189823089725,0.301536754642035,
-9.97224070208929));
#29105=CARTESIAN_POINT('Ctrl Pts',(-1.39413558307793,0.29121109075249,-9.97224063123181));
#29106=CARTESIAN_POINT('Ctrl Pts',(-1.39572483998393,0.280755792321815,
-9.97233220873434));
#29107=CARTESIAN_POINT('Ctrl Pts',(-1.39729372860064,0.263023020532381,
-9.97263847784868));
#29108=CARTESIAN_POINT('Ctrl Pts',(-1.39762074000354,0.255802015807838,
-9.97280493379408));
#29109=CARTESIAN_POINT('Ctrl Pts',(-1.39763881923212,0.248590144708531,
-9.97301158032249));
#29110=CARTESIAN_POINT('',(-1.397638819231,-0.2485901447085,-9.973011580318));
#29111=CARTESIAN_POINT('Origin',(-1.39225353644736,1.10267764200783E-6,
-9.91145751649949));
#29112=CARTESIAN_POINT('',(-1.150376451473,-0.4994251259956,-9.993429160062));
#29113=CARTESIAN_POINT('Ctrl Pts',(-1.3976388192321,-0.248590144708628,
-9.97301158032223));
#29114=CARTESIAN_POINT('Ctrl Pts',(-1.39759430945894,-0.266345257726185,
-9.97250283128663));
#29115=CARTESIAN_POINT('Ctrl Pts',(-1.39567756906876,-0.284094629963931,
-9.97224058239646));
#29116=CARTESIAN_POINT('Ctrl Pts',(-1.39189823089723,-0.301536754641984,
-9.97224070208898));
#29117=CARTESIAN_POINT('Ctrl Pts',(-1.38991809289195,-0.310675342511139,
-9.97224076480042));
#29118=CARTESIAN_POINT('Ctrl Pts',(-1.38743358849185,-0.319697231578498,
-9.97231258505642));
#29119=CARTESIAN_POINT('Ctrl Pts',(-1.37387856724389,-0.360053184990289,
-9.97296163608543));
#29120=CARTESIAN_POINT('Ctrl Pts',(-1.3572156599406,-0.389149980283697,
-9.9743686823338));
#29121=CARTESIAN_POINT('Ctrl Pts',(-1.31376842357717,-0.438990275319886,
-9.97850849048321));
#29122=CARTESIAN_POINT('Ctrl Pts',(-1.2874543364534,-0.459310846587456,
-9.98118840839643));
#29123=CARTESIAN_POINT('Ctrl Pts',(-1.22904755778921,-0.488183202022969,
-9.98684098470943));
#29124=CARTESIAN_POINT('Ctrl Pts',(-1.19763175363558,-0.496681676025323,
-9.98974371061069));
#29125=CARTESIAN_POINT('Ctrl Pts',(-1.16041155214897,-0.499206546933428,
-9.99267187288515));
#29126=CARTESIAN_POINT('Ctrl Pts',(-1.15539199227989,-0.499392510141618,
-9.99305635914094));
#29127=CARTESIAN_POINT('Ctrl Pts',(-1.15037645147317,-0.499425125996162,
-9.99342916006429));
#29128=CARTESIAN_POINT('',(-0.9709426260066,-0.5,-10.));
#29129=CARTESIAN_POINT('Ctrl Pts',(-1.15037645147317,-0.499425125995783,
-9.9934291600643));
#29130=CARTESIAN_POINT('Ctrl Pts',(-1.08908034524041,-0.499823732040897,
-9.99798524800816));
#29131=CARTESIAN_POINT('Ctrl Pts',(-1.02886065465985,-0.50000000000011,
-10.0000000000013));
#29132=CARTESIAN_POINT('Ctrl Pts',(-0.970942626021291,-0.500000000000106,
-10.0000000000012));
#29133=CARTESIAN_POINT('',(-0.5,-0.9709426260066,-10.));
#29134=CARTESIAN_POINT('Origin',(0.,0.,-10.));
#29135=CARTESIAN_POINT('',(-0.4994251259956,-1.150376451473,-9.993429160062));
#29136=CARTESIAN_POINT('Ctrl Pts',(-0.500000000000051,-0.970942626018893,
-10.0000000000006));
#29137=CARTESIAN_POINT('Ctrl Pts',(-0.500000000000073,-1.02886065465818,
-10.0000000000008));
#29138=CARTESIAN_POINT('Ctrl Pts',(-0.499823732040823,-1.08908034523954,
-9.99798524800731));
#29139=CARTESIAN_POINT('Ctrl Pts',(-0.499425125995689,-1.15037645147309,
-9.99342916006323));
#29140=CARTESIAN_POINT('Ctrl Pts',(-0.499425125996068,-1.15037645147309,
-9.99342916006322));
#29141=CARTESIAN_POINT('Ctrl Pts',(-0.49932449235954,-1.16585150547875,
-9.99227891233426));
#29142=CARTESIAN_POINT('Ctrl Pts',(-0.497764366616606,-1.18131193750091,
-9.99102091698688));
#29143=CARTESIAN_POINT('Ctrl Pts',(-0.488479515534827,-1.22820384051498,
-9.9869680130542));
#29144=CARTESIAN_POINT('Ctrl Pts',(-0.476056452234594,-1.25828781051522,
-9.98403403394099));
#29145=CARTESIAN_POINT('Ctrl Pts',(-0.440364616163992,-1.31208986954964,
-9.97871679262466));
#29146=CARTESIAN_POINT('Ctrl Pts',(-0.417419016315419,-1.33530269455811,
-9.97639129073295));
#29147=CARTESIAN_POINT('Ctrl Pts',(-0.363749347025575,-1.37195593643646,
-9.97313064216169));
#29148=CARTESIAN_POINT('Ctrl Pts',(-0.333461063804512,-1.38498091076303,
-9.97224092116012));
#29149=CARTESIAN_POINT('Ctrl Pts',(-0.301536754640641,-1.3918982308973,
-9.97224070208691));
#29150=CARTESIAN_POINT('Ctrl Pts',(-0.291211090751498,-1.39413558307784,
-9.97224063122943));
#29151=CARTESIAN_POINT('Ctrl Pts',(-0.280755792321202,-1.39572483998376,
-9.97233220873195));
#29152=CARTESIAN_POINT('Ctrl Pts',(-0.263023020532205,-1.39729372860043,
-9.97263847784626));
#29153=CARTESIAN_POINT('Ctrl Pts',(-0.255802015807715,-1.39762074000333,
-9.97280493379166));
#29154=CARTESIAN_POINT('Ctrl Pts',(-0.248590144708461,-1.39763881923191,
-9.97301158032005));
#29155=CARTESIAN_POINT('Origin',(1.4,0.6599764278095,-10.));
#29156=CARTESIAN_POINT('',(1.268767004711,-0.1197183301882,-8.5));
#29157=CARTESIAN_POINT('',(1.397638819231,-0.2485901447084,-9.973011580318));
#29158=CARTESIAN_POINT('',(1.268767004711,0.1197183301882,-8.5));
#29159=CARTESIAN_POINT('',(1.268767004711,0.1197183301882,-8.5));
#29160=CARTESIAN_POINT('',(1.397638819231,0.2485901447084,-9.973011580318));
#29161=CARTESIAN_POINT('Origin',(2.321412939997,-1.421412939997,-23.40022640802));
#29162=CARTESIAN_POINT('',(1.019718330188,-0.3687670047111,-8.5));
#29163=CARTESIAN_POINT('Origin',(1.01781204532566,-0.117812045325658,-8.5));
#29164=CARTESIAN_POINT('',(1.150376451473,-0.4994251259956,-9.993429160062));
#29165=CARTESIAN_POINT('Origin',(0.,0.,-8.5));
#29166=CARTESIAN_POINT('',(-0.3687670047111,0.617815679234,-8.5));
#29167=CARTESIAN_POINT('',(-0.3687670047111,1.019718330188,-8.5));
#29168=CARTESIAN_POINT('',(-0.3687670047111,0.617815679234,-8.5));
#29169=CARTESIAN_POINT('',(-0.1197183301882,1.268767004711,-8.5));
#29170=CARTESIAN_POINT('Origin',(-0.117812045325658,1.01781204532566,-8.5));
#29171=CARTESIAN_POINT('',(0.1197183301882,1.268767004711,-8.5));
#29172=CARTESIAN_POINT('',(-0.1197183301882,1.268767004711,-8.5));
#29173=CARTESIAN_POINT('',(0.3687670047111,1.019718330188,-8.5));
#29174=CARTESIAN_POINT('Origin',(0.117812045325658,1.01781204532566,-8.5));
#29175=CARTESIAN_POINT('',(0.3687670047111,0.617815679234,-8.5));
#29176=CARTESIAN_POINT('',(0.3687670047111,1.019718330188,-8.5));
#29177=CARTESIAN_POINT('',(0.617815679234,0.3687670047111,-8.5));
#29178=CARTESIAN_POINT('Origin',(0.619721964096652,0.619721964096652,-8.5));
#29179=CARTESIAN_POINT('',(1.019718330188,0.3687670047111,-8.5));
#29180=CARTESIAN_POINT('',(0.617815679234,0.3687670047111,-8.5));
#29181=CARTESIAN_POINT('Origin',(1.01781204532566,0.117812045325658,-8.5));
#29182=CARTESIAN_POINT('',(0.6178156792341,-0.3687670047111,-8.5));
#29183=CARTESIAN_POINT('',(1.019718330188,-0.3687670047111,-8.5));
#29184=CARTESIAN_POINT('',(0.3687670047111,-0.6178156792341,-8.5));
#29185=CARTESIAN_POINT('Origin',(0.619721964096385,-0.619721964096385,-8.5));
#29186=CARTESIAN_POINT('',(0.3687670047111,-1.019718330188,-8.5));
#29187=CARTESIAN_POINT('',(0.3687670047111,-0.6178156792341,-8.5));
#29188=CARTESIAN_POINT('',(0.1197183301882,-1.268767004711,-8.5));
#29189=CARTESIAN_POINT('Origin',(0.117812045325658,-1.01781204532566,-8.5));
#29190=CARTESIAN_POINT('',(-0.1197183301882,-1.268767004711,-8.5));
#29191=CARTESIAN_POINT('',(0.1197183301882,-1.268767004711,-8.5));
#29192=CARTESIAN_POINT('',(-0.3687670047111,-1.019718330188,-8.5));
#29193=CARTESIAN_POINT('Origin',(-0.117812045325658,-1.01781204532566,-8.5));
#29194=CARTESIAN_POINT('',(-0.3687670047111,-0.6178156792341,-8.5));
#29195=CARTESIAN_POINT('',(-0.3687670047111,-1.019718330188,-8.5));
#29196=CARTESIAN_POINT('',(-0.6178156792341,-0.3687670047111,-8.5));
#29197=CARTESIAN_POINT('Origin',(-0.619721964096385,-0.619721964096385,
-8.5));
#29198=CARTESIAN_POINT('',(-1.019718330188,-0.3687670047111,-8.5));
#29199=CARTESIAN_POINT('',(-0.6178156792341,-0.3687670047111,-8.5));
#29200=CARTESIAN_POINT('',(-1.268767004711,-0.1197183301882,-8.5));
#29201=CARTESIAN_POINT('Origin',(-1.01781204532566,-0.117812045325658,-8.5));
#29202=CARTESIAN_POINT('',(-1.268767004711,0.1197183301882,-8.5));
#29203=CARTESIAN_POINT('',(-1.268767004711,-0.1197183301882,-8.5));
#29204=CARTESIAN_POINT('',(-1.019718330188,0.3687670047111,-8.5));
#29205=CARTESIAN_POINT('Origin',(-1.01781204532566,0.117812045325658,-8.5));
#29206=CARTESIAN_POINT('',(-0.6178156792341,0.3687670047111,-8.5));
#29207=CARTESIAN_POINT('',(-1.019718330188,0.3687670047111,-8.5));
#29208=CARTESIAN_POINT('Origin',(-0.619721964096385,0.619721964096385,-8.5));
#29209=CARTESIAN_POINT('Origin',(-0.5,0.3400235721905,-10.));
#29210=CARTESIAN_POINT('',(-0.5,0.7490486745229,-10.));
#29211=CARTESIAN_POINT('',(-0.5,0.7490486745229,-10.));
#29212=CARTESIAN_POINT('',(-0.4994251259956,1.150376451473,-9.993429160062));
#29213=CARTESIAN_POINT('',(-0.3687670047111,0.617815679234,-8.5));
#29214=CARTESIAN_POINT('Origin',(0.,0.,-10.));
#29215=CARTESIAN_POINT('',(0.5,0.7490486745229,-10.));
#29216=CARTESIAN_POINT('',(0.5,0.9709426260066,-10.));
#29217=CARTESIAN_POINT('',(0.7490486745229,0.5,-10.));
#29218=CARTESIAN_POINT('',(0.7490486745229,0.5,-10.));
#29219=CARTESIAN_POINT('Origin',(0.750954959385537,0.750954959385537,-10.));
#29220=CARTESIAN_POINT('Origin',(0.,0.,-10.));
#29221=CARTESIAN_POINT('',(0.7490486745229,-0.5,-10.));
#29222=CARTESIAN_POINT('',(0.9709426260066,-0.5,-10.));
#29223=CARTESIAN_POINT('',(0.5,-0.7490486745229,-10.));
#29224=CARTESIAN_POINT('',(0.5,-0.7490486745229,-10.));
#29225=CARTESIAN_POINT('Origin',(0.75095495938527,-0.75095495938527,-10.));
#29226=CARTESIAN_POINT('Origin',(0.,0.,-10.));
#29227=CARTESIAN_POINT('',(-0.5,-0.7490486745229,-10.));
#29228=CARTESIAN_POINT('',(-0.5,-0.9709426260066,-10.));
#29229=CARTESIAN_POINT('',(-0.7490486745229,-0.5,-10.));
#29230=CARTESIAN_POINT('',(-0.7490486745229,-0.5,-10.));
#29231=CARTESIAN_POINT('Origin',(-0.75095495938527,-0.75095495938527,-10.));
#29232=CARTESIAN_POINT('Origin',(0.,0.,-10.));
#29233=CARTESIAN_POINT('',(-0.7490486745229,0.5,-10.));
#29234=CARTESIAN_POINT('',(-0.9709426260066,0.5,-10.));
#29235=CARTESIAN_POINT('Origin',(-0.75095495938527,0.75095495938527,-10.));
#29236=CARTESIAN_POINT('Origin',(0.5,1.559976427809,-10.));
#29237=CARTESIAN_POINT('',(0.3687670047111,0.617815679234,-8.5));
#29238=CARTESIAN_POINT('',(0.4994251259956,1.150376451473,-9.993429160062));
#29239=CARTESIAN_POINT('Origin',(1.421412939997,2.321412939997,-23.40022640802));
#29240=CARTESIAN_POINT('',(0.2485901447084,1.397638819231,-9.973011580318));
#29241=CARTESIAN_POINT('Origin',(-0.6599764278095,1.4,-10.));
#29242=CARTESIAN_POINT('',(-0.2485901447084,1.397638819231,-9.973011580318));
#29243=CARTESIAN_POINT('Origin',(-1.421412939997,2.321412939997,-23.40022640802));
#29244=CARTESIAN_POINT('Origin',(-1.4,-0.6599764278095,-10.));
#29245=CARTESIAN_POINT('',(-1.397638819231,0.2485901447084,-9.973011580318));
#29246=CARTESIAN_POINT('',(-1.397638819231,-0.2485901447085,-9.973011580318));
#29247=CARTESIAN_POINT('Origin',(-2.321412939997,1.421412939997,-23.40022640802));
#29248=CARTESIAN_POINT('',(-1.150376451473,0.4994251259956,-9.993429160062));
#29249=CARTESIAN_POINT('Origin',(-1.559976427809,0.5,-10.));
#29250=CARTESIAN_POINT('',(-0.6178156792341,0.3687670047111,-8.5));
#29251=CARTESIAN_POINT('Origin',(1.320743945967,-1.320743945967,13.67962684375));
#29252=CARTESIAN_POINT('Origin',(-2.321412939997,-1.421412939997,-23.40022640802));
#29253=CARTESIAN_POINT('',(-1.150376451473,-0.4994251259956,-9.993429160062));
#29254=CARTESIAN_POINT('Origin',(-0.3400235721905,-0.5,-10.));
#29255=CARTESIAN_POINT('',(-0.6178156792341,-0.3687670047111,-8.5));
#29256=CARTESIAN_POINT('Origin',(1.320743945967,1.320743945967,13.67962684375));
#29257=CARTESIAN_POINT('',(-0.3687670047111,-0.6178156792341,-8.5));
#29258=CARTESIAN_POINT('Origin',(-0.5,-1.559976427809,-10.));
#29259=CARTESIAN_POINT('',(-0.4994251259956,-1.150376451473,-9.993429160062));
#29260=CARTESIAN_POINT('Origin',(-1.421412939997,-2.321412939997,-23.40022640802));
#29261=CARTESIAN_POINT('',(-0.2485901447084,-1.397638819231,-9.973011580318));
#29262=CARTESIAN_POINT('Origin',(0.6599764278095,-1.4,-10.));
#29263=CARTESIAN_POINT('',(0.2485901447084,-1.397638819231,-9.973011580318));
#29264=CARTESIAN_POINT('Origin',(1.421412939997,-2.321412939997,-23.40022640802));
#29265=CARTESIAN_POINT('',(0.4994251259956,-1.150376451473,-9.993429160062));
#29266=CARTESIAN_POINT('Origin',(0.5,-0.3400235721905,-10.));
#29267=CARTESIAN_POINT('',(0.3687670047111,-0.6178156792341,-8.5));
#29268=CARTESIAN_POINT('Origin',(-1.320743945967,1.320743945967,13.67962684375));
#29269=CARTESIAN_POINT('',(0.6178156792341,-0.3687670047111,-8.5));
#29270=CARTESIAN_POINT('Origin',(1.559976427809,-0.5,-10.));
#29271=CARTESIAN_POINT('Origin',(-1.293999677209,-1.293999677209,13.37393845305));
#29272=CARTESIAN_POINT('',(0.617815679234,0.3687670047111,-8.5));
#29273=CARTESIAN_POINT('Origin',(0.3400235721905,0.5,-10.));
#29274=CARTESIAN_POINT('',(1.150376451473,0.4994251259956,-9.993429160062));
#29275=CARTESIAN_POINT('Origin',(2.321412939997,1.421412939997,-23.40022640802));
#52140=UNCERTAINTY_MEASURE_WITH_UNIT(LENGTH_MEASURE(0.01),#52165,
'DISTANCE_ACCURACY_VALUE',
'Maximum model space distance between geometric entities at asserted c
onnectivities');
#52149=UNCERTAINTY_MEASURE_WITH_UNIT(LENGTH_MEASURE(0.01),#52165,
'DISTANCE_ACCURACY_VALUE',
'Maximum model space distance between geometric entities at asserted c
onnectivities');
#52155=(
GEOMETRIC_REPRESENTATION_CONTEXT(3)
GLOBAL_UNCERTAINTY_ASSIGNED_CONTEXT((#52140))
GLOBAL_UNIT_ASSIGNED_CONTEXT((#52165,#52167,#52168))
REPRESENTATION_CONTEXT('','3D')
);
#52164=(
GEOMETRIC_REPRESENTATION_CONTEXT(3)
GLOBAL_UNCERTAINTY_ASSIGNED_CONTEXT((#52149))
GLOBAL_UNIT_ASSIGNED_CONTEXT((#52165,#52167,#52168))
REPRESENTATION_CONTEXT('','3D')
);
#52165=(
LENGTH_UNIT()
NAMED_UNIT(*)
SI_UNIT(.MILLI.,.METRE.)
);
#52167=(
NAMED_UNIT(*)
PLANE_ANGLE_UNIT()
SI_UNIT($,.RADIAN.)
);
#52168=(
NAMED_UNIT(*)
SI_UNIT($,.STERADIAN.)
SOLID_ANGLE_UNIT()
);
#52174=SHAPE_DEFINITION_REPRESENTATION(#52188,#52215);
#52188=PRODUCT_DEFINITION_SHAPE('',$,#52230);
#52215=SHAPE_REPRESENTATION('',(#9704),#52155);
#52224=PRODUCT_DEFINITION_CONTEXT('part definition',#52268,'design');
#52230=PRODUCT_DEFINITION('Screw M3','Screw M3',#52244,#52224);
#52244=PRODUCT_DEFINITION_FORMATION('',$,#52275);
#52268=APPLICATION_CONTEXT('Managed model based 3d engineering');
#52269=PRODUCT_CONTEXT('part definition',#52268,'mechanical');
#52275=PRODUCT('Screw M3','Screw M3','NOT SPECIFIED',(#52269));
#52319=COLOUR_RGB('Black',0.12,0.14,0.17);
#52320=FILL_AREA_STYLE_COLOUR('',#52319);
#52321=FILL_AREA_STYLE('',(#52320));
#52322=SURFACE_STYLE_FILL_AREA(#52321);
#52323=SURFACE_SIDE_STYLE('',(#52322));
#52324=SURFACE_STYLE_USAGE(.BOTH.,#52323);
#52325=PRESENTATION_STYLE_ASSIGNMENT((#52324));
ENDSEC;
END-ISO-10303-21;
